ISO-10303-21;
HEADER;
FILE_DESCRIPTION (('STEP AP214'),
    '1' );
FILE_NAME ('MirrorCaliper Body Half.step',
    '2026-09-24T10:28:59',
    ( '' ),
    ( '' ),
    'SwSTEP 2.0',
    'SolidWorks 2026',
    '' );
FILE_SCHEMA (( 'AUTOMOTIVE_DESIGN' ));
ENDSEC;

DATA;
#6=EDGE_CURVE ( 'NONE', #16160, #8560, #10428, .T. ) ;
#17=EDGE_CURVE ( 'NONE', #16386, #12240, #657, .T. ) ;
#24=DIRECTION ( 'NONE',  ( 0.000000000000000000, 0.000000000000000000, 1.000000000000000000 ) ) ;
#28=CYLINDRICAL_SURFACE ( 'NONE', #14824, 2.749999999999992006 ) ;
#32=CARTESIAN_POINT ( 'NONE',  ( 29.39961944441754227, -3.040961747597316744, 8.283357778048666020 ) ) ;
#33=FACE_OUTER_BOUND ( 'NONE', #10742, .T. ) ;
#40=CARTESIAN_POINT ( 'NONE',  ( 27.63266882139180680, -2.199775856772564708, 5.783357778048668685 ) ) ;
#41=CARTESIAN_POINT ( 'NONE',  ( 19.91592223102268733, -21.66952118561269458, 15.52717098632164117 ) ) ;
#45=CARTESIAN_POINT ( 'NONE',  ( 31.12210306526553083, -4.287250072544045665, 3.283357778048664244 ) ) ;
#46=DIRECTION ( 'NONE',  ( 0.000000000000000000, 1.000000000000000000, 0.000000000000000000 ) ) ;
#56=CARTESIAN_POINT ( 'NONE',  ( 28.75786045390062995, -2.691183018653962034, 4.705209693361167567 ) ) ;
#57=CARTESIAN_POINT ( 'NONE',  ( -15.92260893619738837, -28.39189527176317540, 12.00000000000000000 ) ) ;
#58=CARTESIAN_POINT ( 'NONE',  ( 23.00000000000000000, -16.21813761408365195, 0.000000000000000000 ) ) ;
#59=DIRECTION ( 'NONE',  ( 0.000000000000000000, 0.000000000000000000, 1.000000000000000000 ) ) ;
#60=VERTEX_POINT ( 'NONE', #9170 ) ;
#63=VERTEX_POINT ( 'NONE', #7643 ) ;
#64=CARTESIAN_POINT ( 'NONE',  ( 27.60205212784272177, -2.830435096530727446, 6.861505862736165362 ) ) ;
#65=CARTESIAN_POINT ( 'NONE',  ( 27.46709037723411839, -6.908327297984874882, 7.033357778048657138 ) ) ;
#67=CARTESIAN_POINT ( 'NONE',  ( 26.37178701114681800, -2.351687214456304797, 5.783357778048668685 ) ) ;
#68=ORIENTED_EDGE ( 'NONE', *, *, #11555, .T. ) ;
#79=CARTESIAN_POINT ( 'NONE',  ( 30.08145424927873535, -6.930706697444451336, 5.783357778048664244 ) ) ;
#83=EDGE_CURVE ( 'NONE', #825, #4804, #12452, .T. ) ;
#87=EDGE_LOOP ( 'NONE', ( #1855, #1887, #10424, #16720 ) ) ;
#88=ORIENTED_EDGE ( 'NONE', *, *, #6884, .F. ) ;
#90=CARTESIAN_POINT ( 'NONE',  ( 28.10549950023367316, -2.142809097641162897, 5.783357778048668685 ) ) ;
#98=ADVANCED_FACE ( 'NONE', ( #4634, #14352 ), #12979, .F. ) ;
#102=AXIS2_PLACEMENT_3D ( 'NONE', #2745, #9523, #13625 ) ;
#105=CARTESIAN_POINT ( 'NONE',  ( 31.03206908560819954, -5.751910973953721751, 8.283357778048660691 ) ) ;
#108=CARTESIAN_POINT ( 'NONE',  ( 32.89331279191618762, -2.620040694222726785, 3.283357778048666464 ) ) ;
#114=CARTESIAN_POINT ( 'NONE',  ( 31.97277696464621854, -6.702839660918840536, 5.783357778048664244 ) ) ;
#117=CARTESIAN_POINT ( 'NONE',  ( -23.02601376483258022, 3.965314980223224151, 6.000000000000000000 ) ) ;
#118=VERTEX_POINT ( 'NONE', #924 ) ;
#121=CARTESIAN_POINT ( 'NONE',  ( 29.19631194059803292, -2.001190877926593004, 6.453230759126469707 ) ) ;
#122=VERTEX_POINT ( 'NONE', #5078 ) ;
#124=DIRECTION ( 'NONE',  ( 0.000000000000000000, 0.000000000000000000, -1.000000000000000000 ) ) ;
#125=ORIENTED_EDGE ( 'NONE', *, *, #6084, .F. ) ;
#126=CARTESIAN_POINT ( 'NONE',  ( 26.66770885555339987, -3.370103022578743612, 3.283357778048666464 ) ) ;
#129=CARTESIAN_POINT ( 'NONE',  ( 27.17934203385504333, -30.00000000000000355, 0.000000000000000000 ) ) ;
#132=CARTESIAN_POINT ( 'NONE',  ( 31.27600417729400917, -6.449428405189353342, 4.533357778048659803 ) ) ;
#142=CARTESIAN_POINT ( 'NONE',  ( 30.01874226414561875, -2.539271660970221944, 4.705209693361167567 ) ) ;
#145=CARTESIAN_POINT ( 'NONE',  ( 31.55553118839817728, -4.235030543236534939, 3.627061608673664228 ) ) ;
#149=CARTESIAN_POINT ( 'NONE',  ( 28.24571643650507369, -4.633797857156355171, 3.627061608673664228 ) ) ;
#151=DIRECTION ( 'NONE',  ( 0.000000000000000000, 0.000000000000000000, -1.000000000000000000 ) ) ;
#153=CARTESIAN_POINT ( 'NONE',  ( 27.88665588685489993, -3.423116496867954162, 7.939653947423662927 ) ) ;
#154=ORIENTED_EDGE ( 'NONE', *, *, #5892, .F. ) ;
#156=CYLINDRICAL_SURFACE ( 'NONE', #2297, 2.749999999999992006 ) ;
#157=FACE_OUTER_BOUND ( 'NONE', #4677, .T. ) ;
#159=B_SPLINE_CURVE_WITH_KNOTS ( 'NONE', 3,
 ( #17069, #3694, #6069, #7869 ),
 .UNSPECIFIED., .F., .F.,
 ( 4, 4 ),
 ( 0.000000000000000000, 0.0006487028241592422868 ),
 .UNSPECIFIED. ) ;
#172=VERTEX_POINT ( 'NONE', #5336 ) ;
#173=ADVANCED_FACE ( 'NONE', ( #9510 ), #13344, .F. ) ;
#175=CARTESIAN_POINT ( 'NONE',  ( 30.04066231269008469, -3.163601260824890904, 3.627061608673666449 ) ) ;
#178=DIRECTION ( 'NONE',  ( 0.000000000000000000, 0.000000000000000000, -1.000000000000000000 ) ) ;
#184=ORIENTED_EDGE ( 'NONE', *, *, #3114, .F. ) ;
#190=DIRECTION ( 'NONE',  ( -1.000000000000000000, 0.000000000000000000, 0.000000000000000000 ) ) ;
#192=CARTESIAN_POINT ( 'NONE',  ( 31.59864285835955400, -2.049116061056871274, 4.533357778048667797 ) ) ;
#196=CARTESIAN_POINT ( 'NONE',  ( 26.87859896403794835, -7.316587507915443211, 5.113484796970851676 ) ) ;
#200=EDGE_LOOP ( 'NONE', ( #3718, #1302, #8199, #7677, #6005, #1633 ) ) ;
#201=EDGE_CURVE ( 'NONE', #3274, #13752, #311, .T. ) ;
#203=CARTESIAN_POINT ( 'NONE',  ( 3.248936832696173393, 17.78798921770683350, 17.00000000000000000 ) ) ;
#204=ORIENTED_EDGE ( 'NONE', *, *, #11417, .T. ) ;
#205=VECTOR ( 'NONE', #5367, 1000.000000000000227 ) ;
#210=CARTESIAN_POINT ( 'NONE',  ( 32.57506351453486815, -6.630276025878011126, 6.453230759126467042 ) ) ;
#215=CARTESIAN_POINT ( 'NONE',  ( 33.17547354829333273, -5.293800545841212291, 7.939653947423658487 ) ) ;
#217=AXIS2_PLACEMENT_3D ( 'NONE', #13648, #13735, #1318 ) ;
#221=DIRECTION ( 'NONE',  ( 0.9899494936611662466, -0.1414213562373111965, 0.000000000000000000 ) ) ;
#224=CARTESIAN_POINT ( 'NONE',  ( 28.67914455963771303, -4.581578327848842669, 3.283357778048664244 ) ) ;
#225=VERTEX_POINT ( 'NONE', #1017 ) ;
#226=CARTESIAN_POINT ( 'NONE',  ( 26.92924972366625980, -7.310485091653801781, 5.783357778048669573 ) ) ;
#228=CARTESIAN_POINT ( 'NONE',  ( 45.50000000000000000, -16.03270077640482683, 5.537981825772250843 ) ) ;
#230=ADVANCED_FACE ( 'NONE', ( #6542 ), #5163, .T. ) ;
#235=( GEOMETRIC_REPRESENTATION_CONTEXT ( 3 ) GLOBAL_UNCERTAINTY_ASSIGNED_CONTEXT ( ( #1389 ) ) GLOBAL_UNIT_ASSIGNED_CONTEXT ( ( #897, #4698, #14414 ) ) REPRESENTATION_CONTEXT ( 'NONE', 'WORKASPACE' ) );
#237=CARTESIAN_POINT ( 'NONE',  ( 31.70371634254663817, -2.036456781249897485, 7.033357778048666020 ) ) ;
#238=CARTESIAN_POINT ( 'NONE',  ( 29.52399153675929355, -1.971908820246954130, 5.783357778048668685 ) ) ;
#240=VECTOR ( 'NONE', #8984, 1000.000000000000000 ) ;
#242=CARTESIAN_POINT ( 'NONE',  ( 29.49337484321020497, -2.602568060005117090, 6.861505862736165362 ) ) ;
#246=CARTESIAN_POINT ( 'NONE',  ( 27.12922144900085186, -2.887401855662130146, 6.861505862736166250 ) ) ;
#248=AXIS2_PLACEMENT_3D ( 'NONE', #3421, #10388, #11749 ) ;
#256=ADVANCED_FACE ( 'NONE', ( #8427, #1643 ), #16881, .T. ) ;
#265=EDGE_CURVE ( 'NONE', #1659, #12087, #14509, .T. ) ;
#266=ORIENTED_EDGE ( 'NONE', *, *, #8133, .F. ) ;
#268=CARTESIAN_POINT ( 'NONE',  ( 27.75549246765397271, -7.200742295513424374, 5.783357778048658915 ) ) ;
#276=VECTOR ( 'NONE', #9402, 1000.000000000000227 ) ;
#277=LINE ( 'NONE', #4351, #8745 ) ;
#281=ORIENTED_EDGE ( 'NONE', *, *, #15299, .F. ) ;
#284=DIRECTION ( 'NONE',  ( 0.9899494936611662466, -0.1414213562373111965, 0.000000000000000000 ) ) ;
#285=CARTESIAN_POINT ( 'NONE',  ( -15.92260893619738837, -28.39189527176317540, 16.15082599432113142 ) ) ;
#288=CARTESIAN_POINT ( 'NONE',  ( 31.94023320572814484, -7.096308717197083560, 5.783357778048657138 ) ) ;
#290=VECTOR ( 'NONE', #14393, 1000.000000000000000 ) ;
#291=ORIENTED_EDGE ( 'NONE', *, *, #11495, .T. ) ;
#297=( BOUNDED_SURFACE ( )  B_SPLINE_SURFACE ( 1, 2, ( 
 ( #2861, #15197, #16560, #1329, #12111, #15107, #10908, #4144, #1250, #8037, #10736, #5570, #5480, #9559, #4046, #9474, #17694, #15013, #3878, #2779, #5217, #13662, #9391, #13829, #1416, #14933, #6939, #11088, #13573, #1154, #6676, #12207, #5305, #10826, #2693, #336, #16742, #6022, #9824, #15375, #8767, #5843, #145, #12649, #14022, #4493, #11547, #11262, #1693, #12921, #5748, #3051, #11366, #3136, #7410, #11170, #4404, #1607, #15648, #4314, #16935, #8571, #10007, #14299, #2958, #428, #5933, #1884, #506, #17116, #12739, #4670, #7137, #8487, #15553, #238, #8669, #16841, #5659, #12840, #9919, #14106, #12564, #15469, #11457, #10197, #7226, #15747, #8388, #13920, #14196, #1790, #1516, #17024, #7321, #4578, #10099, #3226, #7049, #17304, #13377, #9199, #6214, #9119, #17215, #7674, #3496, #14476, #4756, #13013, #6492, #10628, #863, #6120, #2156, #13284, #15921, #11732, #7583, #2060, #11648, #10465, #12006, #10281, #14658, #17588, #690, #17503, #15830, #13198, #959, #6395, #2240, #7753, #16026, #11913, #598, #5108, #4841, #7490, #2331, #5027, #3403, #3598, #10549, #7850, #16113, #9026, #3675, #10369, #14577, #14745, #8935, #13110, #775 ),
 ( #8849, #3320, #6302, #11824, #14384, #1966, #17402, #4932, #6566, #5194, #5614, #8440, #5799, #12613, #1562, #11131, #7186, #108, #9454, #13976, #3940, #10715, #13473, #6652, #12182, #1466, #13879, #15330, #11219, #12086, #6994, #16288, #1046, #2491, #3858, #14991, #12696, #2908, #9777, #3012, #192, #9368, #5704, #17673, #9287, #288, #2578, #13552, #4274, #16201, #14909, #7095, #3766, #8014, #14829, #1127, #8347, #17761, #5284, #2414, #16794, #7936, #15427, #12522, #16700, #10801, #16376, #4362, #9872, #14068, #8534, #1651, #4454, #14150, #385, #556, #3281, #14252, #11695, #8897, #1840, #11603, #5893, #10323, #12789, #11315, #17073, #3455, #8813, #16895, #12973, #3180, #17167, #15515, #7370, #13155, #3097, #5977, #14344, #7274, #11414, #6074, #8620, #8985, #4716, #16980, #14528, #7450, #10150, #12886, #2111, #471, #1744, #15790, #735, #11502, #9965, #14430, #6171, #4535, #3365, #17264, #15880, #10055, #7539, #15604, #10242, #2014, #8720, #1931, #4626, #7634, #15700, #13064, #4800, #647, #15980, #10512, #11874, #2379, #3903, #9164, #17550, #10763, #3642, #916, #16157, #1010, #5243, #9079, #2286, #17452, #13517, #14621, #3721 ) ),
 .UNSPECIFIED., .F., .F., .F. ) 
 B_SPLINE_SURFACE_WITH_KNOTS ( ( 2, 2 ),
 ( 3, 2, 2, 2, 2, 2, 2, 2, 2, 2, 2, 2, 2, 2, 2, 2, 2, 2, 2, 2, 2, 2, 2, 2, 2, 2, 2, 2, 2, 2, 2, 2, 2, 2, 2, 2, 2, 2, 2, 2, 2, 2, 2, 2, 2, 2, 2, 2, 2, 2, 2, 2, 2, 2, 2, 2, 2, 2, 2, 2, 2, 2, 2, 2, 2, 2, 2, 2, 2, 2, 2, 2, 2, 2, 2, 2, 2, 3 ),
 ( 0.000000000000000000, 1.000000000000000000 ),
 ( 0.000000000000000000, 0.01282051282051282007, 0.02564102564102564014, 0.03846153846153846367, 0.05128205128205128027, 0.06410256410256409687, 0.07692307692307692735, 0.08974358974358974395, 0.1025641025641025605, 0.1153846153846153910, 0.1282051282051281937, 0.1410256410256410242, 0.1538461538461538547, 0.1666666666666666574, 0.1794871794871794879, 0.1923076923076923184, 0.2051282051282051211, 0.2179487179487179516, 0.2307692307692307820, 0.2435897435897435848, 0.2564102564102563875, 0.2692307692307692180, 0.2820512820512820484, 0.2948717948717948789, 0.3076923076923077094, 0.3205128205128205399, 0.3333333333333333148, 0.3461538461538461453, 0.3589743589743589758, 0.3717948717948718063, 0.3846153846153846367, 0.3974358974358974117, 0.4102564102564102422, 0.4230769230769230727, 0.4358974358974359031, 0.4487179487179487336, 0.4615384615384615641, 0.4743589743589743390, 0.4871794871794871695, 0.5000000000000000000, 0.5128205128205127750, 0.5256410256410256610, 0.5384615384615384359, 0.5512820512820513219, 0.5641025641025640969, 0.5769230769230768718, 0.5897435897435897578, 0.6025641025641025328, 0.6153846153846154188, 0.6282051282051281937, 0.6410256410256410797, 0.6538461538461538547, 0.6666666666666666297, 0.6794871794871795156, 0.6923076923076922906, 0.7051282051282051766, 0.7179487179487179516, 0.7307692307692307265, 0.7435897435897436125, 0.7564102564102563875, 0.7692307692307692735, 0.7820512820512820484, 0.7948717948717948234, 0.8076923076923077094, 0.8205128205128204844, 0.8333333333333333703, 0.8461538461538461453, 0.8589743589743589203, 0.8717948717948718063, 0.8846153846153845812, 0.8974358974358974672, 0.9102564102564102422, 0.9230769230769231282, 0.9358974358974359031, 0.9487179487179486781, 0.9615384615384615641, 0.9690837477411259338, 0.9787745852185372186 ),
 .UNSPECIFIED. ) 
 GEOMETRIC_REPRESENTATION_ITEM ( )  RATIONAL_B_SPLINE_SURFACE ( (
 ( 1.000000000000000000, 0.8660254037844387076, 1.000000000000000000, 0.8660254037844387076, 1.000000000000000000, 0.8660254037844387076, 1.000000000000000000, 0.8660254037844387076, 1.000000000000000000, 0.8660254037844387076, 1.000000000000000000, 0.8660254037844387076, 1.000000000000000000, 0.8660254037844387076, 1.000000000000000000, 0.8660254037844387076, 1.000000000000000000, 0.8660254037844387076, 1.000000000000000000, 0.8660254037844387076, 1.000000000000000000, 0.8660254037844387076, 1.000000000000000000, 0.8660254037844387076, 1.000000000000000000, 0.8660254037844387076, 1.000000000000000000, 0.8660254037844387076, 1.000000000000000000, 0.8660254037844387076, 1.000000000000000000, 0.8660254037844387076, 1.000000000000000000, 0.8660254037844387076, 1.000000000000000000, 0.8660254037844387076, 1.000000000000000000, 0.8660254037844387076, 1.000000000000000000, 0.8660254037844387076, 1.000000000000000000, 0.8660254037844387076, 1.000000000000000000, 0.8660254037844387076, 1.000000000000000000, 0.8660254037844387076, 1.000000000000000000, 0.8660254037844387076, 1.000000000000000000, 0.8660254037844387076, 1.000000000000000000, 0.8660254037844387076, 1.000000000000000000, 0.8660254037844387076, 1.000000000000000000, 0.8660254037844387076, 1.000000000000000000, 0.8660254037844387076, 1.000000000000000000, 0.8660254037844387076, 1.000000000000000000, 0.8660254037844387076, 1.000000000000000000, 0.8660254037844387076, 1.000000000000000000, 0.8660254037844387076, 1.000000000000000000, 0.8660254037844387076, 1.000000000000000000, 0.8660254037844387076, 1.000000000000000000, 0.8660254037844387076, 1.000000000000000000, 0.8660254037844387076, 1.000000000000000000, 0.8660254037844387076, 1.000000000000000000, 0.8660254037844387076, 1.000000000000000000, 0.8660254037844387076, 1.000000000000000000, 0.8660254037844387076, 1.000000000000000000, 0.8660254037844387076, 1.000000000000000000, 0.8660254037844387076, 1.000000000000000000, 0.8660254037844387076, 1.000000000000000000, 0.8660254037844387076, 1.000000000000000000, 0.8660254037844387076, 1.000000000000000000, 0.8660254037844387076, 1.000000000000000000, 0.8660254037844387076, 1.000000000000000000, 0.8660254037844387076, 1.000000000000000000, 0.8660254037844387076, 1.000000000000000000, 0.8660254037844387076, 1.000000000000000000, 0.8660254037844387076, 1.000000000000000000, 0.8660254037844387076, 1.000000000000000000, 0.8660254037844387076, 1.000000000000000000, 0.8660254037844387076, 1.000000000000000000, 0.8660254037844387076, 1.000000000000000000, 0.8660254037844387076, 1.000000000000000000, 0.8660254037844387076, 1.000000000000000000, 0.8660254037844387076, 1.000000000000000000, 0.8660254037844387076, 1.000000000000000000, 0.8660254037844387076, 1.000000000000000000, 0.8660254037844387076, 1.000000000000000000, 0.8660254037844387076, 1.000000000000000000, 0.8660254037844387076, 1.000000000000000000, 0.8660254037844387076, 1.000000000000000000, 0.8660254037844387076, 1.000000000000000000, 0.8660254037844387076, 1.000000000000000000, 0.8660254037844387076, 1.000000000000000000, 0.8660254037844387076, 1.000000000000000000, 0.8660254037844387076, 1.000000000000000000, 0.8660254037844387076, 1.000000000000000000, 0.8660254037844387076, 1.000000000000000000, 0.8660254037844387076, 1.000000000000000000, 0.8660254037844387076, 1.000000000000000000, 0.8660254037844387076, 1.000000000000000000, 0.9211516195580409239, 0.9351128802560608744, 0.9351128802560608744, 0.9351128802560608744),
 ( 1.000000000000000000, 0.8660254037844387076, 1.000000000000000000, 0.8660254037844387076, 1.000000000000000000, 0.8660254037844387076, 1.000000000000000000, 0.8660254037844387076, 1.000000000000000000, 0.8660254037844387076, 1.000000000000000000, 0.8660254037844387076, 1.000000000000000000, 0.8660254037844387076, 1.000000000000000000, 0.8660254037844387076, 1.000000000000000000, 0.8660254037844387076, 1.000000000000000000, 0.8660254037844387076, 1.000000000000000000, 0.8660254037844387076, 1.000000000000000000, 0.8660254037844387076, 1.000000000000000000, 0.8660254037844387076, 1.000000000000000000, 0.8660254037844387076, 1.000000000000000000, 0.8660254037844387076, 1.000000000000000000, 0.8660254037844387076, 1.000000000000000000, 0.8660254037844387076, 1.000000000000000000, 0.8660254037844387076, 1.000000000000000000, 0.8660254037844387076, 1.000000000000000000, 0.8660254037844387076, 1.000000000000000000, 0.8660254037844387076, 1.000000000000000000, 0.8660254037844387076, 1.000000000000000000, 0.8660254037844387076, 1.000000000000000000, 0.8660254037844387076, 1.000000000000000000, 0.8660254037844387076, 1.000000000000000000, 0.8660254037844387076, 1.000000000000000000, 0.8660254037844387076, 1.000000000000000000, 0.8660254037844387076, 1.000000000000000000, 0.8660254037844387076, 1.000000000000000000, 0.8660254037844387076, 1.000000000000000000, 0.8660254037844387076, 1.000000000000000000, 0.8660254037844387076, 1.000000000000000000, 0.8660254037844387076, 1.000000000000000000, 0.8660254037844387076, 1.000000000000000000, 0.8660254037844387076, 1.000000000000000000, 0.8660254037844387076, 1.000000000000000000, 0.8660254037844387076, 1.000000000000000000, 0.8660254037844387076, 1.000000000000000000, 0.8660254037844387076, 1.000000000000000000, 0.8660254037844387076, 1.000000000000000000, 0.8660254037844387076, 1.000000000000000000, 0.8660254037844387076, 1.000000000000000000, 0.8660254037844387076, 1.000000000000000000, 0.8660254037844387076, 1.000000000000000000, 0.8660254037844387076, 1.000000000000000000, 0.8660254037844387076, 1.000000000000000000, 0.8660254037844387076, 1.000000000000000000, 0.8660254037844387076, 1.000000000000000000, 0.8660254037844387076, 1.000000000000000000, 0.8660254037844387076, 1.000000000000000000, 0.8660254037844387076, 1.000000000000000000, 0.8660254037844387076, 1.000000000000000000, 0.8660254037844387076, 1.000000000000000000, 0.8660254037844387076, 1.000000000000000000, 0.8660254037844387076, 1.000000000000000000, 0.8660254037844387076, 1.000000000000000000, 0.8660254037844387076, 1.000000000000000000, 0.8660254037844387076, 1.000000000000000000, 0.8660254037844387076, 1.000000000000000000, 0.8660254037844387076, 1.000000000000000000, 0.8660254037844387076, 1.000000000000000000, 0.8660254037844387076, 1.000000000000000000, 0.8660254037844387076, 1.000000000000000000, 0.8660254037844387076, 1.000000000000000000, 0.8660254037844387076, 1.000000000000000000, 0.8660254037844387076, 1.000000000000000000, 0.8660254037844387076, 1.000000000000000000, 0.8660254037844387076, 1.000000000000000000, 0.8660254037844387076, 1.000000000000000000, 0.8660254037844387076, 1.000000000000000000, 0.8660254037844387076, 1.000000000000000000, 0.8660254037844387076, 1.000000000000000000, 0.8660254037844387076, 1.000000000000000000, 0.8660254037844387076, 1.000000000000000000, 0.8660254037844387076, 1.000000000000000000, 0.9211516195580409239, 0.9351128802560608744, 0.9351128802560608744, 0.9351128802560608744) ) ) 
 REPRESENTATION_ITEM ( '' )  SURFACE ( )  );
#299=ADVANCED_FACE ( 'NONE', ( #4183 ), #15505, .F. ) ;
#303=CARTESIAN_POINT ( 'NONE',  ( 30.08145424927873535, -6.930706697444451336, 5.783357778048664244 ) ) ;
#304=DIRECTION ( 'NONE',  ( 1.000000000000000000, 0.000000000000000000, 0.000000000000000000 ) ) ;
#306=DIRECTION ( 'NONE',  ( 0.6000000000000000888, 0.7999999999999999334, 0.000000000000000000 ) ) ;
#309=CARTESIAN_POINT ( 'NONE',  ( 33.14902674121363901, -1.535163666906202318, 5.783357778048668685 ) ) ;
#310=AXIS2_PLACEMENT_3D ( 'NONE', #17045, #11193, #5866 ) ;
#311=B_SPLINE_CURVE_WITH_KNOTS ( 'NONE', 3,
 ( #3913, #14963, #2548, #9253, #15054, #13611, #2295, #12250, #7815, #6459, #11975, #3828, #10680, #14798, #10859, #16254 ),
 .UNSPECIFIED., .F., .F.,
 ( 4, 2, 2, 2, 2, 2, 2, 4 ),
 ( 0.000000000000000000, 0.0008414457502979328513, 0.001262168625446899277, 0.001682891500595865703, 0.002103614375744832128, 0.002524337250893798554, 0.002945060126042764979, 0.003365783001191731405 ),
 .UNSPECIFIED. ) ;
#314=CARTESIAN_POINT ( 'NONE',  ( 27.45766530510195835, -4.728742455708699666, 7.939653947423662039 ) ) ;
#315=CARTESIAN_POINT ( 'NONE',  ( -25.01192583800304448, -22.13892749297381002, 14.47384481777684151 ) ) ;
#321=ORIENTED_EDGE ( 'NONE', *, *, #9994, .T. ) ;
#322=ORIENTED_EDGE ( 'NONE', *, *, #10221, .F. ) ;
#324=CIRCLE ( 'NONE', #13067, 2.000000000000001776 ) ;
#334=DIRECTION ( 'NONE',  ( 0.9928203230275510771, 0.1196152422706614205, 0.000000000000000000 ) ) ;
#335=EDGE_CURVE ( 'NONE', #2070, #225, #4373, .T. ) ;
#336=CARTESIAN_POINT ( 'NONE',  ( 32.07220196432897552, -5.426722983814484813, 7.939653947423658487 ) ) ;
#337=ORIENTED_EDGE ( 'NONE', *, *, #15957, .T. ) ;
#341=CARTESIAN_POINT ( 'NONE',  ( 27.61527553138257574, -4.709753535998224550, 3.627061608673664228 ) ) ;
#342=CARTESIAN_POINT ( 'NONE',  ( -45.00000000000000711, -19.03270077640483038, 5.537981825772250843 ) ) ;
#344=ORIENTED_EDGE ( 'NONE', *, *, #4632, .T. ) ;
#346=ORIENTED_EDGE ( 'NONE', *, *, #15420, .F. ) ;
#351=ORIENTED_EDGE ( 'NONE', *, *, #12885, .F. ) ;
#355=CARTESIAN_POINT ( 'NONE',  ( -20.00000000000000000, 7.999999999999996447, 12.00000000000000000 ) ) ;
#358=CYLINDRICAL_SURFACE ( 'NONE', #310, 5.000000000000000000 ) ;
#361=ORIENTED_EDGE ( 'NONE', *, *, #14655, .T. ) ;
#362=ORIENTED_EDGE ( 'NONE', *, *, #13450, .F. ) ;
#366=CARTESIAN_POINT ( 'NONE',  ( 29.99682221560115991, -1.914942061115552541, 5.783357778048668685 ) ) ;
#367=AXIS2_PLACEMENT_3D ( 'NONE', #11007, #6593, #15201 ) ;
#370=DIRECTION ( 'NONE',  ( -0.7999999999999999334, -0.6000000000000001998, 0.000000000000000000 ) ) ;
#374=DIRECTION ( 'NONE',  ( 0.9928203230275512992, 0.1196152422706610180, 4.006172263299093133E-17 ) ) ;
#375=CIRCLE ( 'NONE', #6145, 13.00000000000000178 ) ;
#377=DIRECTION ( 'NONE',  ( -0.6174492339697512655, -0.7866107318554506067, 0.000000000000000000 ) ) ;
#378=EDGE_CURVE ( 'NONE', #2087, #11687, #3800, .T. ) ;
#381=CARTESIAN_POINT ( 'NONE',  ( -2.016448651773435938E-27, -20.49999999999999645, 13.00000000000000178 ) ) ;
#384=CARTESIAN_POINT ( 'NONE',  ( 28.05993251931039012, -3.202367565343740452, 8.283357778048666020 ) ) ;
#385=CARTESIAN_POINT ( 'NONE',  ( 29.81239362717914787, -2.264323817775507397, 7.033357778048666020 ) ) ;
#387=ORIENTED_EDGE ( 'NONE', *, *, #378, .F. ) ;
#390=DIRECTION ( 'NONE',  ( 0.9928203230275510771, 0.1196152422706609902, 4.006172263299092517E-17 ) ) ;
#406=CARTESIAN_POINT ( 'NONE',  ( 25.52694003402523748, -4.961356722058193114, 3.283357778048664244 ) ) ;
#407=( BOUNDED_CURVE ( )  B_SPLINE_CURVE ( 3, ( #13282, #6744, #6491, #3856 ),
 .UNSPECIFIED., .F., .T. ) 
 B_SPLINE_CURVE_WITH_KNOTS ( ( 4, 4 ),
 ( 1.825438360997748255, 1.919862177193756514 ),
 .UNSPECIFIED. ) 
 CURVE ( )  GEOMETRIC_REPRESENTATION_ITEM ( )  RATIONAL_B_SPLINE_CURVE ( ( 1.000000000000000000, 0.9992571499088201969, 0.9992571499088201969, 1.000000000000000000 ) ) 
 REPRESENTATION_ITEM ( '' )  );
#410=CARTESIAN_POINT ( 'NONE',  ( -16.75000000000000000, -16.21813761408365195, 16.03574476417183448 ) ) ;
#412=EDGE_LOOP ( 'NONE', ( #5824, #3661, #12344, #1418, #13778, #8078, #11628, #2736, #4071, #7877, #15831 ) ) ;
#413=CARTESIAN_POINT ( 'NONE',  ( 26.18940075748478691, -6.337263906362392341, 3.743184633113769699 ) ) ;
#422=CARTESIAN_POINT ( 'NONE',  ( -9.099998387031003944, -19.29508120620799616, 12.00000000000000000 ) ) ;
#423=CARTESIAN_POINT ( 'NONE',  ( 33.81344892038539740, -6.481075040654873831, 5.113484796970855228 ) ) ;
#426=CARTESIAN_POINT ( 'NONE',  ( 8.632250723006720250, -18.84644399697197770, 16.84735068286506987 ) ) ;
#428=CARTESIAN_POINT ( 'NONE',  ( 30.19827253897071273, -3.144612341114420673, 3.627061608673666893 ) ) ;
#429=ORIENTED_EDGE ( 'NONE', *, *, #16185, .F. ) ;
#431=EDGE_CURVE ( 'NONE', #3807, #1473, #11303, .T. ) ;
#432=( BOUNDED_CURVE ( )  B_SPLINE_CURVE ( 2, ( #7895, #3983, #3719, #2460, #1275, #16246, #6699, #3817, #13689 ),
 .UNSPECIFIED., .F., .T. ) 
 B_SPLINE_CURVE_WITH_KNOTS ( ( 3, 2, 2, 2, 3 ),
 ( 0.2115384615384615641, 0.2179487179487179516, 0.2307692307692307820, 0.2435897435897435848, 0.2500000000000000000 ),
 .UNSPECIFIED. ) 
 CURVE ( )  GEOMETRIC_REPRESENTATION_ITEM ( )  RATIONAL_B_SPLINE_CURVE ( ( 0.9330127018922194093, 0.9330127018922196314, 1.000000000000000000, 0.8660254037844387076, 1.000000000000000000, 0.8660254037844387076, 1.000000000000000000, 0.9330127018922191873, 0.9330127018922194093 ) ) 
 REPRESENTATION_ITEM ( '' )  );
#434=CARTESIAN_POINT ( 'NONE',  ( 28.36401332423200827, -6.500457016816879374, 4.705209693361160461 ) ) ;
#437=ORIENTED_EDGE ( 'NONE', *, *, #17620, .F. ) ;
#440=FACE_OUTER_BOUND ( 'NONE', #9087, .T. ) ;
#446=CARTESIAN_POINT ( 'NONE',  ( -8.632250723006720250, -18.84644399697197770, 13.00000000000000178 ) ) ;
#449=EDGE_LOOP ( 'NONE', ( #10237, #6974, #15692, #17847 ) ) ;
#451=CARTESIAN_POINT ( 'NONE',  ( 30.48043329534786849, -5.818372192732907067, 8.283357778048658915 ) ) ;
#455=CARTESIAN_POINT ( 'NONE',  ( 30.13703915187255689, -4.405930820630744371, 3.627061608673664228 ) ) ;
#457=CARTESIAN_POINT ( 'NONE',  ( 0.000000000000000000, 0.000000000000000000, 8.700000000000001066 ) ) ;
#459=CARTESIAN_POINT ( 'NONE',  ( -15.92260893619738837, -28.39189527176317540, 16.15082599432113142 ) ) ;
#461=LINE ( 'NONE', #1551, #9865 ) ;
#462=LINE ( 'NONE', #8801, #7562 ) ;
#471=CARTESIAN_POINT ( 'NONE',  ( 27.78220930431293922, -1.782014143258494832, 5.783357778048668685 ) ) ;
#477=DIRECTION ( 'NONE',  ( -0.000000000000000000, -0.000000000000000000, 1.000000000000000000 ) ) ;
#482=ORIENTED_EDGE ( 'NONE', *, *, #16676, .F. ) ;
#485=CARTESIAN_POINT ( 'NONE',  ( 27.21934464581372737, -3.303641803799556964, 3.283357778048666464 ) ) ;
#488=CARTESIAN_POINT ( 'NONE',  ( 26.34507017448785504, -7.770415366711231009, 5.783357778048657138 ) ) ;
#490=DIRECTION ( 'NONE',  ( 0.9928203230275512992, 0.1196152422706614482, 0.000000000000000000 ) ) ;
#493=ORIENTED_EDGE ( 'NONE', *, *, #7842, .T. ) ;
#494=DIRECTION ( 'NONE',  ( 0.9928203230275510771, 0.1196152422706609902, 4.006172263299092517E-17 ) ) ;
#499=CYLINDRICAL_SURFACE ( 'NONE', #17938, 2.500000000000001776 ) ;
#502=CYLINDRICAL_SURFACE ( 'NONE', #6351, 5.500000000000000888 ) ;
#506=CARTESIAN_POINT ( 'NONE',  ( 30.41294626588012306, -6.253601060580800564, 4.705209693361159573 ) ) ;
#513=CARTESIAN_POINT ( 'NONE',  ( 33.43363050022580296, -2.127845067243429256, 6.861505862736166250 ) ) ;
#523=VECTOR ( 'NONE', #4783, 1000.000000000000227 ) ;
#528=EDGE_CURVE ( 'NONE', #12891, #17459, #462, .T. ) ;
#530=CARTESIAN_POINT ( 'NONE',  ( 32.55182397003001427, -2.661183353387966299, 8.283357778048664244 ) ) ;
#532=EDGE_CURVE ( 'NONE', #5221, #4376, #13144, .T. ) ;
#533=CIRCLE ( 'NONE', #11801, 5.000000000000000000 ) ;
#534=ORIENTED_EDGE ( 'NONE', *, *, #3431, .T. ) ;
#535=CARTESIAN_POINT ( 'NONE',  ( 33.40301380667672504, -2.758504307001591549, 7.939653947423664704 ) ) ;
#537=CARTESIAN_POINT ( 'NONE',  ( 33.43363050022580296, -2.127845067243429256, 6.861505862736166250 ) ) ;
#539=CARTESIAN_POINT ( 'NONE',  ( -45.50000000000000000, -16.03270077640482683, 5.537981825772250843 ) ) ;
#543=DIRECTION ( 'NONE',  ( -0.000000000000000000, -0.000000000000000000, 1.000000000000000000 ) ) ;
#545=LINE ( 'NONE', #13055, #3288 ) ;
#547=AXIS2_PLACEMENT_3D ( 'NONE', #3870, #17861, #15190 ) ;
#549=EDGE_CURVE ( 'NONE', #13209, #1004, #4526, .T. ) ;
#556=CARTESIAN_POINT ( 'NONE',  ( 29.67353201968042598, -1.554147106732884920, 5.783357778048668685 ) ) ;
#560=ORIENTED_EDGE ( 'NONE', *, *, #7764, .T. ) ;
#563=CARTESIAN_POINT ( 'NONE',  ( 3.248936832696173393, 17.78798921770683350, 17.00000000000000000 ) ) ;
#569=ADVANCED_FACE ( 'NONE', ( #15869 ), #11769, .T. ) ;
#577=CARTESIAN_POINT ( 'NONE',  ( 26.69778786461289855, -6.274106265784127778, 8.283357778048658915 ) ) ;
#585=AXIS2_PLACEMENT_3D ( 'NONE', #12458, #11078, #6662 ) ;
#592=EDGE_CURVE ( 'NONE', #15079, #14461, #13323, .T. ) ;
#593=CARTESIAN_POINT ( 'NONE',  ( 25.71748644841968456, -2.420320648352046078, 5.783357778048663356 ) ) ;
#596=DIRECTION ( 'NONE',  ( -0.1196152422706610735, 0.9928203230275511881, 0.000000000000000000 ) ) ;
#597=CARTESIAN_POINT ( 'NONE',  ( 33.75714020991769360, -6.487859128256952879, 6.453230759126468818 ) ) ;
#598=CARTESIAN_POINT ( 'NONE',  ( 26.39370705969127684, -2.976016814310973313, 4.705209693361168455 ) ) ;
#600=ORIENTED_EDGE ( 'NONE', *, *, #8612, .T. ) ;
#602=VERTEX_POINT ( 'NONE', #10501 ) ;
#604=CARTESIAN_POINT ( 'NONE',  ( 32.30426898124760982, -6.025734024055190652, 4.705209693361159573 ) ) ;
#605=CARTESIAN_POINT ( 'NONE',  ( -23.43428999263575818, -9.970190943884908563, 14.83168556311182940 ) ) ;
#614=DIRECTION ( 'NONE',  ( -4.179998415399335043E-17, -3.469446951953615175E-16, -1.000000000000000000 ) ) ;
#617=COLOUR_RGB ( '', 0.09019608, 0.27058824, 0.51372549) ;
#619=LINE ( 'NONE', #14124, #14477 ) ;
#623=CARTESIAN_POINT ( 'NONE',  ( 30.72436838703367812, -6.515889623968540434, 4.533357778048659803 ) ) ;
#624=EDGE_LOOP ( 'NONE', ( #16121, #9146, #14535, #15513, #4650, #17869 ) ) ;
#628=CARTESIAN_POINT ( 'NONE',  ( 32.72003615946069743, -2.840789625746940938, 3.627061608673666449 ) ) ;
#631=CARTESIAN_POINT ( 'NONE',  ( -27.17934203385504333, -30.00000000000000355, 13.93658524716016878 ) ) ;
#636=CARTESIAN_POINT ( 'NONE',  ( 11.20128062458870843, 15.41171339406673546, 16.67750984750043486 ) ) ;
#639=CARTESIAN_POINT ( 'NONE',  ( 26.01652455409633902, -4.902371455920926380, 5.783357778048663356 ) ) ;
#642=VECTOR ( 'NONE', #3914, 1000.000000000000000 ) ;
#647=CARTESIAN_POINT ( 'NONE',  ( 26.52132749406794687, -1.933925500942234921, 5.783357778048668685 ) ) ;
#649=ORIENTED_EDGE ( 'NONE', *, *, #16525, .F. ) ;
#657=LINE ( 'NONE', #7724, #6382 ) ;
#666=CARTESIAN_POINT ( 'NONE',  ( 31.49429780130001433, -5.496349022752856861, 3.627061608673662896 ) ) ;
#671=LINE ( 'NONE', #11716, #14501 ) ;
#673=ORIENTED_EDGE ( 'NONE', *, *, #12629, .T. ) ;
#677=CARTESIAN_POINT ( 'NONE',  ( -25.07353123778395343, 1.235291682954730463, 14.60266621045499669 ) ) ;
#678=CARTESIAN_POINT ( 'NONE',  ( 33.18300801526289234, -6.557030719496743210, 5.113484796970852564 ) ) ;
#679=EDGE_LOOP ( 'NONE', ( #8536, #10466 ) ) ;
#684=ORIENTED_EDGE ( 'NONE', *, *, #3431, .F. ) ;
#690=CARTESIAN_POINT ( 'NONE',  ( 27.14244485254070938, -4.766720295129625029, 3.627061608673664228 ) ) ;
#691=SHAPE_REPRESENTATION ( 'MirrorCaliper Body Half', ( #3575 ), #16530 ) ;
#695=CARTESIAN_POINT ( 'NONE',  ( 26.47269060886452507, -6.728324053342490174, 4.705209693361160461 ) ) ;
#696=CARTESIAN_POINT ( 'NONE',  ( -24.62787796620740011, -10.18046270510853368, 14.56338605435095701 ) ) ;
#701=CARTESIAN_POINT ( 'NONE',  ( 20.25000000000000711, -16.21813761408365195, 13.00000000000000178 ) ) ;
#702=DIRECTION ( 'NONE',  ( 0.1196152422706618645, -0.9928203230275510771, 0.000000000000000000 ) ) ;
#712=CARTESIAN_POINT ( 'NONE',  ( 30.38277803966508372, -1.468696967828331701, 5.783357778048668685 ) ) ;
#713=ORIENTED_EDGE ( 'NONE', *, *, #16582, .T. ) ;
#716=CARTESIAN_POINT ( 'NONE',  ( 26.66018910156667232, -2.644102211984857842, 7.033357778048666020 ) ) ;
#717=CARTESIAN_POINT ( 'NONE',  ( 32.93018312783485868, -2.815471066132993805, 7.939653947423662927 ) ) ;
#718=FILL_AREA_STYLE_COLOUR ( '', #818 ) ;
#722=CARTESIAN_POINT ( 'NONE',  ( 29.08935247050201767, -2.014077381790315702, 5.783357778048667797 ) ) ;
#725=DIRECTION ( 'NONE',  ( 0.000000000000000000, 1.000000000000000000, 0.000000000000000000 ) ) ;
#727=CARTESIAN_POINT ( 'NONE',  ( 19.91392456697921531, -10.76755109436559010, 15.52754005891982736 ) ) ;
#733=CARTESIAN_POINT ( 'NONE',  ( 25.92467471225709374, -2.732717170633701453, 4.533357778048667797 ) ) ;
#735=CARTESIAN_POINT ( 'NONE',  ( 27.96989853965305528, -4.667028466753395222, 3.283357778048664244 ) ) ;
#737=CARTESIAN_POINT ( 'NONE',  ( 26.31128205117621022, -7.047579375861630524, 4.533357778048659803 ) ) ;
#738=EDGE_CURVE ( 'NONE', #16186, #6854, #2363, .T. ) ;
#743=DIRECTION ( 'NONE',  ( 0.000000000000000000, 0.000000000000000000, -1.000000000000000000 ) ) ;
#746=ORIENTED_EDGE ( 'NONE', *, *, #9165, .F. ) ;
#750=DIRECTION ( 'NONE',  ( -0.000000000000000000, -0.000000000000000000, 1.000000000000000000 ) ) ;
#755=ADVANCED_BREP_SHAPE_REPRESENTATION ( '', ( #5266, #3575 ), #16530 ) ;
#763=FACE_BOUND ( 'NONE', #1135, .T. ) ;
#766=CARTESIAN_POINT ( 'NONE',  ( 29.94002636988270538, -4.429666970165102136, 3.283357778048664244 ) ) ;
#772=ADVANCED_FACE ( 'NONE', ( #7001 ), #5619, .F. ) ;
#773=DIRECTION ( 'NONE',  ( 0.9928203230275510771, 0.1196152422706609902, 4.006172263299092517E-17 ) ) ;
#775=CARTESIAN_POINT ( 'NONE',  ( 26.05393439953038381, -7.587479618990243146, 5.036916015667400437 ) ) ;
#777=CARTESIAN_POINT ( 'NONE',  ( 26.28374211850154296, -7.120308096563227274, 6.686083953656291712 ) ) ;
#779=CARTESIAN_POINT ( 'NONE',  ( 33.56062403295735663, -2.739515387291124426, 7.939653947423664704 ) ) ;
#780=CARTESIAN_POINT ( 'NONE',  ( -20.27735869291019810, -10.58859781672278899, 15.46157951461808189 ) ) ;
#784=CARTESIAN_POINT ( 'NONE',  ( 30.66124439477291475, -6.860853434864224276, 5.113484796970852564 ) ) ;
#786=DIRECTION ( 'NONE',  ( 0.000000000000000000, -0.000000000000000000, 1.000000000000000000 ) ) ;
#790=CARTESIAN_POINT ( 'NONE',  ( 31.04700706809921940, -2.115577279836057922, 4.533357778048667797 ) ) ;
#796=CARTESIAN_POINT ( 'NONE',  ( 31.98525019727866692, -6.363978266284800789, 4.533357778048659803 ) ) ;
#797=ORIENTED_EDGE ( 'NONE', *, *, #6971, .F. ) ;
#800=CARTESIAN_POINT ( 'NONE',  ( 26.35439372113758694, -4.861664893681965083, 3.627061608673664228 ) ) ;
#801=CARTESIAN_POINT ( 'NONE',  ( 32.06767520579373354, -2.292415704734142690, 4.705209693361168455 ) ) ;
#803=CARTESIAN_POINT ( 'NONE',  ( 32.47301885516785092, -2.670677813450649918, 8.283357778048666020 ) ) ;
#807=DIRECTION ( 'NONE',  ( 0.000000000000000000, 0.000000000000000000, 1.000000000000000000 ) ) ;
#812=ORIENTED_EDGE ( 'NONE', *, *, #12281, .T. ) ;
#818=COLOUR_RGB ( '', 0.09019608, 0.27058824, 0.51372549) ;
#822=CARTESIAN_POINT ( 'NONE',  ( 26.31065902414478686, -7.328232685206446106, 5.254681170202263552 ) ) ;
#825=VERTEX_POINT ( 'NONE', #13523 ) ;
#827=CARTESIAN_POINT ( 'NONE',  ( 7.499998387031003411, -20.49508120620799900, 13.00000000000000178 ) ) ;
#832=DIRECTION ( 'NONE',  ( 1.000000000000000000, 0.000000000000000000, 0.000000000000000000 ) ) ;
#837=EDGE_CURVE ( 'NONE', #7608, #1468, #5335, .T. ) ;
#843=DIRECTION ( 'NONE',  ( -1.000000000000000000, 0.000000000000000000, 0.000000000000000000 ) ) ;
#845=CARTESIAN_POINT ( 'NONE',  ( -2.016448651773435938E-27, -20.49999999999999645, 13.00000000000000178 ) ) ;
#850=ADVANCED_FACE ( 'NONE', ( #2547 ), #1096, .T. ) ;
#861=LINE ( 'NONE', #7487, #4406 ) ;
#863=CARTESIAN_POINT ( 'NONE',  ( 27.65458886993626564, -2.824105456627233224, 4.705209693361168455 ) ) ;
#869=CARTESIAN_POINT ( 'NONE',  ( 33.44685390376565692, -4.007163506710925027, 3.627061608673664228 ) ) ;
#870=CARTESIAN_POINT ( 'NONE',  ( -26.11885528537984413, -10.78654967147420329, 14.20677827292374040 ) ) ;
#879=EDGE_LOOP ( 'NONE', ( #7853, #3390, #4842, #9756 ) ) ;
#881=CARTESIAN_POINT ( 'NONE',  ( 31.20090818012769773, -4.277755612481361602, 3.283357778048664244 ) ) ;
#883=EDGE_CURVE ( 'NONE', #15791, #4053, #3323, .T. ) ;
#888=CARTESIAN_POINT ( 'NONE',  ( 30.12771560522282499, -7.314681293660012074, 5.783357778048657138 ) ) ;
#891=CIRCLE ( 'NONE', #10711, 2.749999999999988454 ) ;
#892=EDGE_LOOP ( 'NONE', ( #16804, #362, #17173, #5580, #7051, #16763, #4405, #6326, #15115, #12241, #12488, #3250, #12215, #13332, #13318, #14853, #7542, #437, #17367, #11537, #17704, #12031, #11724, #1885, #14496, #10853, #684, #7322, #1022 ) ) ;
#894=LINE ( 'NONE', #10494, #523 ) ;
#895=CARTESIAN_POINT ( 'NONE',  ( 33.46007730730551799, -5.886481946178435010, 6.861505862736157368 ) ) ;
#897=( LENGTH_UNIT ( ) NAMED_UNIT ( * ) SI_UNIT ( .MILLI., .METRE. ) );
#903=CARTESIAN_POINT ( 'NONE',  ( 0.000000000000000000, 0.000000000000000000, 10.50000000000000000 ) ) ;
#904=CARTESIAN_POINT ( 'NONE',  ( 20.00000000000000355, 7.999999999999996447, 6.000000000000000000 ) ) ;
#906=VECTOR ( 'NONE', #7722, 1000.000000000000000 ) ;
#909=VECTOR ( 'NONE', #7982, 1000.000000000000227 ) ;
#916=CARTESIAN_POINT ( 'NONE',  ( 26.16860980394290692, -3.430234601869349920, 8.283357778048664244 ) ) ;
#924=CARTESIAN_POINT ( 'NONE',  ( -35.77680296528374271, -19.03270077640483038, 0.5379818257722508434 ) ) ;
#928=EDGE_LOOP ( 'NONE', ( #13170, #2992, #5507, #9711 ) ) ;
#939=AXIS2_PLACEMENT_3D ( 'NONE', #15744, #17213, #596 ) ;
#942=CARTESIAN_POINT ( 'NONE',  ( -35.41536221060850664, -16.03270077640482683, 10.53798182577225084 ) ) ;
#945=CARTESIAN_POINT ( 'NONE',  ( 26.01345249736710841, -4.876873030332669501, 3.385440998859989836 ) ) ;
#954=DIRECTION ( 'NONE',  ( 0.000000000000000000, 0.000000000000000000, -1.000000000000000000 ) ) ;
#955=CARTESIAN_POINT ( 'NONE',  ( -7.499998387031003411, -20.49508120620799900, 12.00000000000000000 ) ) ;
#959=CARTESIAN_POINT ( 'NONE',  ( 27.15566825608056689, -6.646038734597135011, 6.861505862736157368 ) ) ;
#960=ORIENTED_EDGE ( 'NONE', *, *, #7086, .F. ) ;
#961=EDGE_CURVE ( 'NONE', #5034, #5157, #461, .T. ) ;
#965=CARTESIAN_POINT ( 'NONE',  ( 31.65190802758064592, -5.477360103042387074, 3.627061608673662896 ) ) ;
#966=CARTESIAN_POINT ( 'NONE',  ( 27.36943512155133362, -2.558652073080304845, 7.033357778048666020 ) ) ;
#973=VECTOR ( 'NONE', #7890, 1000.000000000000000 ) ;
#982=CARTESIAN_POINT ( 'NONE',  ( 5.500000000000000000, -20.49999999999999645, 6.000000000000000000 ) ) ;
#984=CARTESIAN_POINT ( 'NONE',  ( 28.16881664323205570, -6.096876348486420127, 3.283357778048663800 ) ) ;
#990=CARTESIAN_POINT ( 'NONE',  ( 33.38562051666750818, -5.268481986227246061, 3.627061608673662896 ) ) ;
#991=CARTESIAN_POINT ( 'NONE',  ( 31.65190802758064592, -5.477360103042387074, 3.627061608673662896 ) ) ;
#996=CARTESIAN_POINT ( 'NONE',  ( 32.92339180097568629, -5.524043937428110063, 8.283357778048660691 ) ) ;
#999=CARTESIAN_POINT ( 'NONE',  ( 33.60446413004628141, -3.988174587000466342, 7.939653947423662039 ) ) ;
#1003=CARTESIAN_POINT ( 'NONE',  ( 18.32916366311290091, -12.06017896066153128, 15.79554754021495633 ) ) ;
#1004=VERTEX_POINT ( 'NONE', #12876 ) ;
#1007=ORIENTED_EDGE ( 'NONE', *, *, #1104, .F. ) ;
#1008=CARTESIAN_POINT ( 'NONE',  ( -30.07408527595751124, -27.82894256842315883, 13.18310524188696853 ) ) ;
#1010=CARTESIAN_POINT ( 'NONE',  ( 25.89088658894545603, -2.009881179784104965, 5.783357778048668685 ) ) ;
#1012=VERTEX_POINT ( 'NONE', #15590 ) ;
#1013=CARTESIAN_POINT ( 'NONE',  ( 30.75425665345519732, -2.450656702321377001, 6.861505862736165362 ) ) ;
#1017=CARTESIAN_POINT ( 'NONE',  ( -13.00000000000000178, -1.592040838891559293E-15, 6.000000000000000000 ) ) ;
#1022=ORIENTED_EDGE ( 'NONE', *, *, #17303, .T. ) ;
#1035=CARTESIAN_POINT ( 'NONE',  ( 25.79194807336802597, -3.038360733637183397, 4.591826007371929919 ) ) ;
#1036=CARTESIAN_POINT ( 'NONE',  ( 13.65694651542703397, -25.37101204406936361, 16.45580752066269881 ) ) ;
#1042=CARTESIAN_POINT ( 'NONE',  ( -35.74085044863416272, -18.73429073671335132, 11.27079897466147607 ) ) ;
#1045=LINE ( 'NONE', #10800, #205 ) ;
#1046=CARTESIAN_POINT ( 'NONE',  ( 32.53688598753899441, -6.297517047505613697, 4.533357778048659803 ) ) ;
#1047=ORIENTED_EDGE ( 'NONE', *, *, #5609, .T. ) ;
#1050=CARTESIAN_POINT ( 'NONE',  ( 29.56783163384821833, -3.220568019956291383, 3.627061608673666893 ) ) ;
#1051=DIRECTION ( 'NONE',  ( 0.000000000000000000, 0.000000000000000000, -1.000000000000000000 ) ) ;
#1052=CARTESIAN_POINT ( 'NONE',  ( 24.43282520912215006, -22.30499949230690504, 14.60822674442184699 ) ) ;
#1055=FACE_OUTER_BOUND ( 'NONE', #13406, .T. ) ;
#1059=CYLINDRICAL_SURFACE ( 'NONE', #5164, 5.500000000000000888 ) ;
#1061=CARTESIAN_POINT ( 'NONE',  ( 26.97161122272022382, -2.906390775372597712, 6.861505862736165362 ) ) ;
#1066=CARTESIAN_POINT ( 'NONE',  ( 29.46348657678868577, -6.667800981652280967, 4.533357778048659803 ) ) ;
#1070=CARTESIAN_POINT ( 'NONE',  ( 32.14665875496697822, -6.044722943765660439, 4.705209693361160461 ) ) ;
#1072=CARTESIAN_POINT ( 'NONE',  ( 30.39102621733566423, -5.629271460726127607, 3.627061608673662896 ) ) ;
#1074=FACE_OUTER_BOUND ( 'NONE', #8041, .T. ) ;
#1080=CARTESIAN_POINT ( 'NONE',  ( 31.71123609653335507, -2.762457591843783256, 3.283357778048666464 ) ) ;
#1093=CARTESIAN_POINT ( 'NONE',  ( 31.30154412293507349, -3.011689903141150815, 3.627061608673666449 ) ) ;
#1095=CARTESIAN_POINT ( 'NONE',  ( 28.04870365451522218, -4.657534006690712935, 3.283357778048664244 ) ) ;
#1096=PLANE ( 'NONE',  #10161 ) ;
#1097=DIRECTION ( 'NONE',  ( 1.000000000000000000, 0.000000000000000000, 0.000000000000000000 ) ) ;
#1098=EDGE_CURVE ( 'NONE', #15002, #2720, #10409, .T. ) ;
#1102=ORIENTED_EDGE ( 'NONE', *, *, #11417, .F. ) ;
#1104=EDGE_CURVE ( 'NONE', #17832, #13470, #5059, .T. ) ;
#1116=CIRCLE ( 'NONE', #14443, 6.249999999999996447 ) ;
#1121=CARTESIAN_POINT ( 'NONE',  ( 25.11802603177690330, -16.03270077640482683, 0.5379818257722508434 ) ) ;
#1127=CARTESIAN_POINT ( 'NONE',  ( 31.24221605398236790, -5.726592414339752857, 3.283357778048663800 ) ) ;
#1128=EDGE_LOOP ( 'NONE', ( #16946, #361, #10128, #4367 ) ) ;
#1130=CARTESIAN_POINT ( 'NONE',  ( 29.78250536075762867, -6.329556739422670830, 4.705209693361159573 ) ) ;
#1132=CARTESIAN_POINT ( 'NONE',  ( 24.62797819841904001, -22.25577170577939157, 14.56336204217505426 ) ) ;
#1133=ORIENTED_EDGE ( 'NONE', *, *, #3776, .F. ) ;
#1135=EDGE_LOOP ( 'NONE', ( #15094, #7609 ) ) ;
#1147=CARTESIAN_POINT ( 'NONE',  ( 32.55182397003001427, -2.661183353387966299, 8.283357778048666020 ) ) ;
#1149=AXIS2_PLACEMENT_3D ( 'NONE', #5454, #8274, #1391 ) ;
#1151=CARTESIAN_POINT ( 'NONE',  ( 29.82181869931131146, -4.443908660051686610, 7.939653947423662039 ) ) ;
#1153=CARTESIAN_POINT ( 'NONE',  ( 0.000000000000000000, 0.000000000000000000, 10.50000000000000000 ) ) ;
#1154=CARTESIAN_POINT ( 'NONE',  ( 32.08959525433819238, -2.916745304588811649, 3.627061608673666893 ) ) ;
#1155=CARTESIAN_POINT ( 'NONE',  ( 27.89480254248674740, -2.495355674045408367, 4.533357778048667797 ) ) ;
#1156=VECTOR ( 'NONE', #15774, 1000.000000000000227 ) ;
#1159=EDGE_CURVE ( 'NONE', #13209, #11980, #1304, .T. ) ;
#1160=ORIENTED_EDGE ( 'NONE', *, *, #5892, .T. ) ;
#1162=CARTESIAN_POINT ( 'NONE',  ( 33.17547354829333273, -5.293800545841212291, 7.939653947423658487 ) ) ;
#1164=CARTESIAN_POINT ( 'NONE',  ( 29.67743187657054449, -6.342216019229654833, 6.861505862736157368 ) ) ;
#1165=ORIENTED_EDGE ( 'NONE', *, *, #5934, .F. ) ;
#1166=CARTESIAN_POINT ( 'NONE',  ( 29.89119874204131122, -2.254829357712824667, 7.033357778048666020 ) ) ;
#1169=CARTESIAN_POINT ( 'NONE',  ( -34.91600907648203389, -11.88801210197604341, 11.56671555609732671 ) ) ;
#1176=CARTESIAN_POINT ( 'NONE',  ( 26.04410741498555382, -2.380969272135942560, 6.453230759126468818 ) ) ;
#1183=DIRECTION ( 'NONE',  ( 0.1196152422706587976, -0.9928203230275515212, 1.866876274697368064E-15 ) ) ;
#1184=VERTEX_POINT ( 'NONE', #9571 ) ;
#1186=EDGE_CURVE ( 'NONE', #63, #14701, #1906, .T. ) ;
#1188=CARTESIAN_POINT ( 'NONE',  ( 30.65370992780335868, -5.597623261208692469, 7.939653947423658487 ) ) ;
#1193=CARTESIAN_POINT ( 'NONE',  ( 32.30788887834420819, -1.963665922152317833, 4.533357778048667797 ) ) ;
#1197=VECTOR ( 'NONE', #9155, 1000.000000000000000 ) ;
#1200=CARTESIAN_POINT ( 'NONE',  ( 28.53771668024168662, -2.080538600569502794, 5.783357778048667797 ) ) ;
#1204=CARTESIAN_POINT ( 'NONE',  ( -29.25000000000000000, -16.21813761408365195, 13.00000000000000178 ) ) ;
#1208=ADVANCED_FACE ( 'NONE', ( #1342 ), #12312, .T. ) ;
#1210=LINE ( 'NONE', #15070, #3594 ) ;
#1212=ORIENTED_EDGE ( 'NONE', *, *, #11508, .T. ) ;
#1215=CARTESIAN_POINT ( 'NONE',  ( 25.84832697747032526, -3.506312147857045147, 3.985547620975729899 ) ) ;
#1216=EDGE_CURVE ( 'NONE', #14120, #8870, #2004, .T. ) ;
#1222=PLANE ( 'NONE',  #13590 ) ;
#1229=CARTESIAN_POINT ( 'NONE',  ( 28.74176732417158320, -7.092112515190875044, 5.783357778048669573 ) ) ;
#1230=CARTESIAN_POINT ( 'NONE',  ( 31.02146712245815507, -5.553315781884258229, 3.627061608673662896 ) ) ;
#1231=CARTESIAN_POINT ( 'NONE',  ( 34.91600907648203389, -11.88801210197604341, 0.000000000000000000 ) ) ;
#1232=CARTESIAN_POINT ( 'NONE',  ( 18.90799107099199716, -20.96007437013451380, 15.70102267215298042 ) ) ;
#1236=VERTEX_POINT ( 'NONE', #10842 ) ;
#1237=DIRECTION ( 'NONE',  ( 0.000000000000000000, 0.000000000000000000, -1.000000000000000000 ) ) ;
#1246=CARTESIAN_POINT ( 'NONE',  ( 28.12741954877813555, -2.767138697495831856, 4.705209693361167567 ) ) ;
#1247=AXIS2_PLACEMENT_3D ( 'NONE', #8112, #9206, #12096 ) ;
#1250=CARTESIAN_POINT ( 'NONE',  ( 33.56515079149260572, -5.873822666371450119, 4.705209693361159573 ) ) ;
#1254=ORIENTED_EDGE ( 'NONE', *, *, #12502, .T. ) ;
#1256=CARTESIAN_POINT ( 'NONE',  ( 33.17094678975809074, -2.159493266760871499, 4.705209693361167567 ) ) ;
#1257=CIRCLE ( 'NONE', #6474, 0.9999999999999995559 ) ;
#1260=CARTESIAN_POINT ( 'NONE',  ( 29.13014440709066832, -5.781182818409868140, 3.627061608673662896 ) ) ;
#1262=DIRECTION ( 'NONE',  ( -0.1196152422706610735, 0.9928203230275511881, 0.000000000000000000 ) ) ;
#1263=CARTESIAN_POINT ( 'NONE',  ( 8.632250723006720250, -18.84644399697197770, 13.00000000000000178 ) ) ;
#1264=VECTOR ( 'NONE', #15862, 1000.000000000000000 ) ;
#1267=CARTESIAN_POINT ( 'NONE',  ( 31.97277696464621854, -6.702839660918840536, 5.783357778048664244 ) ) ;
#1270=CARTESIAN_POINT ( 'NONE',  ( 26.10855331130634127, -2.710563430764044490, 7.033357778048666020 ) ) ;
#1275=CARTESIAN_POINT ( 'NONE',  ( 31.51612863268893960, -4.239777773060436239, 8.283357778048662468 ) ) ;
#1277=ORIENTED_EDGE ( 'NONE', *, *, #12144, .F. ) ;
#1278=CARTESIAN_POINT ( 'NONE',  ( 33.28924367748503244, -4.026152426421394814, 3.627061608673664228 ) ) ;
#1291=DIRECTION ( 'NONE',  ( 0.000000000000000000, 0.000000000000000000, -1.000000000000000000 ) ) ;
#1297=DIRECTION ( 'NONE',  ( 1.000000000000000000, 0.000000000000000000, 0.000000000000000000 ) ) ;
#1302=ORIENTED_EDGE ( 'NONE', *, *, #3384, .T. ) ;
#1303=DIRECTION ( 'NONE',  ( -1.000000000000000000, 0.000000000000000000, 0.000000000000000000 ) ) ;
#1304=( BOUNDED_CURVE ( )  B_SPLINE_CURVE ( 2, ( #722, #9231, #6247, #2188, #13229, #6337, #13322, #17961, #17624 ),
 .UNSPECIFIED., .F., .T. ) 
 B_SPLINE_CURVE_WITH_KNOTS ( ( 3, 2, 2, 2, 3 ),
 ( 0.5576923076923077094, 0.5641025641025640969, 0.5769230769230768718, 0.5897435897435897578, 0.5961538461538461453 ),
 .UNSPECIFIED. ) 
 CURVE ( )  GEOMETRIC_REPRESENTATION_ITEM ( )  RATIONAL_B_SPLINE_CURVE ( ( 0.9330127018922194093, 0.9330127018922194093, 1.000000000000000000, 0.8660254037844387076, 1.000000000000000000, 0.8660254037844387076, 1.000000000000000000, 0.9330127018922194093, 0.9330127018922194093 ) ) 
 REPRESENTATION_ITEM ( '' )  );
#1311=EDGE_CURVE ( 'NONE', #15079, #1236, #3214, .T. ) ;
#1312=CARTESIAN_POINT ( 'NONE',  ( 25.96861057204955259, -6.167300557297518360, 4.026422103237231376 ) ) ;
#1313=CARTESIAN_POINT ( 'NONE',  ( -17.40654580017221065, -13.42197210625884551, 15.93919332483364748 ) ) ;
#1317=EDGE_LOOP ( 'NONE', ( #16339, #11212, #14885, #12801, #7636 ) ) ;
#1318=DIRECTION ( 'NONE',  ( 0.9396926207859104263, 0.000000000000000000, 0.3420201433256631063 ) ) ;
#1323=CARTESIAN_POINT ( 'NONE',  ( 27.96989853965305528, -4.667028466753395222, 3.283357778048664244 ) ) ;
#1325=CARTESIAN_POINT ( 'NONE',  ( 27.10313151398701947, -6.652368374500619908, 4.705209693361160461 ) ) ;
#1326=CARTESIAN_POINT ( 'NONE',  ( 27.73357241910951743, -6.576412695658750529, 4.705209693361160461 ) ) ;
#1329=CARTESIAN_POINT ( 'NONE',  ( 33.30663696749426350, -1.516174747195733863, 5.783357778048668685 ) ) ;
#1334=CARTESIAN_POINT ( 'NONE',  ( 31.51169109130924184, -2.986371343527201905, 7.939653947423664704 ) ) ;
#1335=DIRECTION ( 'NONE',  ( 0.000000000000000000, 0.000000000000000000, -1.000000000000000000 ) ) ;
#1337=CARTESIAN_POINT ( 'NONE',  ( 31.55553118839817728, -4.235030543236534939, 3.627061608673664228 ) ) ;
#1338=ORIENTED_EDGE ( 'NONE', *, *, #3322, .F. ) ;
#1342=FACE_OUTER_BOUND ( 'NONE', #12131, .T. ) ;
#1346=DIRECTION ( 'NONE',  ( -0.3420201433256631618, 0.000000000000000000, -0.9396926207859104263 ) ) ;
#1347=CARTESIAN_POINT ( 'NONE',  ( 28.59583933521957277, -13.42685997174391765, 13.55623838816837079 ) ) ;
#1352=CARTESIAN_POINT ( 'NONE',  ( 33.86058074732183343, -3.957317592522819005, 8.111505862736160921 ) ) ;
#1354=ORIENTED_EDGE ( 'NONE', *, *, #14243, .T. ) ;
#1355=ORIENTED_EDGE ( 'NONE', *, *, #14455, .F. ) ;
#1356=EDGE_CURVE ( 'NONE', #11980, #6730, #14286, .T. ) ;
#1357=CARTESIAN_POINT ( 'NONE',  ( 31.53813789838894621, -6.745008222462202774, 5.783357778048658915 ) ) ;
#1364=DIRECTION ( 'NONE',  ( 0.000000000000000000, 0.000000000000000000, 1.000000000000000000 ) ) ;
#1366=EDGE_CURVE ( 'NONE', #10101, #15480, #1791, .T. ) ;
#1369=CARTESIAN_POINT ( 'NONE',  ( -13.00000000000000178, -1.592040838891559293E-15, 10.50000000000000000 ) ) ;
#1373=CARTESIAN_POINT ( 'NONE',  ( 31.17093069310692499, -6.462087684996337345, 7.033357778048657138 ) ) ;
#1381=EDGE_CURVE ( 'NONE', #10674, #2813, #10903, .T. ) ;
#1384=CARTESIAN_POINT ( 'NONE',  ( 9.099998387031005720, -19.29508120620799971, 12.00000000000000000 ) ) ;
#1385=ORIENTED_EDGE ( 'NONE', *, *, #5413, .F. ) ;
#1386=AXIS2_PLACEMENT_3D ( 'NONE', #10169, #15444, #5994 ) ;
#1388=CARTESIAN_POINT ( 'NONE',  ( 26.64639396487419987, -2.308405637095112706, 5.783357778048667797 ) ) ;
#1389=UNCERTAINTY_MEASURE_WITH_UNIT (LENGTH_MEASURE( 1.000000000000000082E-05 ), #897, 'distance_accuracy_value', 'NONE');
#1391=DIRECTION ( 'NONE',  ( -1.000000000000000000, 0.000000000000000000, 0.000000000000000000 ) ) ;
#1395=CARTESIAN_POINT ( 'NONE',  ( 29.14074637024071990, -5.979778010479330774, 8.283357778048660691 ) ) ;
#1399=CARTESIAN_POINT ( 'NONE',  ( 27.91310269393460430, -7.181753375802955475, 5.783357778048657138 ) ) ;
#1401=CARTESIAN_POINT ( 'NONE',  ( 25.76872643656706074, -21.83605427490913797, 14.29305147543152366 ) ) ;
#1403=EDGE_LOOP ( 'NONE', ( #16798, #2310, #7379, #1277 ) ) ;
#1405=ORIENTED_EDGE ( 'NONE', *, *, #961, .F. ) ;
#1410=CARTESIAN_POINT ( 'NONE',  ( -1.917618200156724081E-28, -7.000000000000001776, 6.000000000000000000 ) ) ;
#1413=CARTESIAN_POINT ( 'NONE',  ( 29.01637427789896151, -7.048830937829683840, 5.783357778048658027 ) ) ;
#1415=CARTESIAN_POINT ( 'NONE',  ( 31.63927044622584717, -1.706862622621797110, 6.453230759126472371 ) ) ;
#1416=CARTESIAN_POINT ( 'NONE',  ( 32.50119254608192421, -4.121097024973739309, 7.939653947423662039 ) ) ;
#1418=ORIENTED_EDGE ( 'NONE', *, *, #1366, .T. ) ;
#1422=CARTESIAN_POINT ( 'NONE',  ( 29.50659824675005893, -4.481886499472614638, 3.627061608673664228 ) ) ;
#1425=CARTESIAN_POINT ( 'NONE',  ( 27.63266882139180325, -2.199775856772564708, 5.783357778048668685 ) ) ;
#1426=CARTESIAN_POINT ( 'NONE',  ( 30.71189515440122975, -6.854751018602581958, 5.783357778048664244 ) ) ;
#1428=DIRECTION ( 'NONE',  ( 0.000000000000000000, 0.000000000000000000, -1.000000000000000000 ) ) ;
#1430=CARTESIAN_POINT ( 'NONE',  ( 30.05650519998692971, -5.408673599982567026, 13.28483438372752445 ) ) ;
#1437=CARTESIAN_POINT ( 'NONE',  ( 5.499998817156068753, -20.49639288455253450, 13.00000000000000178 ) ) ;
#1442=FACE_OUTER_BOUND ( 'NONE', #12868, .T. ) ;
#1443=ORIENTED_EDGE ( 'NONE', *, *, #13426, .T. ) ;
#1447=CARTESIAN_POINT ( 'NONE',  ( 27.49697864365563760, -2.843094376337701679, 4.705209693361167567 ) ) ;
#1461=DIRECTION ( 'NONE',  ( -0.000000000000000000, -0.000000000000000000, 1.000000000000000000 ) ) ;
#1464=CARTESIAN_POINT ( 'NONE',  ( 28.51030546511822195, -6.055733689321201041, 8.283357778048660691 ) ) ;
#1466=CARTESIAN_POINT ( 'NONE',  ( 32.47301885516785092, -2.670677813450649474, 8.283357778048664244 ) ) ;
#1468=VERTEX_POINT ( 'NONE', #13002 ) ;
#1471=DIRECTION ( 'NONE',  ( -0.000000000000000000, -1.000000000000000000, -0.000000000000000000 ) ) ;
#1473=VERTEX_POINT ( 'NONE', #14374 ) ;
#1485=DIRECTION ( 'NONE',  ( 1.000000000000000000, 0.000000000000000000, 0.000000000000000000 ) ) ;
#1487=AXIS2_PLACEMENT_3D ( 'NONE', #6586, #17784, #13491 ) ;
#1491=CARTESIAN_POINT ( 'NONE',  ( 26.60013260893011378, -1.924431040879551746, 5.783357778048668685 ) ) ;
#1493=CARTESIAN_POINT ( 'NONE',  ( 27.04606801335823718, -3.524390735323772006, 3.627061608673666893 ) ) ;
#1498=AXIS2_PLACEMENT_3D ( 'NONE', #7821, #3735, #9092 ) ;
#1503=LINE ( 'NONE', #17936, #9904 ) ;
#1511=CARTESIAN_POINT ( 'NONE',  ( 28.99445422935450267, -6.424501337975009996, 4.705209693361160461 ) ) ;
#1513=CARTESIAN_POINT ( 'NONE',  ( 5.499998817156068753, -20.49639288455253450, 12.00000000000000000 ) ) ;
#1515=AXIS2_PLACEMENT_3D ( 'NONE', #6480, #11994, #10616 ) ;
#1516=CARTESIAN_POINT ( 'NONE',  ( 29.15206445563513071, -6.405512418264540209, 4.705209693361159573 ) ) ;
#1517=ORIENTED_EDGE ( 'NONE', *, *, #13251, .T. ) ;
#1522=CARTESIAN_POINT ( 'NONE',  ( 28.87615734162756453, -4.557842178314484016, 3.627061608673664228 ) ) ;
#1525=CARTESIAN_POINT ( 'NONE',  ( 30.45035428628836627, -2.914368949527523789, 3.283357778048666464 ) ) ;
#1528=DIRECTION ( 'NONE',  ( -0.1196152422706618645, 0.9928203230275510771, 0.000000000000000000 ) ) ;
#1534=CARTESIAN_POINT ( 'NONE',  ( 29.25000000000000000, -16.21813761408365195, 13.37255996287876236 ) ) ;
#1542=ORIENTED_EDGE ( 'NONE', *, *, #7546, .T. ) ;
#1544=VERTEX_POINT ( 'NONE', #11995 ) ;
#1545=CARTESIAN_POINT ( 'NONE',  ( 30.27725608814395386, -6.896919580145944195, 5.783357778048658915 ) ) ;
#1551=CARTESIAN_POINT ( 'NONE',  ( -25.11802603177690330, -16.03270077640482683, 10.53798182577225084 ) ) ;
#1552=DIRECTION ( 'NONE',  ( 0.000000000000000000, -1.000000000000000000, 0.000000000000000000 ) ) ;
#1562=CARTESIAN_POINT ( 'NONE',  ( 32.96459815279162342, -1.884545423566157174, 7.033357778048666020 ) ) ;
#1565=ORIENTED_EDGE ( 'NONE', *, *, #5453, .T. ) ;
#1575=CARTESIAN_POINT ( 'NONE',  ( 20.00000000000000000, 7.999999999999996447, 15.51150668642334374 ) ) ;
#1583=CARTESIAN_POINT ( 'NONE',  ( -20.00000000000000000, 7.999999999999996447, 6.000000000000000000 ) ) ;
#1584=CARTESIAN_POINT ( 'NONE',  ( 25.61697401368257587, -3.496695820648536568, 8.283357778048664244 ) ) ;
#1586=CARTESIAN_POINT ( 'NONE',  ( 26.51200394741821498, -4.842675973971495296, 3.627061608673664228 ) ) ;
#1587=CARTESIAN_POINT ( 'NONE',  ( -27.68843801662522353, -20.37088413741627235, 13.80304640004047023 ) ) ;
#1588=FACE_OUTER_BOUND ( 'NONE', #14144, .T. ) ;
#1591=ORIENTED_EDGE ( 'NONE', *, *, #13557, .T. ) ;
#1593=( BOUNDED_CURVE ( )  B_SPLINE_CURVE ( 2, ( #4224, #12834, #15370, #15275, #12644, #7044, #6934, #423, #2953 ),
 .UNSPECIFIED., .F., .T. ) 
 B_SPLINE_CURVE_WITH_KNOTS ( ( 3, 2, 2, 2, 3 ),
 ( 0.01923076923076925265, 0.02564102564102564014, 0.03846153846153846367, 0.05128205128205128027, 0.05769230769230772327 ),
 .UNSPECIFIED. ) 
 CURVE ( )  GEOMETRIC_REPRESENTATION_ITEM ( )  RATIONAL_B_SPLINE_CURVE ( ( 0.9330127018922194093, 0.9330127018922196314, 1.000000000000000000, 0.8660254037844387076, 1.000000000000000000, 0.8660254037844387076, 1.000000000000000000, 0.9330127018922189652, 0.9330127018922192983 ) ) 
 REPRESENTATION_ITEM ( '' )  );
#1596=CARTESIAN_POINT ( 'NONE',  ( 2.749999999999992895, -20.49999999999999645, 6.000000000000000000 ) ) ;
#1599=DIRECTION ( 'NONE',  ( -0.000000000000000000, -1.000000000000000000, -0.000000000000000000 ) ) ;
#1607=CARTESIAN_POINT ( 'NONE',  ( 31.06530721954707985, -6.801974981593605030, 5.783357778048657138 ) ) ;
#1610=EDGE_LOOP ( 'NONE', ( #5758, #2567, #184, #10705, #12070, #3518 ) ) ;
#1611=EDGE_CURVE ( 'NONE', #11687, #4942, #3105, .T. ) ;
#1612=CARTESIAN_POINT ( 'NONE',  ( 29.64681518302145591, -6.972875258987813574, 5.783357778048658027 ) ) ;
#1616=CARTESIAN_POINT ( 'NONE',  ( 30.41656616297672500, -2.191532958677927745, 4.533357778048667797 ) ) ;
#1617=ORIENTED_EDGE ( 'NONE', *, *, #4835, .T. ) ;
#1622=DIRECTION ( 'NONE',  ( 1.000000000000000000, 0.000000000000000000, 0.000000000000000000 ) ) ;
#1633=ORIENTED_EDGE ( 'NONE', *, *, #14529, .F. ) ;
#1635=CARTESIAN_POINT ( 'NONE',  ( 28.99445422935450267, -6.424501337975009996, 4.705209693361160461 ) ) ;
#1643=FACE_OUTER_BOUND ( 'NONE', #7429, .T. ) ;
#1648=FACE_OUTER_BOUND ( 'NONE', #13072, .T. ) ;
#1649=DIRECTION ( 'NONE',  ( 0.000000000000000000, 1.000000000000000000, 0.000000000000000000 ) ) ;
#1651=CARTESIAN_POINT ( 'NONE',  ( 30.40162818048570514, -5.827866652795590241, 8.283357778048658915 ) ) ;
#1652=DIRECTION ( 'NONE',  ( 0.9928203230275512992, 0.1196152422706610180, 4.006172263299093133E-17 ) ) ;
#1659=VERTEX_POINT ( 'NONE', #10600 ) ;
#1671=CARTESIAN_POINT ( 'NONE',  ( 32.14213199643172914, -2.910415664685331638, 7.939653947423664704 ) ) ;
#1673=EDGE_CURVE ( 'NONE', #11071, #12891, #14799, .T. ) ;
#1674=CARTESIAN_POINT ( 'NONE',  ( 26.65222088368961195, -7.333664733486695120, 5.783357778048657138 ) ) ;
#1675=CARTESIAN_POINT ( 'NONE',  ( -29.20851401586840979, -17.04915871481012246, 13.38439546398730329 ) ) ;
#1676=CARTESIAN_POINT ( 'NONE',  ( 29.77118727536321074, -5.903822331637461396, 8.283357778048660691 ) ) ;
#1677=EDGE_LOOP ( 'NONE', ( #3552, #11692, #15019, #10159 ) ) ;
#1678=CARTESIAN_POINT ( 'NONE',  ( 28.55903157092087952, -3.142235986053133256, 3.283357778048666464 ) ) ;
#1681=EDGE_LOOP ( 'NONE', ( #2872, #12942, #8506, #11459 ) ) ;
#1685=CARTESIAN_POINT ( 'NONE',  ( 33.50243880635947846, -1.482387629897225390, 5.783357778048663356 ) ) ;
#1690=CYLINDRICAL_SURFACE ( 'NONE', #4990, 2.500000000000001776 ) ;
#1691=CARTESIAN_POINT ( 'NONE',  ( 32.29295089585318834, -5.599999616269981217, 8.283357778048660691 ) ) ;
#1693=CARTESIAN_POINT ( 'NONE',  ( 31.24031073583692475, -4.273008382657478954, 7.939653947423662039 ) ) ;
#1696=ORIENTED_EDGE ( 'NONE', *, *, #592, .T. ) ;
#1697=CARTESIAN_POINT ( 'NONE',  ( 27.49697864365563760, -2.843094376337701679, 4.705209693361167567 ) ) ;
#1702=CARTESIAN_POINT ( 'NONE',  ( 30.71189515440122975, -6.854751018602581958, 5.783357778048664244 ) ) ;
#1709=CARTESIAN_POINT ( 'NONE',  ( 25.90934487712387480, 0.1208734971681818676, -4.216642221951339309 ) ) ;
#1712=CYLINDRICAL_SURFACE ( 'NONE', #15739, 5.000000000000000000 ) ;
#1715=ADVANCED_FACE ( 'NONE', ( #10335 ), #17464, .F. ) ;
#1722=CARTESIAN_POINT ( 'NONE',  ( 28.73594040535617467, -2.066853418799292630, 5.783357778048668685 ) ) ;
#1726=DIRECTION ( 'NONE',  ( -0.9928203230275510771, -0.1196152422706610735, 0.000000000000000000 ) ) ;
#1731=CIRCLE ( 'NONE', #11847, 2.000000000000001776 ) ;
#1732=CARTESIAN_POINT ( 'NONE',  ( 13.00000000000000178, 0.000000000000000000, 6.000000000000000000 ) ) ;
#1736=CARTESIAN_POINT ( 'NONE',  ( 26.01652455409633902, -4.902371455920926380, 5.783357778048663356 ) ) ;
#1739=B_SPLINE_CURVE_WITH_KNOTS ( 'NONE', 3,
 ( #15486, #8503, #8586, #15572, #17039, #1983, #10116, #15666, #3336, #11568, #8866, #14399, #7506, #15393, #2981, #1401, #9374, #6753, #1132, #1052, #13642, #5289, #8018, #14915, #2583, #2495, #16294, #9294, #17932, #41, #2765, #1232, #12284, #16381, #6573, #10982, #16460, #6921, #8110, #11075, #14834, #9631, #6658 ),
 .UNSPECIFIED., .F., .F.,
 ( 4, 2, 2, 1, 2, 2, 2, 2, 2, 2, 2, 2, 2, 2, 2, 2, 2, 2, 2, 2, 2, 4 ),
 ( 0.01976987703536532692, 0.02100501831352976842, 0.02162258895261198396, 0.02224015959169420298, 0.02285773023077641852, 0.02347530086985863407, 0.02471044214802306516, 0.02594558342618749971, 0.02718072470435193080, 0.02779829534343414288, 0.02841586598251635495, 0.02965100726068079298, 0.03088614853884522754, 0.03150371917792745002, 0.03212128981700967945, 0.03335643109517413829, 0.03459157237333859714, 0.03582671365150305598, 0.03644428429058528540, 0.03706185492966751482, 0.03829699620783197367, 0.03953213748599642557 ),
 .UNSPECIFIED. ) ;
#1740=AXIS2_PLACEMENT_3D ( 'NONE', #5863, #7155, #11283 ) ;
#1741=CIRCLE ( 'NONE', #10673, 14.00000000000000178 ) ;
#1742=CARTESIAN_POINT ( 'NONE',  ( 26.82229025357024454, -7.323371595517525812, 6.453230759126462601 ) ) ;
#1744=CARTESIAN_POINT ( 'NONE',  ( 27.81599742762458050, -2.504850134108091098, 4.533357778048667797 ) ) ;
#1749=CYLINDRICAL_SURFACE ( 'NONE', #2139, 2.500000000000001776 ) ;
#1754=AXIS2_PLACEMENT_3D ( 'NONE', #2951, #1599, #1782 ) ;
#1763=VECTOR ( 'NONE', #10981, 1000.000000000000114 ) ;
#1765=CARTESIAN_POINT ( 'NONE',  ( 32.64557936882268052, -2.222789665795767089, 6.861505862736165362 ) ) ;
#1769=CARTESIAN_POINT ( 'NONE',  ( -16.96458082634299558, -17.85487492059188597, 16.00470661676384054 ) ) ;
#1771=ORIENTED_EDGE ( 'NONE', *, *, #6840, .T. ) ;
#1776=ORIENTED_EDGE ( 'NONE', *, *, #17144, .T. ) ;
#1779=AXIS2_PLACEMENT_3D ( 'NONE', #16654, #16311, #6853 ) ;
#1782=DIRECTION ( 'NONE',  ( 0.000000000000000000, 0.000000000000000000, -1.000000000000000000 ) ) ;
#1783=PRODUCT_CONTEXT ( 'NONE', #5262, 'mechanical' ) ;
#1788=DIRECTION ( 'NONE',  ( -0.1196152422706610735, 0.9928203230275511881, 0.000000000000000000 ) ) ;
#1790=CARTESIAN_POINT ( 'NONE',  ( 29.13014440709066832, -5.781182818409868140, 3.627061608673662896 ) ) ;
#1791=( BOUNDED_CURVE ( )  B_SPLINE_CURVE ( 3, ( #6007, #677, #1872, #6201 ),
 .UNSPECIFIED., .F., .T. ) 
 B_SPLINE_CURVE_WITH_KNOTS ( ( 4, 4 ),
 ( 4.889642689481717319, 5.052230418047667371 ),
 .UNSPECIFIED. ) 
 CURVE ( )  GEOMETRIC_REPRESENTATION_ITEM ( )  RATIONAL_B_SPLINE_CURVE ( ( 1.000000000000000000, 0.9977983154653931042, 0.9977983154653931042, 1.000000000000000000 ) ) 
 REPRESENTATION_ITEM ( '' )  );
#1792=ORIENTED_EDGE ( 'NONE', *, *, #15004, .T. ) ;
#1793=CONICAL_SURFACE ( 'NONE', #9020, 3.999999999999986677, 0.7853981633974400633 ) ;
#1796=CARTESIAN_POINT ( 'NONE',  ( 28.25893984004492765, -6.513116296623863377, 6.861505862736158257 ) ) ;
#1800=CARTESIAN_POINT ( 'NONE',  ( 25.86833963875586306, -3.039313213345869791, 6.861505862736166250 ) ) ;
#1805=CARTESIAN_POINT ( 'NONE',  ( -1.917618200156724081E-28, -7.000000000000001776, 0.000000000000000000 ) ) ;
#1818=EDGE_LOOP ( 'NONE', ( #15282, #13982, #15252, #337 ) ) ;
#1820=CARTESIAN_POINT ( 'NONE',  ( 27.47505859511117521, -2.218764776483033163, 5.783357778048668685 ) ) ;
#1836=CARTESIAN_POINT ( 'NONE',  ( 35.19141017012124451, -14.17387298022714326, 11.46934516270796323 ) ) ;
#1840=CARTESIAN_POINT ( 'NONE',  ( 30.01512236704901682, -6.601339762873093875, 4.533357778048659803 ) ) ;
#1847=VERTEX_POINT ( 'NONE', #13871 ) ;
#1855=ORIENTED_EDGE ( 'NONE', *, *, #17095, .F. ) ;
#1858=CARTESIAN_POINT ( 'NONE',  ( -1.917618200156724081E-28, -7.000000000000001776, 6.000000000000000000 ) ) ;
#1861=CARTESIAN_POINT ( 'NONE',  ( 33.42946061375642586, -6.517141185936593750, 5.783357778048658027 ) ) ;
#1864=CARTESIAN_POINT ( 'NONE',  ( 31.24973580796908834, -6.452593224933654170, 7.033357778048657138 ) ) ;
#1865=CARTESIAN_POINT ( 'NONE',  ( -17.59998316743469715, -19.37170218437266200, 15.90983619775817459 ) ) ;
#1871=EDGE_CURVE ( 'NONE', #9271, #10223, #12515, .T. ) ;
#1872=CARTESIAN_POINT ( 'NONE',  ( -30.05650519998691195, -5.408673599982547486, 13.28483438372753156 ) ) ;
#1879=CARTESIAN_POINT ( 'NONE',  ( 30.42903939560917337, -1.852671564043892660, 5.783357778048667797 ) ) ;
#1883=CARTESIAN_POINT ( 'NONE',  ( 33.32864623319426300, -4.021405196597508613, 8.283357778048662468 ) ) ;
#1884=CARTESIAN_POINT ( 'NONE',  ( 30.39102621733566423, -5.629271460726126719, 3.627061608673662896 ) ) ;
#1885=ORIENTED_EDGE ( 'NONE', *, *, #16260, .F. ) ;
#1887=ORIENTED_EDGE ( 'NONE', *, *, #13260, .T. ) ;
#1888=CARTESIAN_POINT ( 'NONE',  ( 26.45077056032005913, -6.103994453487816330, 3.627061608673662896 ) ) ;
#1894=CARTESIAN_POINT ( 'NONE',  ( 26.31065902414478330, -7.328232685206446106, 5.254681170202263552 ) ) ;
#1900=( NAMED_UNIT ( * ) PLANE_ANGLE_UNIT ( ) SI_UNIT ( $, .RADIAN. ) );
#1903=CARTESIAN_POINT ( 'NONE',  ( 28.36392410707646761, -4.619556167269785796, 8.283357778048662468 ) ) ;
#1904=CARTESIAN_POINT ( 'NONE',  ( 33.24613200752366282, -6.212066908601060256, 4.533357778048659803 ) ) ;
#1906=B_SPLINE_CURVE_WITH_KNOTS ( 'NONE', 1,
 ( #999, #17710 ),
 .UNSPECIFIED., .F., .F.,
 ( 2, 2 ),
 ( 0.000000000000000000, 1.000000000000000000 ),
 .UNSPECIFIED. ) ;
#1907=ORIENTED_EDGE ( 'NONE', *, *, #2046, .F. ) ;
#1909=CARTESIAN_POINT ( 'NONE',  ( 26.98483462626008134, -4.785709214840094816, 3.627061608673664228 ) ) ;
#1910=CARTESIAN_POINT ( 'NONE',  ( 31.66930131758986633, -2.967382423816733894, 7.939653947423662927 ) ) ;
#1912=DIRECTION ( 'NONE',  ( 0.6000000000000001998, -0.7999999999999999334, 0.000000000000000000 ) ) ;
#1919=LINE ( 'NONE', #12960, #7002 ) ;
#1923=ORIENTED_EDGE ( 'NONE', *, *, #14468, .F. ) ;
#1927=DIRECTION ( 'NONE',  ( -0.1196152422706621143, 0.9928203230275509661, 0.000000000000000000 ) ) ;
#1931=CARTESIAN_POINT ( 'NONE',  ( 27.52714686987067694, -7.627998469090175426, 5.783357778048657138 ) ) ;
#1942=DIRECTION ( 'NONE',  ( -1.000000000000000000, 0.000000000000000000, 0.000000000000000000 ) ) ;
#1948=CARTESIAN_POINT ( 'NONE',  ( 31.27962407439061110, -2.387360303286481855, 4.705209693361167567 ) ) ;
#1949=AXIS2_PLACEMENT_3D ( 'NONE', #7182, #6991, #2648 ) ;
#1950=ORIENTED_EDGE ( 'NONE', *, *, #13954, .T. ) ;
#1953=CARTESIAN_POINT ( 'NONE',  ( 26.01652455409633902, -4.902371455920926380, 5.783357778048663356 ) ) ;
#1965=LINE ( 'NONE', #13109, #4002 ) ;
#1966=CARTESIAN_POINT ( 'NONE',  ( 33.52375369703867847, -2.544085015380856518, 3.283357778048666464 ) ) ;
#1971=CARTESIAN_POINT ( 'NONE',  ( 26.04653150877178902, -5.151432644682725659, 7.991496109485919597 ) ) ;
#1973=CARTESIAN_POINT ( 'NONE',  ( 32.82963640218302004, -5.962437625020304388, 6.861505862736157368 ) ) ;
#1976=ORIENTED_EDGE ( 'NONE', *, *, #6097, .F. ) ;
#1977=FACE_OUTER_BOUND ( 'NONE', #3480, .T. ) ;
#1983=CARTESIAN_POINT ( 'NONE',  ( 28.91480295676398171, -18.24795679052564168, 13.46730161501605316 ) ) ;
#1988=CARTESIAN_POINT ( 'NONE',  ( 30.69058026372202974, -5.793053633118939061, 3.283357778048663800 ) ) ;
#1990=ORIENTED_EDGE ( 'NONE', *, *, #11427, .T. ) ;
#1994=CARTESIAN_POINT ( 'NONE',  ( 26.45077056032005913, -6.103994453487816330, 3.627061608673662896 ) ) ;
#1998=FACE_OUTER_BOUND ( 'NONE', #12793, .T. ) ;
#2004=( BOUNDED_CURVE ( )  B_SPLINE_CURVE ( 2, ( #12224, #6600, #15029, #6524, #5230, #16577, #12036, #9405, #17799 ),
 .UNSPECIFIED., .F., .T. ) 
 B_SPLINE_CURVE_WITH_KNOTS ( ( 3, 2, 2, 2, 3 ),
 ( 0.4423076923076923461, 0.4487179487179487336, 0.4615384615384615641, 0.4743589743589743390, 0.4807692307692307820 ),
 .UNSPECIFIED. ) 
 CURVE ( )  GEOMETRIC_REPRESENTATION_ITEM ( )  RATIONAL_B_SPLINE_CURVE ( ( 0.9330127018922194093, 0.9330127018922196314, 1.000000000000000000, 0.8660254037844387076, 1.000000000000000000, 0.8660254037844387076, 1.000000000000000000, 0.9330127018922190762, 0.9330127018922194093 ) ) 
 REPRESENTATION_ITEM ( '' )  );
#2008=EDGE_LOOP ( 'NONE', ( #14323, #3119, #13925, #6516, #3343, #3960, #8396, #13583, #9584, #17855, #7809 ) ) ;
#2014=CARTESIAN_POINT ( 'NONE',  ( 27.45957062324739795, -6.182326487390973568, 3.283357778048663800 ) ) ;
#2035=CARTESIAN_POINT ( 'NONE',  ( 31.51621784984448738, -6.120678622607529817, 4.705209693361160461 ) ) ;
#2046=EDGE_CURVE ( 'NONE', #11770, #9400, #277, .T. ) ;
#2048=CARTESIAN_POINT ( 'NONE',  ( 32.85952466860454280, -1.897204703373130741, 4.533357778048667797 ) ) ;
#2051=FACE_OUTER_BOUND ( 'NONE', #14308, .T. ) ;
#2052=AXIS2_PLACEMENT_3D ( 'NONE', #16004, #7472, #7829 ) ;
#2058=LINE ( 'NONE', #10366, #6162 ) ;
#2060=CARTESIAN_POINT ( 'NONE',  ( 27.65911562847151117, -5.958412735707574015, 7.939653947423658487 ) ) ;
#2065=ORIENTED_EDGE ( 'NONE', *, *, #5392, .F. ) ;
#2066=CARTESIAN_POINT ( 'NONE',  ( 32.32618902979206865, -6.650063623909865385, 5.783357778048657138 ) ) ;
#2067=CARTESIAN_POINT ( 'NONE',  ( -27.54501800341186168, -11.92321325334030568, 13.84074570522889047 ) ) ;
#2070=VERTEX_POINT ( 'NONE', #1732 ) ;
#2072=CYLINDRICAL_SURFACE ( 'NONE', #2603, 2.749999999999992006 ) ;
#2085=CARTESIAN_POINT ( 'NONE',  ( 31.38859741546781379, -7.162769935976271540, 5.783357778048657138 ) ) ;
#2087=VERTEX_POINT ( 'NONE', #7361 ) ;
#2091=CARTESIAN_POINT ( 'NONE',  ( 31.87075164095941915, -4.197052703815608687, 7.939653947423662039 ) ) ;
#2100=CARTESIAN_POINT ( 'NONE',  ( 18.99795248260418745, 9.336063356527739998, 15.69100717631305031 ) ) ;
#2105=ORIENTED_EDGE ( 'NONE', *, *, #8053, .F. ) ;
#2111=CARTESIAN_POINT ( 'NONE',  ( 27.92107091181166467, -2.492190854301117753, 7.033357778048666020 ) ) ;
#2112=AXIS2_PLACEMENT_3D ( 'NONE', #5664, #8577, #16941 ) ;
#2121=ORIENTED_EDGE ( 'NONE', *, *, #6696, .F. ) ;
#2132=CARTESIAN_POINT ( 'NONE',  ( 28.82057243903374655, -7.082618055128190093, 5.783357778048657138 ) ) ;
#2134=AXIS2_PLACEMENT_3D ( 'NONE', #2794, #14951, #12318 ) ;
#2135=VERTEX_POINT ( 'NONE', #8708 ) ;
#2139=AXIS2_PLACEMENT_3D ( 'NONE', #14071, #4278, #15607 ) ;
#2140=ORIENTED_EDGE ( 'NONE', *, *, #5392, .T. ) ;
#2142=FACE_BOUND ( 'NONE', #15014, .T. ) ;
#2147=ORIENTED_EDGE ( 'NONE', *, *, #8896, .T. ) ;
#2152=VECTOR ( 'NONE', #543, 1000.000000000000000 ) ;
#2156=CARTESIAN_POINT ( 'NONE',  ( 27.77288575766320378, -4.690764616287755651, 3.627061608673664228 ) ) ;
#2161=CARTESIAN_POINT ( 'NONE',  ( 33.13163345120441505, -4.045141346131868154, 7.939653947423662039 ) ) ;
#2162=CARTESIAN_POINT ( 'NONE',  ( -20.46503100693326260, -10.50166121531458430, 15.42720773483998009 ) ) ;
#2167=FACE_OUTER_BOUND ( 'NONE', #2291, .T. ) ;
#2176=CARTESIAN_POINT ( 'NONE',  ( 31.64365984991007252, -1.316785610144591390, 5.783357778048668685 ) ) ;
#2179=VERTEX_POINT ( 'NONE', #6341 ) ;
#2180=ORIENTED_EDGE ( 'NONE', *, *, #6084, .T. ) ;
#2182=FACE_OUTER_BOUND ( 'NONE', #17259, .T. ) ;
#2188=CARTESIAN_POINT ( 'NONE',  ( 29.11066736118121767, -3.075774767273946608, 3.283357778048666464 ) ) ;
#2192=CARTESIAN_POINT ( 'NONE',  ( 34.07870238058739432, -4.938269840783200415, 5.783357778048663356 ) ) ;
#2199=ORIENTED_EDGE ( 'NONE', *, *, #1098, .T. ) ;
#2201=CARTESIAN_POINT ( 'NONE',  ( 33.95908713831673964, -3.945449517755641455, 8.283357778048662468 ) ) ;
#2204=FACE_OUTER_BOUND ( 'NONE', #7802, .T. ) ;
#2210=CARTESIAN_POINT ( 'NONE',  ( 0.000000000000000000, 0.000000000000000000, 12.00000000000000000 ) ) ;
#2213=VERTEX_POINT ( 'NONE', #904 ) ;
#2222=CARTESIAN_POINT ( 'NONE',  ( 33.95908713831673964, -3.945449517755641455, 8.283357778048662468 ) ) ;
#2227=CARTESIAN_POINT ( 'NONE',  ( -25.11802603177690330, -19.03270077640483038, 0.5379818257722508434 ) ) ;
#2235=DIRECTION ( 'NONE',  ( 1.000000000000000000, 0.000000000000000000, 0.000000000000000000 ) ) ;
#2240=CARTESIAN_POINT ( 'NONE',  ( 26.82722439997946395, -4.804698134550569044, 7.939653947423662039 ) ) ;
#2244=CARTESIAN_POINT ( 'NONE',  ( 26.49461065740898036, -7.352653653197164019, 5.783357778048658027 ) ) ;
#2247=VERTEX_POINT ( 'NONE', #2192 ) ;
#2249=CARTESIAN_POINT ( 'NONE',  ( 30.49166216014303643, -4.363205751385915931, 3.283357778048664244 ) ) ;
#2259=FACE_OUTER_BOUND ( 'NONE', #1681, .T. ) ;
#2260=DIRECTION ( 'NONE',  ( 0.000000000000000000, 0.000000000000000000, 1.000000000000000000 ) ) ;
#2261=CARTESIAN_POINT ( 'NONE',  ( 31.11087420047036289, -5.742416513891037688, 8.283357778048658915 ) ) ;
#2263=VERTEX_POINT ( 'NONE', #4975 ) ;
#2264=EDGE_LOOP ( 'NONE', ( #291, #15770, #3880, #3682, #12528, #12381 ) ) ;
#2265=VERTEX_POINT ( 'NONE', #9233 ) ;
#2266=CARTESIAN_POINT ( 'NONE',  ( 26.21417678486618641, -2.370676134166772808, 5.783357778048668685 ) ) ;
#2267=CARTESIAN_POINT ( 'NONE',  ( 32.07220196432898263, -5.426722983814484813, 7.939653947423658487 ) ) ;
#2268=ORIENTED_EDGE ( 'NONE', *, *, #8081, .F. ) ;
#2272=LINE ( 'NONE', #9403, #6139 ) ;
#2277=EDGE_CURVE ( 'NONE', #10674, #16241, #17626, .T. ) ;
#2279=ADVANCED_FACE ( 'NONE', ( #3634, #14422 ), #9157, .T. ) ;
#2286=CARTESIAN_POINT ( 'NONE',  ( 26.07857582428556853, -4.894895503279006022, 3.283357778048664244 ) ) ;
#2291=EDGE_LOOP ( 'NONE', ( #13405, #6679, #1165, #2943, #17413 ) ) ;
#2292=( BOUNDED_CURVE ( )  B_SPLINE_CURVE ( 3, ( #631, #4611, #13141, #459 ),
 .UNSPECIFIED., .F., .T. ) 
 B_SPLINE_CURVE_WITH_KNOTS ( ( 4, 4 ),
 ( 1.316154292592045083, 1.436990331221392081 ),
 .UNSPECIFIED. ) 
 CURVE ( )  GEOMETRIC_REPRESENTATION_ITEM ( )  RATIONAL_B_SPLINE_CURVE ( ( 1.000000000000000000, 0.9987835910734581546, 0.9987835910734581546, 1.000000000000000000 ) ) 
 REPRESENTATION_ITEM ( '' )  );
#2295=CARTESIAN_POINT ( 'NONE',  ( 25.78902048130849423, -3.014061381488923885, 6.808963882184758454 ) ) ;
#2297=AXIS2_PLACEMENT_3D ( 'NONE', #11180, #16751, #15385 ) ;
#2304=DIRECTION ( 'NONE',  ( 0.9928203230275510771, 0.1196152422706609902, 4.006172263299092517E-17 ) ) ;
#2305=CARTESIAN_POINT ( 'NONE',  ( -23.00000000000000000, -16.21813761408365195, 13.00000000000000178 ) ) ;
#2310=ORIENTED_EDGE ( 'NONE', *, *, #11089, .T. ) ;
#2311=ORIENTED_EDGE ( 'NONE', *, *, #16894, .F. ) ;
#2314=ORIENTED_EDGE ( 'NONE', *, *, #5721, .T. ) ;
#2315=CARTESIAN_POINT ( 'NONE',  ( 25.76466184735054910, -2.811881907026620553, 5.318565573966401061 ) ) ;
#2318=DIRECTION ( 'NONE',  ( -1.000000000000000000, 0.000000000000000000, 0.000000000000000000 ) ) ;
#2326=CARTESIAN_POINT ( 'NONE',  ( 31.58296173575813981, -1.713646710223874381, 5.113484796970860558 ) ) ;
#2329=DIRECTION ( 'NONE',  ( 1.000000000000000000, 0.000000000000000000, 0.000000000000000000 ) ) ;
#2331=CARTESIAN_POINT ( 'NONE',  ( 26.63030083514515312, -6.709335133632020387, 4.705209693361159573 ) ) ;
#2336=CARTESIAN_POINT ( 'NONE',  ( 30.28142597461332741, -2.507623461452779701, 6.861505862736166250 ) ) ;
#2337=CARTESIAN_POINT ( 'NONE',  ( -28.60529878918911706, -13.42304697295875648, 13.55371198823188017 ) ) ;
#2341=DIRECTION ( 'NONE',  ( 0.6000000000000000888, -0.7999999999999999334, 0.000000000000000000 ) ) ;
#2342=ORIENTED_EDGE ( 'NONE', *, *, #11382, .F. ) ;
#2349=AXIS2_PLACEMENT_3D ( 'NONE', #9861, #374, #7085 ) ;
#2350=CARTESIAN_POINT ( 'NONE',  ( 3.538288549924106796, -15.34800872113743431, 16.99955934415557479 ) ) ;
#2353=CARTESIAN_POINT ( 'NONE',  ( 29.21955148510287614, -5.970283550416647600, 8.283357778048658915 ) ) ;
#2359=CARTESIAN_POINT ( 'NONE',  ( 30.78070346053490880, -6.209293581256383199, 6.861505862736158257 ) ) ;
#2360=CARTESIAN_POINT ( 'NONE',  ( 28.28502977505876359, -2.748149777785362957, 4.705209693361168455 ) ) ;
#2362=CARTESIAN_POINT ( 'NONE',  ( 2.749999999999988454, -20.49999999999999645, 13.00000000000000355 ) ) ;
#2363=CIRCLE ( 'NONE', #5819, 2.749999999999992895 ) ;
#2364=DIRECTION ( 'NONE',  ( 0.7999999999999999334, 0.6000000000000001998, 0.000000000000000000 ) ) ;
#2373=CARTESIAN_POINT ( 'NONE',  ( -15.38839387855823126, 12.77214111725050216, 16.22946975555079163 ) ) ;
#2379=CARTESIAN_POINT ( 'NONE',  ( 26.82912971812490355, -6.258282166232842947, 3.283357778048663800 ) ) ;
#2380=( BOUNDED_CURVE ( )  B_SPLINE_CURVE ( 2, ( #5842, #13828, #11000, #1691, #5747, #15374, #237, #1415, #11260 ),
 .UNSPECIFIED., .F., .T. ) 
 B_SPLINE_CURVE_WITH_KNOTS ( ( 3, 2, 2, 2, 3 ),
 ( 0.2115384615384615641, 0.2179487179487179516, 0.2307692307692307820, 0.2435897435897435848, 0.2500000000000000000 ),
 .UNSPECIFIED. ) 
 CURVE ( )  GEOMETRIC_REPRESENTATION_ITEM ( )  RATIONAL_B_SPLINE_CURVE ( ( 0.9330127018922194093, 0.9330127018922196314, 1.000000000000000000, 0.8660254037844387076, 1.000000000000000000, 0.8660254037844387076, 1.000000000000000000, 0.9330127018922191873, 0.9330127018922194093 ) ) 
 REPRESENTATION_ITEM ( '' )  );
#2382=EDGE_CURVE ( 'NONE', #11016, #11836, #4106, .T. ) ;
#2383=CARTESIAN_POINT ( 'NONE',  ( 26.03726795043090547, -3.446058701420613879, 3.283357778048666464 ) ) ;
#2386=CARTESIAN_POINT ( 'NONE',  ( 27.90727577511918867, -2.156494279411373061, 5.783357778048657138 ) ) ;
#2393=AXIS2_PLACEMENT_3D ( 'NONE', #12034, #14690, #17622 ) ;
#2402=CARTESIAN_POINT ( 'NONE',  ( 30.52163964716380917, -2.178873678870954400, 7.033357778048666020 ) ) ;
#2404=DIRECTION ( 'NONE',  ( 1.000000000000000000, 0.000000000000000000, 0.000000000000000000 ) ) ;
#2410=DIRECTION ( 'NONE',  ( -1.000000000000000000, 0.000000000000000000, 0.000000000000000000 ) ) ;
#2414=CARTESIAN_POINT ( 'NONE',  ( 31.03206908560819954, -5.751910973953720863, 8.283357778048658915 ) ) ;
#2418=CARTESIAN_POINT ( 'NONE',  ( 29.15206445563513071, -6.405512418264540209, 4.705209693361159573 ) ) ;
#2424=FACE_OUTER_BOUND ( 'NONE', #2744, .T. ) ;
#2428=ORIENTED_EDGE ( 'NONE', *, *, #12252, .T. ) ;
#2429=CARTESIAN_POINT ( 'NONE',  ( 31.32102116884452414, -5.717097954277069682, 3.283357778048663356 ) ) ;
#2432=CARTESIAN_POINT ( 'NONE',  ( 26.84461768998868436, -2.294720455324902542, 5.783357778048668685 ) ) ;
#2437=CARTESIAN_POINT ( 'NONE',  ( 27.57216386142120257, -6.895668018177890879, 4.533357778048659803 ) ) ;
#2440=ADVANCED_FACE ( 'NONE', ( #9573 ), #15125, .F. ) ;
#2442=CARTESIAN_POINT ( 'NONE',  ( 31.39792096211754924, -4.254019462947003838, 3.627061608673664228 ) ) ;
#2443=CARTESIAN_POINT ( 'NONE',  ( 30.40841950734487753, -3.119293781500474427, 7.939653947423662927 ) ) ;
#2447=DIRECTION ( 'NONE',  ( -0.1196152422706610735, 0.9928203230275511881, 0.000000000000000000 ) ) ;
#2452=CARTESIAN_POINT ( 'NONE',  ( 31.66176685062031027, -1.704152250161192539, 5.113484796970859669 ) ) ;
#2453=CARTESIAN_POINT ( 'NONE',  ( 19.22414633752738666, -11.22056979495215145, 15.64782563911137814 ) ) ;
#2460=CARTESIAN_POINT ( 'NONE',  ( 31.74131510559286085, -5.666460835049167422, 8.283357778048660691 ) ) ;
#2461=CARTESIAN_POINT ( 'NONE',  ( 25.71748644841968456, -2.420320648352046078, 5.783357778048663356 ) ) ;
#2464=CARTESIAN_POINT ( 'NONE',  ( 30.67110321781257909, -3.087645581983020637, 3.627061608673666449 ) ) ;
#2475=FACE_OUTER_BOUND ( 'NONE', #9632, .T. ) ;
#2481=ORIENTED_EDGE ( 'NONE', *, *, #11895, .F. ) ;
#2487=CARTESIAN_POINT ( 'NONE',  ( 30.63309003953906995, -6.864245478665264244, 5.783357778048664244 ) ) ;
#2491=CARTESIAN_POINT ( 'NONE',  ( 32.57067411085063924, -7.020353038355215070, 5.783357778048657138 ) ) ;
#2492=ORIENTED_EDGE ( 'NONE', *, *, #265, .T. ) ;
#2493=CARTESIAN_POINT ( 'NONE',  ( 29.34898802046944155, -4.500875419183088866, 7.939653947423662039 ) ) ;
#2495=CARTESIAN_POINT ( 'NONE',  ( 21.42986351335030548, -22.27113001973728146, 15.24426822127429659 ) ) ;
#2497=DIRECTION ( 'NONE',  ( -0.000000000000000000, -0.000000000000000000, 1.000000000000000000 ) ) ;
#2505=CARTESIAN_POINT ( 'NONE',  ( 33.14105852333657509, -6.224726188408045147, 7.033357778048657138 ) ) ;
#2507=CARTESIAN_POINT ( 'NONE',  ( 30.25533603959949502, -6.272589980291270351, 4.705209693361160461 ) ) ;
#2512=CARTESIAN_POINT ( 'NONE',  ( 29.18947247604337392, -3.066280307211263878, 3.283357778048666464 ) ) ;
#2515=EDGE_LOOP ( 'NONE', ( #5955, #482 ) ) ;
#2517=CARTESIAN_POINT ( 'NONE',  ( 32.77709966008947617, -5.968767264923789284, 4.705209693361160461 ) ) ;
#2519=CARTESIAN_POINT ( 'NONE',  ( 31.04338717100262102, -6.177645381738930297, 4.705209693361159573 ) ) ;
#2521=DIRECTION ( 'NONE',  ( 0.9928203230275511881, 0.1196152422706610735, 9.614813431917827710E-17 ) ) ;
#2527=VECTOR ( 'NONE', #3474, 1000.000000000000000 ) ;
#2542=VERTEX_POINT ( 'NONE', #6277 ) ;
#2543=CARTESIAN_POINT ( 'NONE',  ( 30.78070346053490880, -6.209293581256383199, 6.861505862736158257 ) ) ;
#2545=CARTESIAN_POINT ( 'NONE',  ( 27.65467808709180630, -4.705006306174339237, 8.283357778048662468 ) ) ;
#2547=FACE_OUTER_BOUND ( 'NONE', #16682, .T. ) ;
#2548=CARTESIAN_POINT ( 'NONE',  ( 25.75668387115780078, -2.745663783273349701, 5.876686579351208195 ) ) ;
#2554=ORIENTED_EDGE ( 'NONE', *, *, #13467, .F. ) ;
#2563=CIRCLE ( 'NONE', #9223, 5.000000000000000000 ) ;
#2565=CARTESIAN_POINT ( 'NONE',  ( -45.00000000000000711, -16.03270077640482683, 0.5379818257722508434 ) ) ;
#2567=ORIENTED_EDGE ( 'NONE', *, *, #17594, .F. ) ;
#2568=CARTESIAN_POINT ( 'NONE',  ( 25.83183225892937784, -3.369404079293177201, 4.123432853728487224 ) ) ;
#2573=CARTESIAN_POINT ( 'NONE',  ( 3.248936832696173393, -30.00000000000000355, -78.00000000000000000 ) ) ;
#2577=CARTESIAN_POINT ( 'NONE',  ( 34.25812524399339765, -6.427500325324518649, 5.783357778048663356 ) ) ;
#2578=CARTESIAN_POINT ( 'NONE',  ( 31.80137159822941939, -6.386132006154467078, 7.033357778048657138 ) ) ;
#2579=ORIENTED_EDGE ( 'NONE', *, *, #7647, .T. ) ;
#2580=ADVANCED_FACE ( 'NONE', ( #2475 ), #5171, .F. ) ;
#2581=CARTESIAN_POINT ( 'NONE',  ( 30.80679339554874119, -2.444327062417882779, 4.705209693361168455 ) ) ;
#2582=CARTESIAN_POINT ( 'NONE',  ( -16.75000000000000000, -16.21813761408365195, 16.03574476417183448 ) ) ;
#2583=CARTESIAN_POINT ( 'NONE',  ( 21.62682814333776804, -22.31876753225984800, 15.20565444446567227 ) ) ;
#2589=EDGE_LOOP ( 'NONE', ( #534, #1950, #17877 ) ) ;
#2595=DIRECTION ( 'NONE',  ( 0.000000000000000000, 1.000000000000000000, 0.000000000000000000 ) ) ;
#2597=CARTESIAN_POINT ( 'NONE',  ( 28.77978050244509944, -3.315512618508630993, 3.627061608673666893 ) ) ;
#2602=CARTESIAN_POINT ( 'NONE',  ( 30.09392748191118017, -6.591845302810410701, 4.533357778048659803 ) ) ;
#2603=AXIS2_PLACEMENT_3D ( 'NONE', #10559, #13479, #14591 ) ;
#2608=CARTESIAN_POINT ( 'NONE',  ( 32.67202617590239555, -5.981426544730773287, 6.861505862736158257 ) ) ;
#2609=CARTESIAN_POINT ( 'NONE',  ( 27.10304229683147526, -4.771467524953526329, 8.283357778048662468 ) ) ;
#2611=AXIS2_PLACEMENT_3D ( 'NONE', #5101, #13275, #11907 ) ;
#2612=CARTESIAN_POINT ( 'NONE',  ( 30.28142597461332741, -2.507623461452779701, 6.861505862736166250 ) ) ;
#2622=CYLINDRICAL_SURFACE ( 'NONE', #2134, 2.500000000000001776 ) ;
#2631=PLANE ( 'NONE',  #8134 ) ;
#2634=CARTESIAN_POINT ( 'NONE',  ( 25.71748644841968456, -2.420320648352046078, 5.783357778048663356 ) ) ;
#2647=DIRECTION ( 'NONE',  ( -1.000000000000000000, 0.000000000000000000, 0.000000000000000000 ) ) ;
#2648=DIRECTION ( 'NONE',  ( -1.000000000000000000, 0.000000000000000000, 0.000000000000000000 ) ) ;
#2654=DIRECTION ( 'NONE',  ( 0.000000000000000000, 1.000000000000000000, 0.000000000000000000 ) ) ;
#2655=VECTOR ( 'NONE', #4703, 1000.000000000000000 ) ;
#2665=CARTESIAN_POINT ( 'NONE',  ( 31.89397184978405519, -6.712334120981523711, 5.783357778048664244 ) ) ;
#2672=CARTESIAN_POINT ( 'NONE',  ( 30.93831368681553684, -6.190304661545915188, 6.861505862736157368 ) ) ;
#2673=LINE ( 'NONE', #1231, #1763 ) ;
#2675=ORIENTED_EDGE ( 'NONE', *, *, #6372, .T. ) ;
#2680=CARTESIAN_POINT ( 'NONE',  ( 8.632250723006720250, -18.84644399697197770, 16.84735068286506987 ) ) ;
#2683=FACE_OUTER_BOUND ( 'NONE', #5573, .T. ) ;
#2687=LINE ( 'NONE', #9306, #4025 ) ;
#2688=CARTESIAN_POINT ( 'NONE',  ( 28.14933959732260149, -3.391468297350501260, 3.627061608673666893 ) ) ;
#2693=CARTESIAN_POINT ( 'NONE',  ( 32.19919549706052209, -6.038393303862174655, 6.861505862736157368 ) ) ;
#2695=ORIENTED_EDGE ( 'NONE', *, *, #4529, .F. ) ;
#2696=ORIENTED_EDGE ( 'NONE', *, *, #6303, .T. ) ;
#2698=CARTESIAN_POINT ( 'NONE',  ( 31.28415083292585663, -5.521667582366822202, 7.939653947423658487 ) ) ;
#2703=CARTESIAN_POINT ( 'NONE',  ( 28.26310972651430120, -2.123820177930694442, 5.783357778048668685 ) ) ;
#2705=CARTESIAN_POINT ( 'NONE',  ( 45.00000000000000711, -19.03270077640483038, 5.537981825772250843 ) ) ;
#2712=CARTESIAN_POINT ( 'NONE',  ( 31.98525019727866692, -6.363978266284800789, 4.533357778048659803 ) ) ;
#2720=VERTEX_POINT ( 'NONE', #12425 ) ;
#2721=CARTESIAN_POINT ( 'NONE',  ( 26.18940075748478691, -6.337263906362392341, 3.743184633113769699 ) ) ;
#2722=CARTESIAN_POINT ( 'NONE',  ( 30.00264913441657555, -6.940201157507134511, 5.783357778048669573 ) ) ;
#2725=CARTESIAN_POINT ( 'NONE',  ( 33.17094678975809074, -2.159493266760871499, 4.705209693361167567 ) ) ;
#2728=CARTESIAN_POINT ( 'NONE',  ( 45.50000000000000000, -16.03270077640482683, 5.537981825772250843 ) ) ;
#2729=CYLINDRICAL_SURFACE ( 'NONE', #14532, 14.00000000000000178 ) ;
#2736=ORIENTED_EDGE ( 'NONE', *, *, #12430, .T. ) ;
#2742=EDGE_CURVE ( 'NONE', #11992, #7755, #15417, .T. ) ;
#2744=EDGE_LOOP ( 'NONE', ( #16538, #8104, #960, #8680, #3077, #3144 ) ) ;
#2745=CARTESIAN_POINT ( 'NONE',  ( -27.17934203385504333, -30.00000000000000355, 12.00000000000000000 ) ) ;
#2752=DIRECTION ( 'NONE',  ( 0.000000000000000000, 0.000000000000000000, -1.000000000000000000 ) ) ;
#2753=ORIENTED_EDGE ( 'NONE', *, *, #8666, .T. ) ;
#2762=EDGE_CURVE ( 'NONE', #6838, #4560, #13379, .T. ) ;
#2763=LINE ( 'NONE', #2936, #2828 ) ;
#2765=CARTESIAN_POINT ( 'NONE',  ( 19.23308179030308551, -21.22208063239337505, 15.64628783324453387 ) ) ;
#2766=ORIENTED_EDGE ( 'NONE', *, *, #17392, .F. ) ;
#2768=DIRECTION ( 'NONE',  ( -0.000000000000000000, -0.000000000000000000, 1.000000000000000000 ) ) ;
#2776=CARTESIAN_POINT ( 'NONE',  ( 30.02326902268086428, -5.673578940050561847, 7.939653947423658487 ) ) ;
#2777=CARTESIAN_POINT ( 'NONE',  ( 6.935828204433864386, -17.68137362934027124, 16.94363565911716663 ) ) ;
#2779=CARTESIAN_POINT ( 'NONE',  ( 32.91278983782564183, -5.325448745358647429, 3.627061608673662896 ) ) ;
#2782=CARTESIAN_POINT ( 'NONE',  ( 26.88845778707760914, -3.543379655034240905, 3.627061608673666893 ) ) ;
#2785=CARTESIAN_POINT ( 'NONE',  ( 26.82722439997946395, -4.804698134550569044, 7.939653947423662039 ) ) ;
#2787=CARTESIAN_POINT ( 'NONE',  ( -7.499998387031003411, -20.49508120620799900, 6.000000000000000000 ) ) ;
#2794=CARTESIAN_POINT ( 'NONE',  ( 26.01652455409633902, -4.902371455920926380, 5.783357778048663356 ) ) ;
#2800=ORIENTED_EDGE ( 'NONE', *, *, #3515, .F. ) ;
#2802=CARTESIAN_POINT ( 'NONE',  ( 32.64557936882268052, -2.222789665795767089, 6.861505862736165362 ) ) ;
#2803=CARTESIAN_POINT ( 'NONE',  ( 30.98067518586950442, -1.786210345264705790, 5.783357778048667797 ) ) ;
#2813=VERTEX_POINT ( 'NONE', #5528 ) ;
#2821=EDGE_LOOP ( 'NONE', ( #11159, #16274, #16071, #4011, #2554 ) ) ;
#2825=DIRECTION ( 'NONE',  ( 0.000000000000000000, 0.000000000000000000, 1.000000000000000000 ) ) ;
#2827=EDGE_CURVE ( 'NONE', #4229, #11393, #12106, .T. ) ;
#2828=VECTOR ( 'NONE', #2841, 1000.000000000000000 ) ;
#2836=CARTESIAN_POINT ( 'NONE',  ( 28.55151181693415907, -2.416235175459247486, 7.033357778048666020 ) ) ;
#2841=DIRECTION ( 'NONE',  ( -1.000000000000000000, 0.000000000000000000, 0.000000000000000000 ) ) ;
#2842=CARTESIAN_POINT ( 'NONE',  ( -24.42841412577760352, -22.30604244805903136, 14.60923613736931514 ) ) ;
#2843=CARTESIAN_POINT ( 'NONE',  ( 33.24613200752366282, -6.212066908601060256, 4.533357778048659803 ) ) ;
#2844=ORIENTED_EDGE ( 'NONE', *, *, #3254, .T. ) ;
#2845=CARTESIAN_POINT ( 'NONE',  ( 31.26353094466156080, -6.788289799823394866, 5.783357778048664244 ) ) ;
#2857=EDGE_CURVE ( 'NONE', #1544, #9271, #1116, .T. ) ;
#2858=CARTESIAN_POINT ( 'NONE',  ( 28.25893984004492765, -6.513116296623863377, 6.861505862736158257 ) ) ;
#2861=CARTESIAN_POINT ( 'NONE',  ( 33.76207435632690590, -3.969185667289998332, 7.939653947423662039 ) ) ;
#2863=AXIS2_PLACEMENT_3D ( 'NONE', #2573, #8100, #5363 ) ;
#2867=CARTESIAN_POINT ( 'NONE',  ( 28.38593337277646711, -7.124786616671554107, 5.783357778048658027 ) ) ;
#2870=CARTESIAN_POINT ( 'NONE',  ( 27.45766530510195835, -4.728742455708699666, 7.939653947423662039 ) ) ;
#2872=ORIENTED_EDGE ( 'NONE', *, *, #3783, .T. ) ;
#2876=CARTESIAN_POINT ( 'NONE',  ( 29.45101334415624095, -7.006662376286321603, 5.783357778048669573 ) ) ;
#2882=DIRECTION ( 'NONE',  ( 0.9928203230275510771, 0.1196152422706609902, 4.006172263299092517E-17 ) ) ;
#2891=CARTESIAN_POINT ( 'NONE',  ( 29.64681518302145946, -6.972875258987813574, 5.783357778048658915 ) ) ;
#2893=VECTOR ( 'NONE', #5036, 1000.000000000000000 ) ;
#2905=CARTESIAN_POINT ( 'NONE',  ( 30.44283453230164227, -2.188368138933637574, 7.033357778048666020 ) ) ;
#2906=CARTESIAN_POINT ( 'NONE',  ( 29.08935247050201767, -2.014077381790315702, 5.783357778048667797 ) ) ;
#2907=ADVANCED_FACE ( 'NONE', ( #2259 ), #10051, .F. ) ;
#2908=CARTESIAN_POINT ( 'NONE',  ( 31.84257795004535652, -2.746633492292519296, 8.283357778048664244 ) ) ;
#2911=CIRCLE ( 'NONE', #9561, 2.749999999999991118 ) ;
#2912=AXIS2_PLACEMENT_3D ( 'NONE', #5047, #6322, #3618 ) ;
#2920=VERTEX_POINT ( 'NONE', #285 ) ;
#2928=ORIENTED_EDGE ( 'NONE', *, *, #8053, .T. ) ;
#2930=EDGE_CURVE ( 'NONE', #13090, #10047, #16789, .T. ) ;
#2933=CARTESIAN_POINT ( 'NONE',  ( 32.51858583609114106, -1.611119345748072362, 5.783357778048668685 ) ) ;
#2935=( BOUNDED_CURVE ( )  B_SPLINE_CURVE ( 2, ( #12242, #15140, #13520, #10938, #2725, #12409, #1278, #6799, #6538, #8247, #10854, #16422, #3820, #8068, #2802, #12051, #9337, #7985, #8162, #16504, #8327, #3988, #10675, #5246, #6616, #15047, #4175, #3907, #17813, #5512, #16347, #13605, #9504, #13694, #3688, #12327, #5331, #17638, #17892, #14877, #5423, #1093, #4075, #9674, #9585, #1357, #11030, #6880, #12146, #15225, #1013, #5158, #16249, #2464, #9419, #17726, #10766, #14958, #2543, #1188, #6704, #16770, #9853, #366, #15679, #175, #455, #12869, #11484, #1545, #16683, #7352, #11397, #15497, #5873, #7078, #16961, #5957, #10035, #12676, #5685, #2891, #4256, #17052, #14132, #4519, #4341, #1722, #8419, #4605, #15311, #13859, #1635, #15582, #4435, #15407, #11294, #11200, #7253, #90, #2993, #9757, #12770, #10129, #8515, #3258, #14048, #3161, #8599, #8699, #14232, #1820, #1447, #6975, #5597, #12505, #7167, #268, #11114, #13953, #5779, #12594, #16873, #9945, #3078, #6152, #1909, #13223, #10573, #13042, #13315, #7784, #6427, #14412, #11578, #2266, #6330, #10401, #800, #1994, #11851, #17246, #4871, #11947, #14685, #15771, #17148 ),
 .UNSPECIFIED., .F., .T. ) 
 B_SPLINE_CURVE_WITH_KNOTS ( ( 3, 2, 2, 2, 2, 2, 2, 2, 2, 2, 2, 2, 2, 2, 2, 2, 2, 2, 2, 2, 2, 2, 2, 2, 2, 2, 2, 2, 2, 2, 2, 2, 2, 2, 2, 2, 2, 2, 2, 2, 2, 2, 2, 2, 2, 2, 2, 2, 2, 2, 2, 2, 2, 2, 2, 2, 2, 2, 2, 2, 2, 2, 2, 2, 2, 2, 2, 2, 2, 2, 2, 2, 2, 3 ),
 ( 0.000000000000000000, 0.01322951968774666726, 0.02645903937549333451, 0.03968855906324000177, 0.05291807875098666902, 0.06614759843873332934, 0.07937711812648000353, 0.09260663781422667773, 0.1058361575019733380, 0.1190656771897200122, 0.1322951968774666587, 0.1455247165652133190, 0.1587542362529600071, 0.1719837559407066396, 0.1852132756284533555, 0.1984427953162000158, 0.2116723150039466761, 0.2249018346916933364, 0.2381313543794400245, 0.2513608740671866570, 0.2645903937549333174, 0.2778199134426800332, 0.2910494331304266380, 0.3042789528181733538, 0.3175084725059200141, 0.3307379921936667300, 0.3439675118814132793, 0.3571970315691599951, 0.3704265512569067109, 0.3836560709446533712, 0.3968855906324000316, 0.4101151103201466364, 0.4233446300078933522, 0.4365741496956400125, 0.4498036693833866728, 0.4630331890711333331, 0.4762627087588800490, 0.4894922284466267093, 0.5027217481343733141, 0.5159512678221199744, 0.5291807875098666347, 0.5424103071976132950, 0.5556398268853600664, 0.5688693465731067267, 0.5820988662608532760, 0.5953283859485999363, 0.6085579056363467076, 0.6217874253240932569, 0.6350169450118400283, 0.6482464646995866886, 0.6614759843873334599, 0.6747055040750800092, 0.6879350237628265585, 0.7011645434505734409, 0.7143940631383199902, 0.7276235828260666505, 0.7408531025138134218, 0.7540826222015599711, 0.7673121418893067425, 0.7805416615770532918, 0.7937711812648000631, 0.8070007009525467234, 0.8202302206402932727, 0.8334597403280399330, 0.8466892600157867044, 0.8599187797035333647, 0.8731482993912800250, 0.8863778190790266853, 0.8996073387667733456, 0.9128368584545200060, 0.9260663781422666663, 0.9392958978300133266, 0.9525254175177600979, 0.9555550897579921932 ),
 .UNSPECIFIED. ) 
 CURVE ( )  GEOMETRIC_REPRESENTATION_ITEM ( )  RATIONAL_B_SPLINE_CURVE ( ( 1.000000000000000000, 0.8660254037844387076, 1.000000000000000000, 0.8660254037844387076, 1.000000000000000000, 0.8660254037844387076, 1.000000000000000000, 0.8660254037844387076, 1.000000000000000000, 0.8660254037844387076, 1.000000000000000000, 0.8660254037844387076, 1.000000000000000000, 0.8660254037844387076, 1.000000000000000000, 0.8660254037844387076, 1.000000000000000000, 0.8660254037844387076, 1.000000000000000000, 0.8660254037844387076, 1.000000000000000000, 0.8660254037844387076, 1.000000000000000000, 0.8660254037844387076, 1.000000000000000000, 0.8660254037844387076, 1.000000000000000000, 0.8660254037844387076, 1.000000000000000000, 0.8660254037844387076, 1.000000000000000000, 0.8660254037844387076, 1.000000000000000000, 0.8660254037844387076, 1.000000000000000000, 0.8660254037844387076, 1.000000000000000000, 0.8660254037844387076, 1.000000000000000000, 0.8660254037844387076, 1.000000000000000000, 0.8660254037844387076, 1.000000000000000000, 0.8660254037844387076, 1.000000000000000000, 0.8660254037844387076, 1.000000000000000000, 0.8660254037844387076, 1.000000000000000000, 0.8660254037844387076, 1.000000000000000000, 0.8660254037844387076, 1.000000000000000000, 0.8660254037844387076, 1.000000000000000000, 0.8660254037844387076, 1.000000000000000000, 0.8660254037844387076, 1.000000000000000000, 0.8660254037844387076, 1.000000000000000000, 0.8660254037844387076, 1.000000000000000000, 0.8660254037844387076, 1.000000000000000000, 0.8660254037844387076, 1.000000000000000000, 0.8660254037844387076, 1.000000000000000000, 0.8660254037844387076, 1.000000000000000000, 0.8660254037844387076, 1.000000000000000000, 0.8660254037844387076, 1.000000000000000000, 0.8660254037844387076, 1.000000000000000000, 0.8660254037844387076, 1.000000000000000000, 0.8660254037844387076, 1.000000000000000000, 0.8660254037844387076, 1.000000000000000000, 0.8660254037844387076, 1.000000000000000000, 0.8660254037844387076, 1.000000000000000000, 0.8660254037844387076, 1.000000000000000000, 0.8660254037844387076, 1.000000000000000000, 0.8660254037844387076, 1.000000000000000000, 0.8660254037844387076, 1.000000000000000000, 0.8660254037844387076, 1.000000000000000000, 0.8660254037844387076, 1.000000000000000000, 0.8660254037844387076, 1.000000000000000000, 0.8660254037844387076, 1.000000000000000000, 0.8660254037844387076, 1.000000000000000000, 0.8660254037844387076, 1.000000000000000000, 0.8660254037844387076, 1.000000000000000000, 0.8660254037844387076, 1.000000000000000000, 0.8660254037844387076, 1.000000000000000000, 0.8660254037844387076, 1.000000000000000000, 0.8660254037844387076, 1.000000000000000000, 0.8660254037844387076, 1.000000000000000000, 0.8660254037844387076, 1.000000000000000000, 0.8660254037844387076, 1.000000000000000000, 0.8660254037844387076, 1.000000000000000000, 0.8660254037844387076, 1.000000000000000000, 0.8660254037844387076, 1.000000000000000000, 0.8660254037844387076, 1.000000000000000000, 0.8660254037844387076, 1.000000000000000000, 0.8660254037844387076, 1.000000000000000000, 0.8660254037844387076, 1.000000000000000000, 0.8660254037844387076, 1.000000000000000000, 0.8660254037844387076, 1.000000000000000000, 0.8660254037844387076, 1.000000000000000000, 0.8660254037844387076, 1.000000000000000000, 0.9693186809021840933, 0.9526899265169710418 ) ) 
 REPRESENTATION_ITEM ( '' )  );
#2936=CARTESIAN_POINT ( 'NONE',  ( -25.11802603177690330, -16.03270077640482683, 0.5379818257722508434 ) ) ;
#2937=CARTESIAN_POINT ( 'NONE',  ( -25.20430036322041545, -22.07000804769847591, 14.42834449896450799 ) ) ;
#2938=CARTESIAN_POINT ( 'NONE',  ( 33.23365877489121090, -6.550928303235100891, 5.783357778048664244 ) ) ;
#2939=AXIS2_PLACEMENT_3D ( 'NONE', #1805, #4920, #2318 ) ;
#2940=VERTEX_POINT ( 'NONE', #9869 ) ;
#2943=ORIENTED_EDGE ( 'NONE', *, *, #12056, .T. ) ;
#2944=CARTESIAN_POINT ( 'NONE',  ( 26.90793483298705979, -6.248787706170159773, 3.283357778048663356 ) ) ;
#2945=VERTEX_POINT ( 'NONE', #15424 ) ;
#2951=CARTESIAN_POINT ( 'NONE',  ( 45.00000000000000711, -16.03270077640482683, 5.537981825772250843 ) ) ;
#2953=CARTESIAN_POINT ( 'NONE',  ( 33.78529456515154550, -6.484467084455913799, 5.783357778048664244 ) ) ;
#2958=CARTESIAN_POINT ( 'NONE',  ( 30.17635249042624679, -2.520282741259753045, 4.705209693361168455 ) ) ;
#2959=EDGE_CURVE ( 'NONE', #7076, #5666, #14064, .T. ) ;
#2963=( BOUNDED_CURVE ( )  B_SPLINE_CURVE ( 2, ( #5127, #16219, #13489, #17782, #17866 ),
 .UNSPECIFIED., .F., .T. ) 
 B_SPLINE_CURVE_WITH_KNOTS ( ( 3, 2, 3 ),
 ( 0.000000000000000000, 0.01282051282051282007, 0.01923076923076925265 ),
 .UNSPECIFIED. ) 
 CURVE ( )  GEOMETRIC_REPRESENTATION_ITEM ( )  RATIONAL_B_SPLINE_CURVE ( ( 1.000000000000000000, 0.8660254037844387076, 1.000000000000000000, 0.9330127018922191873, 0.9330127018922194093 ) ) 
 REPRESENTATION_ITEM ( '' )  );
#2965=CARTESIAN_POINT ( 'NONE',  ( 28.77978050244509944, -3.315512618508630993, 3.627061608673666893 ) ) ;
#2970=CARTESIAN_POINT ( 'NONE',  ( 30.74004950963507810, -6.851358974801540214, 5.113484796970852564 ) ) ;
#2972=ORIENTED_EDGE ( 'NONE', *, *, #8391, .T. ) ;
#2975=CYLINDRICAL_SURFACE ( 'NONE', #7300, 13.00000000000000178 ) ;
#2981=CARTESIAN_POINT ( 'NONE',  ( 26.12396475346091052, -21.64644127732803014, 14.20549555447399470 ) ) ;
#2989=ORIENTED_EDGE ( 'NONE', *, *, #3415, .F. ) ;
#2992=ORIENTED_EDGE ( 'NONE', *, *, #3137, .T. ) ;
#2993=CARTESIAN_POINT ( 'NONE',  ( 28.12741954877813555, -2.767138697495831856, 4.705209693361167567 ) ) ;
#2994=EDGE_CURVE ( 'NONE', #9531, #3302, #8385, .T. ) ;
#3001=DIRECTION ( 'NONE',  ( -1.000000000000000000, 0.000000000000000000, 0.000000000000000000 ) ) ;
#3010=CARTESIAN_POINT ( 'NONE',  ( 27.92107091181166467, -2.492190854301117753, 7.033357778048666020 ) ) ;
#3012=CARTESIAN_POINT ( 'NONE',  ( 31.56485473504790917, -1.326280070207274564, 5.783357778048668685 ) ) ;
#3022=EDGE_CURVE ( 'NONE', #16104, #4963, #12392, .T. ) ;
#3024=CARTESIAN_POINT ( 'NONE',  ( 0.000000000000000000, 0.000000000000000000, 8.700000000000001066 ) ) ;
#3025=CARTESIAN_POINT ( 'NONE',  ( -25.74999999999999289, -16.21813761408365195, 13.00000000000000178 ) ) ;
#3029=ORIENTED_EDGE ( 'NONE', *, *, #13098, .T. ) ;
#3030=CARTESIAN_POINT ( 'NONE',  ( 33.30246708102489350, -5.905470865888903020, 6.861505862736158257 ) ) ;
#3032=CARTESIAN_POINT ( 'NONE',  ( 26.39370705969127684, -2.976016814310973313, 4.705209693361168455 ) ) ;
#3033=CARTESIAN_POINT ( 'NONE',  ( -28.92121476417970882, -18.25996810291579209, 13.46562832783231478 ) ) ;
#3034=CARTESIAN_POINT ( 'NONE',  ( 29.97449477918272009, -6.943593201308171814, 6.453230759126468818 ) ) ;
#3035=VERTEX_POINT ( 'NONE', #982 ) ;
#3038=CARTESIAN_POINT ( 'NONE',  ( 33.78529456515154550, -6.484467084455913799, 5.783357778048664244 ) ) ;
#3049=DIRECTION ( 'NONE',  ( 0.000000000000000000, 0.000000000000000000, -1.000000000000000000 ) ) ;
#3051=CARTESIAN_POINT ( 'NONE',  ( 30.78487334700428590, -1.819997462563214263, 5.783357778048668685 ) ) ;
#3055=CARTESIAN_POINT ( 'NONE',  ( 28.34209327568754233, -5.876127416962207306, 3.627061608673662896 ) ) ;
#3058=ORIENTED_EDGE ( 'NONE', *, *, #17306, .T. ) ;
#3059=CARTESIAN_POINT ( 'NONE',  ( 30.57046727500519978, -4.353711291323232757, 3.283357778048664244 ) ) ;
#3069=CARTESIAN_POINT ( 'NONE',  ( 45.00000000000000711, -19.03270077640483038, 5.537981825772250843 ) ) ;
#3071=ORIENTED_EDGE ( 'NONE', *, *, #2857, .F. ) ;
#3075=ORIENTED_EDGE ( 'NONE', *, *, #11293, .F. ) ;
#3077=ORIENTED_EDGE ( 'NONE', *, *, #14387, .T. ) ;
#3078=CARTESIAN_POINT ( 'NONE',  ( 26.86653773853314320, -2.919050055179571945, 4.705209693361167567 ) ) ;
#3081=DIRECTION ( 'NONE',  ( 0.000000000000000000, 0.000000000000000000, -1.000000000000000000 ) ) ;
#3082=CARTESIAN_POINT ( 'NONE',  ( -7.499998387031003411, -20.49508120620799900, 13.00000000000000178 ) ) ;
#3083=DIRECTION ( 'NONE',  ( -0.1196152422706610735, 0.9928203230275511881, 0.000000000000000000 ) ) ;
#3092=FACE_OUTER_BOUND ( 'NONE', #7807, .T. ) ;
#3094=ORIENTED_EDGE ( 'NONE', *, *, #738, .T. ) ;
#3097=CARTESIAN_POINT ( 'NONE',  ( 28.91555989733679866, -4.553094948490599592, 8.283357778048662468 ) ) ;
#3098=FACE_OUTER_BOUND ( 'NONE', #9375, .T. ) ;
#3100=CARTESIAN_POINT ( 'NONE',  ( 26.86291784143654127, -6.981118157082444320, 4.533357778048659803 ) ) ;
#3105=LINE ( 'NONE', #11229, #6131 ) ;
#3109=DIRECTION ( 'NONE',  ( -0.000000000000000000, -0.000000000000000000, 1.000000000000000000 ) ) ;
#3110=EDGE_LOOP ( 'NONE', ( #8128, #11092, #9634 ) ) ;
#3113=CARTESIAN_POINT ( 'NONE',  ( 25.47811240618384687, -2.786519109605914757, 7.033357778048666020 ) ) ;
#3114=EDGE_CURVE ( 'NONE', #602, #2265, #12023, .T. ) ;
#3115=AXIS2_PLACEMENT_3D ( 'NONE', #11067, #4205, #14268 ) ;
#3116=CARTESIAN_POINT ( 'NONE',  ( 28.28955653359400557, -5.882457056865704637, 7.939653947423658487 ) ) ;
#3117=CARTESIAN_POINT ( 'NONE',  ( -16.91320375285265953, -17.65223671300078223, 16.01217750721622579 ) ) ;
#3118=CYLINDRICAL_SURFACE ( 'NONE', #12137, 5.000000000000001776 ) ;
#3119=ORIENTED_EDGE ( 'NONE', *, *, #7617, .T. ) ;
#3128=CARTESIAN_POINT ( 'NONE',  ( 26.01652455409633902, -4.902371455920926380, 5.783357778048663356 ) ) ;
#3132=CIRCLE ( 'NONE', #6317, 2.749999999999988454 ) ;
#3136=CARTESIAN_POINT ( 'NONE',  ( 30.82871344409320713, -3.068656662272551738, 3.627061608673666893 ) ) ;
#3137=EDGE_CURVE ( 'NONE', #3302, #6631, #2380, .T. ) ;
#3139=CARTESIAN_POINT ( 'NONE',  ( 26.24651417059167002, -6.811311830135040601, 7.170103614070669096 ) ) ;
#3141=CARTESIAN_POINT ( 'NONE',  ( 30.25533603959949502, -6.272589980291270351, 4.705209693361160461 ) ) ;
#3143=CARTESIAN_POINT ( 'NONE',  ( 15.92260893619738837, -28.39189527176317540, 0.000000000000000000 ) ) ;
#3144=ORIENTED_EDGE ( 'NONE', *, *, #10769, .F. ) ;
#3145=CARTESIAN_POINT ( 'NONE',  ( 27.67650891848073158, -3.448435056481901295, 3.627061608673666449 ) ) ;
#3147=CARTESIAN_POINT ( 'NONE',  ( 27.53837573810955419, -6.172832027328289506, 3.283357778048663356 ) ) ;
#3149=CARTESIAN_POINT ( 'NONE',  ( -35.77680296528374271, -19.03270077640483038, 0.5379818257722512875 ) ) ;
#3156=CARTESIAN_POINT ( 'NONE',  ( -37.55714628004649569, -12.56174331051002113, 5.783357778048663356 ) ) ;
#3161=CARTESIAN_POINT ( 'NONE',  ( 28.13194630731337753, -5.901445976576172647, 7.939653947423658487 ) ) ;
#3162=DIRECTION ( 'NONE',  ( 0.1113444980252557837, -0.9937818688019538493, 0.000000000000000000 ) ) ;
#3172=FACE_OUTER_BOUND ( 'NONE', #10594, .T. ) ;
#3180=CARTESIAN_POINT ( 'NONE',  ( 29.35089333861488115, -5.954459450865362768, 3.283357778048663800 ) ) ;
#3185=ORIENTED_EDGE ( 'NONE', *, *, #4228, .F. ) ;
#3186=CARTESIAN_POINT ( 'NONE',  ( 26.31556265977298992, -7.384422263489805793, 5.783357778048663356 ) ) ;
#3191=CIRCLE ( 'NONE', #1754, 5.000000000000000000 ) ;
#3192=EDGE_CURVE ( 'NONE', #14557, #9400, #4492, .T. ) ;
#3202=CARTESIAN_POINT ( 'NONE',  ( 26.06734695949040059, -6.350061944625998933, 8.283357778048658915 ) ) ;
#3206=CARTESIAN_POINT ( 'NONE',  ( 31.34233605952372415, -6.778795339760710803, 5.783357778048664244 ) ) ;
#3207=CARTESIAN_POINT ( 'NONE',  ( -28.29220412912503946, -19.54937045720491184, 13.63977809545137454 ) ) ;
#3208=LINE ( 'NONE', #6002, #13005 ) ;
#3211=CARTESIAN_POINT ( 'NONE',  ( -5.237433445017501299, -16.51494876461869765, 16.99438405180048761 ) ) ;
#3214=LINE ( 'NONE', #16670, #6412 ) ;
#3215=EDGE_LOOP ( 'NONE', ( #9786, #351 ) ) ;
#3226=CARTESIAN_POINT ( 'NONE',  ( 28.51709679197739078, -3.347160818026084339, 7.939653947423664704 ) ) ;
#3230=VERTEX_POINT ( 'NONE', #15279 ) ;
#3232=CARTESIAN_POINT ( 'NONE',  ( 25.97837335112617652, -4.585712065882579402, 7.940391451607452744 ) ) ;
#3234=CARTESIAN_POINT ( 'NONE',  ( 32.28234893270314387, -5.401404424200516807, 3.627061608673662896 ) ) ;
#3235=CARTESIAN_POINT ( 'NONE',  ( 26.01652455409633902, -4.902371455920926380, 5.783357778048663356 ) ) ;
#3237=EDGE_LOOP ( 'NONE', ( #17265, #5595, #321, #9664 ) ) ;
#3238=AXIS2_PLACEMENT_3D ( 'NONE', #17315, #6409, #9130 ) ;
#3250=ORIENTED_EDGE ( 'NONE', *, *, #1159, .F. ) ;
#3252=CARTESIAN_POINT ( 'NONE',  ( 32.97211790677835097, -2.610546234160043610, 3.283357778048666464 ) ) ;
#3254=EDGE_CURVE ( 'NONE', #8113, #2945, #9214, .T. ) ;
#3258=CARTESIAN_POINT ( 'NONE',  ( 28.38593337277646711, -7.124786616671554107, 5.783357778048658915 ) ) ;
#3260=CARTESIAN_POINT ( 'NONE',  ( 33.32855701603872234, -2.140504347050403045, 4.705209693361168455 ) ) ;
#3262=LINE ( 'NONE', #15682, #1156 ) ;
#3263=CIRCLE ( 'NONE', #13399, 2.000000000000001776 ) ;
#3268=CIRCLE ( 'NONE', #17489, 1.000000000000000000 ) ;
#3274=VERTEX_POINT ( 'NONE', #4227 ) ;
#3281=CARTESIAN_POINT ( 'NONE',  ( 29.70732014299206369, -2.276983097582480742, 4.533357778048667797 ) ) ;
#3282=CYLINDRICAL_SURFACE ( 'NONE', #17636, 2.500000000000001776 ) ;
#3283=AXIS2_PLACEMENT_3D ( 'NONE', #5830, #4482, #14012 ) ;
#3288=VECTOR ( 'NONE', #15873, 1000.000000000000227 ) ;
#3301=CARTESIAN_POINT ( 'NONE',  ( 26.31128205117621022, -7.047579375861630524, 4.533357778048659803 ) ) ;
#3302=VERTEX_POINT ( 'NONE', #12563 ) ;
#3304=DIRECTION ( 'NONE',  ( 1.000000000000000000, 0.000000000000000000, 0.000000000000000000 ) ) ;
#3316=FACE_OUTER_BOUND ( 'NONE', #5844, .T. ) ;
#3320=CARTESIAN_POINT ( 'NONE',  ( 33.73390066541284682, -2.518766455766909385, 8.283357778048664244 ) ) ;
#3322=EDGE_CURVE ( 'NONE', #9702, #14428, #1965, .T. ) ;
#3323=( BOUNDED_CURVE ( )  B_SPLINE_CURVE ( 2, ( #16602, #8252, #1193, #13785, #6888, #15147, #9340, #8333, #16428 ),
 .UNSPECIFIED., .F., .T. ) 
 B_SPLINE_CURVE_WITH_KNOTS ( ( 3, 2, 2, 2, 3 ),
 ( 0.09615384615384617306, 0.1025641025641025605, 0.1153846153846153910, 0.1282051282051281937, 0.1346153846153846367 ),
 .UNSPECIFIED. ) 
 CURVE ( )  GEOMETRIC_REPRESENTATION_ITEM ( )  RATIONAL_B_SPLINE_CURVE ( ( 0.9330127018922194093, 0.9330127018922196314, 1.000000000000000000, 0.8660254037844387076, 1.000000000000000000, 0.8660254037844387076, 1.000000000000000000, 0.9330127018922190762, 0.9330127018922194093 ) ) 
 REPRESENTATION_ITEM ( '' )  );
#3327=CARTESIAN_POINT ( 'NONE',  ( 32.04575515724926760, -1.668086104879473730, 5.783357778048668685 ) ) ;
#3332=CARTESIAN_POINT ( 'NONE',  ( 27.41826274939272423, -4.733489685532582314, 3.283357778048664244 ) ) ;
#3336=CARTESIAN_POINT ( 'NONE',  ( 28.40369292566375492, -19.36532336263649512, 13.60921607110385523 ) ) ;
#3337=CARTESIAN_POINT ( 'NONE',  ( 45.00000000000000711, 0.000000000000000000, 5.537981825772250843 ) ) ;
#3341=CARTESIAN_POINT ( 'NONE',  ( 30.57046727500519978, -4.353711291323232757, 3.283357778048664244 ) ) ;
#3343=ORIENTED_EDGE ( 'NONE', *, *, #3467, .T. ) ;
#3347=DIRECTION ( 'NONE',  ( -1.000000000000000000, 0.000000000000000000, 0.000000000000000000 ) ) ;
#3350=PLANE ( 'NONE',  #5811 ) ;
#3353=CARTESIAN_POINT ( 'NONE',  ( -21.42601376483257880, 2.765314980223223529, 6.000000000000000000 ) ) ;
#3365=CARTESIAN_POINT ( 'NONE',  ( 27.65467808709180630, -4.705006306174339237, 8.283357778048662468 ) ) ;
#3376=DIRECTION ( 'NONE',  ( 0.9928203230275510771, 0.1196152422706609902, 4.006172263299092517E-17 ) ) ;
#3378=DIRECTION ( 'NONE',  ( -0.000000000000000000, -0.000000000000000000, 1.000000000000000000 ) ) ;
#3383=CARTESIAN_POINT ( 'NONE',  ( 31.53813789838894621, -6.745008222462202774, 5.783357778048658027 ) ) ;
#3384=EDGE_CURVE ( 'NONE', #7756, #13000, #10448, .T. ) ;
#3390=ORIENTED_EDGE ( 'NONE', *, *, #2959, .F. ) ;
#3391=CARTESIAN_POINT ( 'NONE',  ( 26.24567459566274508, -6.804343261277824517, 4.147687604665191152 ) ) ;
#3392=CARTESIAN_POINT ( 'NONE',  ( -27.17934203385504333, -30.00000000000000355, 12.00000000000000000 ) ) ;
#3394=CARTESIAN_POINT ( 'NONE',  ( 20.00000000000000000, 7.999999999999996447, 15.51150668642334374 ) ) ;
#3398=CARTESIAN_POINT ( 'NONE',  ( -27.17934203385504333, -30.00000000000000355, 13.93658524716016878 ) ) ;
#3399=CARTESIAN_POINT ( 'NONE',  ( 26.31176419598820360, -7.352894575460818594, 5.384699358761103838 ) ) ;
#3403=CARTESIAN_POINT ( 'NONE',  ( 26.52522735095806894, -6.721994413439005278, 6.861505862736157368 ) ) ;
#3408=ORIENTED_EDGE ( 'NONE', *, *, #8081, .T. ) ;
#3409=CARTESIAN_POINT ( 'NONE',  ( 32.70264286945147347, -5.350767304972614546, 7.939653947423658487 ) ) ;
#3412=CARTESIAN_POINT ( 'NONE',  ( 45.00000000000000711, -16.03270077640482683, 0.5379818257722508434 ) ) ;
#3415=EDGE_CURVE ( 'NONE', #1004, #6730, #14163, .T. ) ;
#3418=( BOUNDED_CURVE ( )  B_SPLINE_CURVE ( 2, ( #16214, #9043, #790, #9135, #881, #2429, #7771, #17418, #4772 ),
 .UNSPECIFIED., .F., .T. ) 
 B_SPLINE_CURVE_WITH_KNOTS ( ( 3, 2, 2, 2, 3 ),
 ( 0.2500000000000000000, 0.2564102564102563875, 0.2692307692307692180, 0.2820512820512820484, 0.2884615384615384914 ),
 .UNSPECIFIED. ) 
 CURVE ( )  GEOMETRIC_REPRESENTATION_ITEM ( )  RATIONAL_B_SPLINE_CURVE ( ( 0.9330127018922194093, 0.9330127018922195203, 1.000000000000000000, 0.8660254037844387076, 1.000000000000000000, 0.8660254037844387076, 1.000000000000000000, 0.9330127018922190762, 0.9330127018922194093 ) ) 
 REPRESENTATION_ITEM ( '' )  );
#3420=MECHANICAL_DESIGN_GEOMETRIC_PRESENTATION_REPRESENTATION('',(#8047),#235);
#3421=CARTESIAN_POINT ( 'NONE',  ( 26.01652455409633902, -4.902371455920926380, 5.783357778048663356 ) ) ;
#3426=VECTOR ( 'NONE', #5263, 1000.000000000000000 ) ;
#3427=CARTESIAN_POINT ( 'NONE',  ( 31.71123609653335507, -2.762457591843783256, 3.283357778048666464 ) ) ;
#3429=ORIENTED_EDGE ( 'NONE', *, *, #14396, .F. ) ;
#3431=EDGE_CURVE ( 'NONE', #4898, #9735, #7354, .T. ) ;
#3432=VERTEX_POINT ( 'NONE', #1229 ) ;
#3435=CARTESIAN_POINT ( 'NONE',  ( 33.13163345120441505, -4.045141346131868154, 7.939653947423662039 ) ) ;
#3438=FACE_OUTER_BOUND ( 'NONE', #1317, .T. ) ;
#3455=CARTESIAN_POINT ( 'NONE',  ( 29.04309111455793513, -1.630102785574754742, 5.783357778048668685 ) ) ;
#3458=CARTESIAN_POINT ( 'NONE',  ( 26.15738093914773543, -4.885401043216321959, 3.283357778048664244 ) ) ;
#3467=EDGE_CURVE ( 'NONE', #3702, #8474, #407, .T. ) ;
#3470=LINE ( 'NONE', #13173, #10402 ) ;
#3474=DIRECTION ( 'NONE',  ( 0.000000000000000000, 0.000000000000000000, -1.000000000000000000 ) ) ;
#3475=EDGE_CURVE ( 'NONE', #16224, #63, #8851, .T. ) ;
#3480=EDGE_LOOP ( 'NONE', ( #7545, #2766, #493, #13060 ) ) ;
#3485=DIRECTION ( 'NONE',  ( 1.000000000000000000, 0.000000000000000000, 0.000000000000000000 ) ) ;
#3486=EDGE_CURVE ( 'NONE', #9702, #17832, #15294, .T. ) ;
#3494=DIRECTION ( 'NONE',  ( 0.000000000000000000, 0.000000000000000000, 1.000000000000000000 ) ) ;
#3496=CARTESIAN_POINT ( 'NONE',  ( 28.41655006632555569, -6.494127376913395366, 6.861505862736157368 ) ) ;
#3500=ORIENTED_EDGE ( 'NONE', *, *, #17256, .F. ) ;
#3501=CARTESIAN_POINT ( 'NONE',  ( 25.60565592828815440, -3.070961412863312034, 4.705209693361167567 ) ) ;
#3507=CARTESIAN_POINT ( 'NONE',  ( 30.64556327217151122, -6.525384084031224496, 4.533357778048659803 ) ) ;
#3508=PLANE ( 'NONE',  #8769 ) ;
#3510=AXIS2_PLACEMENT_3D ( 'NONE', #13787, #14141, #7176 ) ;
#3515=EDGE_CURVE ( 'NONE', #15247, #11836, #1045, .T. ) ;
#3517=CARTESIAN_POINT ( 'NONE',  ( 31.24973580796908834, -6.452593224933654170, 7.033357778048657138 ) ) ;
#3518=ORIENTED_EDGE ( 'NONE', *, *, #9994, .F. ) ;
#3522=VERTEX_POINT ( 'NONE', #2577 ) ;
#3524=CARTESIAN_POINT ( 'NONE',  ( 32.17274868998081416, -2.279756424927169345, 6.861505862736166250 ) ) ;
#3533=CARTESIAN_POINT ( 'NONE',  ( 15.92260893619738837, -28.39189527176317540, 12.00000000000000000 ) ) ;
#3535=CARTESIAN_POINT ( 'NONE',  ( 14.05146698326616672, 13.69412420653798357, 16.38624388364804219 ) ) ;
#3537=CARTESIAN_POINT ( 'NONE',  ( 35.77680296528374271, -19.03270077640483038, 0.5379818257722512875 ) ) ;
#3538=VECTOR ( 'NONE', #15938, 1000.000000000000000 ) ;
#3541=EDGE_LOOP ( 'NONE', ( #17775, #2844, #8174, #16645 ) ) ;
#3545=ORIENTED_EDGE ( 'NONE', *, *, #7913, .F. ) ;
#3552=ORIENTED_EDGE ( 'NONE', *, *, #14065, .T. ) ;
#3564=EDGE_CURVE ( 'NONE', #11059, #15493, #9709, .T. ) ;
#3565=VECTOR ( 'NONE', #13907, 1000.000000000000227 ) ;
#3571=ORIENTED_EDGE ( 'NONE', *, *, #9985, .T. ) ;
#3575=AXIS2_PLACEMENT_3D ( 'NONE', #5095, #17575, #9272 ) ;
#3587=EDGE_CURVE ( 'NONE', #11980, #9649, #11015, .T. ) ;
#3591=LINE ( 'NONE', #593, #14463 ) ;
#3592=FACE_OUTER_BOUND ( 'NONE', #10283, .T. ) ;
#3594=VECTOR ( 'NONE', #2654, 1000.000000000000000 ) ;
#3596=CARTESIAN_POINT ( 'NONE',  ( 33.53059316159333036, -1.478995586096186088, 6.453230759126471483 ) ) ;
#3598=CARTESIAN_POINT ( 'NONE',  ( 26.39823381822651882, -6.110324093391315436, 7.939653947423658487 ) ) ;
#3599=ORIENTED_EDGE ( 'NONE', *, *, #10221, .T. ) ;
#3601=ORIENTED_EDGE ( 'NONE', *, *, #4512, .T. ) ;
#3602=CARTESIAN_POINT ( 'NONE',  ( 26.21417678486618641, -2.370676134166772808, 5.783357778048668685 ) ) ;
#3603=CARTESIAN_POINT ( 'NONE',  ( -29.25000000000000000, -16.21813761408365195, 13.37255996287876947 ) ) ;
#3605=EDGE_CURVE ( 'NONE', #17262, #225, #7021, .T. ) ;
#3607=CARTESIAN_POINT ( 'NONE',  ( 33.83947189604607786, -2.952629194728097595, 5.783357778048663356 ) ) ;
#3608=DIRECTION ( 'NONE',  ( -0.1196152422706621005, -0.9928203230275509661, -0.000000000000000000 ) ) ;
#3612=DIRECTION ( 'NONE',  ( 1.000000000000000000, 0.000000000000000000, 0.000000000000000000 ) ) ;
#3618=DIRECTION ( 'NONE',  ( 0.1196152422706618645, -0.9928203230275510771, 0.000000000000000000 ) ) ;
#3619=CARTESIAN_POINT ( 'NONE',  ( 31.15208055228630357, -2.102918000029084578, 7.033357778048666020 ) ) ;
#3620=ORIENTED_EDGE ( 'NONE', *, *, #3254, .F. ) ;
#3624=CARTESIAN_POINT ( 'NONE',  ( 32.30426898124760982, -6.025734024055190652, 4.705209693361159573 ) ) ;
#3632=CARTESIAN_POINT ( 'NONE',  ( -15.92260893619738837, -28.39189527176317540, 6.000000000000000000 ) ) ;
#3634=FACE_BOUND ( 'NONE', #12027, .T. ) ;
#3637=ORIENTED_EDGE ( 'NONE', *, *, #17620, .T. ) ;
#3642=CARTESIAN_POINT ( 'NONE',  ( 26.39379627684682106, -4.856917663858078882, 8.283357778048662468 ) ) ;
#3653=EDGE_CURVE ( 'NONE', #3230, #10383, #8916, .T. ) ;
#3655=CARTESIAN_POINT ( 'NONE',  ( -23.02601376483258022, 3.965314980223224151, 6.000000000000000000 ) ) ;
#3661=ORIENTED_EDGE ( 'NONE', *, *, #5483, .T. ) ;
#3662=CARTESIAN_POINT ( 'NONE',  ( 26.16909369068367752, -6.168712907020688974, 3.640912447338509939 ) ) ;
#3669=CARTESIAN_POINT ( 'NONE',  ( -35.19141017012124451, -14.17387298022714148, 11.46934516270795079 ) ) ;
#3675=CARTESIAN_POINT ( 'NONE',  ( 25.76326615456878244, -3.051972493152843580, 4.705209693361168455 ) ) ;
#3677=VERTEX_POINT ( 'NONE', #2132 ) ;
#3678=CARTESIAN_POINT ( 'NONE',  ( 31.67382807612511542, -6.101689702897060030, 4.705209693361159573 ) ) ;
#3679=CARTESIAN_POINT ( 'NONE',  ( 27.30498922523054617, -2.229057914452205136, 6.453230759126474148 ) ) ;
#3681=EDGE_CURVE ( 'NONE', #12087, #4193, #15900, .T. ) ;
#3682=ORIENTED_EDGE ( 'NONE', *, *, #9212, .T. ) ;
#3683=DIRECTION ( 'NONE',  ( 0.000000000000000000, 0.000000000000000000, -1.000000000000000000 ) ) ;
#3687=AXIS2_PLACEMENT_3D ( 'NONE', #12340, #16610, #284 ) ;
#3688=CARTESIAN_POINT ( 'NONE',  ( 32.04158527077989760, -6.057382223572642665, 6.861505862736158257 ) ) ;
#3690=CARTESIAN_POINT ( 'NONE',  ( 29.79859849048667897, -1.928627242885762705, 5.783357778048662468 ) ) ;
#3694=CARTESIAN_POINT ( 'NONE',  ( -8.968477750016525363, -19.11972035685536042, 16.82776078363834671 ) ) ;
#3695=CARTESIAN_POINT ( 'NONE',  ( 27.90727577511918867, -2.156494279411373061, 5.783357778048657138 ) ) ;
#3696=CARTESIAN_POINT ( 'NONE',  ( 28.79925754835455010, -6.020920669644549861, 3.283357778048663800 ) ) ;
#3700=CARTESIAN_POINT ( 'NONE',  ( 32.51858583609114106, -1.611119345748072362, 5.783357778048668685 ) ) ;
#3701=CARTESIAN_POINT ( 'NONE',  ( 28.49970350196817392, -5.857138497251737519, 3.627061608673662896 ) ) ;
#3702=VERTEX_POINT ( 'NONE', #7558 ) ;
#3718=ORIENTED_EDGE ( 'NONE', *, *, #7188, .F. ) ;
#3719=CARTESIAN_POINT ( 'NONE',  ( 31.88017671309158274, -6.376637546091784792, 7.033357778048657138 ) ) ;
#3721=CARTESIAN_POINT ( 'NONE',  ( 26.30185955129047315, -7.986322017489088765, 4.917936583846921117 ) ) ;
#3735=DIRECTION ( 'NONE',  ( 0.5661261679878573094, 0.8243186046180107640, 0.000000000000000000 ) ) ;
#3741=AXIS2_PLACEMENT_3D ( 'NONE', #845, #6284, #14960 ) ;
#3743=EDGE_CURVE ( 'NONE', #15480, #60, #7653, .T. ) ;
#3747=DIRECTION ( 'NONE',  ( 0.000000000000000000, 0.000000000000000000, -1.000000000000000000 ) ) ;
#3755=AXIS2_PLACEMENT_3D ( 'NONE', #10039, #370, #1912 ) ;
#3760=FACE_OUTER_BOUND ( 'NONE', #9580, .T. ) ;
#3761=DIRECTION ( 'NONE',  ( 0.000000000000000000, 0.000000000000000000, 1.000000000000000000 ) ) ;
#3766=CARTESIAN_POINT ( 'NONE',  ( 30.96820195323705605, -2.125071739898741097, 4.533357778048667797 ) ) ;
#3768=EDGE_LOOP ( 'NONE', ( #387, #8537 ) ) ;
#3770=CARTESIAN_POINT ( 'NONE',  ( 30.81132015408399027, -5.578634341498224458, 7.939653947423658487 ) ) ;
#3771=CARTESIAN_POINT ( 'NONE',  ( -25.01528890617809253, -10.29849948291661121, 14.47305271942837557 ) ) ;
#3772=DIRECTION ( 'NONE',  ( -1.000000000000000000, 0.000000000000000000, 0.000000000000000000 ) ) ;
#3776=EDGE_CURVE ( 'NONE', #16386, #15079, #7466, .T. ) ;
#3781=CARTESIAN_POINT ( 'NONE',  ( 27.62849893492243325, -6.589071975465733644, 6.861505862736158257 ) ) ;
#3783=EDGE_CURVE ( 'NONE', #13090, #3230, #13534, .T. ) ;
#3788=CARTESIAN_POINT ( 'NONE',  ( 28.63031693179632242, -2.406740715396564756, 7.033357778048666020 ) ) ;
#3795=CARTESIAN_POINT ( 'NONE',  ( 32.75517961154501023, -5.344437665069116328, 3.627061608673662896 ) ) ;
#3797=CARTESIAN_POINT ( 'NONE',  ( 31.44176105920648112, -5.502678662656354192, 7.939653947423658487 ) ) ;
#3799=CARTESIAN_POINT ( 'NONE',  ( 30.68374079916737429, -6.858143062403621926, 6.453230759126467042 ) ) ;
#3800=CIRCLE ( 'NONE', #3510, 6.249999999999998224 ) ;
#3801=CYLINDRICAL_SURFACE ( 'NONE', #13881, 13.00000000000000178 ) ;
#3807=VERTEX_POINT ( 'NONE', #7734 ) ;
#3812=CARTESIAN_POINT ( 'NONE',  ( -45.50000000000000000, -19.03270077640483038, 2.787981825772258837 ) ) ;
#3813=AXIS2_PLACEMENT_3D ( 'NONE', #3959, #6770, #59 ) ;
#3815=DIRECTION ( 'NONE',  ( -1.000000000000000000, 0.000000000000000000, 0.000000000000000000 ) ) ;
#3817=CARTESIAN_POINT ( 'NONE',  ( 31.08763465596552322, -1.773323841400983758, 6.453230759126472371 ) ) ;
#3820=CARTESIAN_POINT ( 'NONE',  ( 32.97402322492378346, -4.064130265842336165, 7.939653947423662039 ) ) ;
#3827=ADVANCED_FACE ( 'NONE', ( #3098 ), #3282, .F. ) ;
#3828=CARTESIAN_POINT ( 'NONE',  ( 25.87953856062030766, -3.765371892057810754, 7.615734152686682634 ) ) ;
#3842=CARTESIAN_POINT ( 'NONE',  ( -8.632250723006720250, -18.84644399697197770, 13.00000000000000178 ) ) ;
#3850=PLANE ( 'NONE',  #12213 ) ;
#3856=CARTESIAN_POINT ( 'NONE',  ( 35.74085044863416982, -23.57886868891565513, 11.27079897466147251 ) ) ;
#3858=CARTESIAN_POINT ( 'NONE',  ( 32.43181250335191379, -6.310176327312596811, 7.033357778048657138 ) ) ;
#3861=CARTESIAN_POINT ( 'NONE',  ( 29.52399153675929355, -1.971908820246954130, 5.783357778048668685 ) ) ;
#3863=CARTESIAN_POINT ( 'NONE',  ( 28.45891156537951971, -2.090033060632186412, 5.783357778048657138 ) ) ;
#3867=ORIENTED_EDGE ( 'NONE', *, *, #13954, .F. ) ;
#3868=CARTESIAN_POINT ( 'NONE',  ( -3.538288549924106796, -15.34800872113743431, 13.00000000000000178 ) ) ;
#3870=CARTESIAN_POINT ( 'NONE',  ( 23.00000000000000000, -16.21813761408365195, 13.00000000000000178 ) ) ;
#3874=CARTESIAN_POINT ( 'NONE',  ( 25.62757597683262034, -3.695291012717980994, 3.627061608673666893 ) ) ;
#3878=CARTESIAN_POINT ( 'NONE',  ( 32.81641299864316608, -4.083119185552795294, 3.627061608673664228 ) ) ;
#3879=CARTESIAN_POINT ( 'NONE',  ( 27.10304229683147526, -4.771467524953526329, 8.283357778048662468 ) ) ;
#3880=ORIENTED_EDGE ( 'NONE', *, *, #1366, .F. ) ;
#3881=ORIENTED_EDGE ( 'NONE', *, *, #431, .F. ) ;
#3882=ORIENTED_EDGE ( 'NONE', *, *, #17864, .F. ) ;
#3883=CARTESIAN_POINT ( 'NONE',  ( 30.45225960443380231, -4.367952981209816343, 7.939653947423662039 ) ) ;
#3885=CARTESIAN_POINT ( 'NONE',  ( 31.03886041246737548, -3.043338102658604161, 7.939653947423662927 ) ) ;
#3886=DIRECTION ( 'NONE',  ( -0.1196152422706614343, 0.9928203230275510771, 0.000000000000000000 ) ) ;
#3900=( BOUNDED_CURVE ( )  B_SPLINE_CURVE ( 2, ( #11738, #10470, #16032, #14483, #16119, #10287, #966, #3679, #9125 ),
 .UNSPECIFIED., .F., .T. ) 
 B_SPLINE_CURVE_WITH_KNOTS ( ( 3, 2, 2, 2, 3 ),
 ( 0.6730769230769231282, 0.6794871794871795156, 0.6923076923076922906, 0.7051282051282051766, 0.7115384615384615641 ),
 .UNSPECIFIED. ) 
 CURVE ( )  GEOMETRIC_REPRESENTATION_ITEM ( )  RATIONAL_B_SPLINE_CURVE ( ( 0.9330127018922192983, 0.9330127018922198534, 1.000000000000000000, 0.8660254037844387076, 1.000000000000000000, 0.8660254037844387076, 1.000000000000000000, 0.9330127018922194093, 0.9330127018922194093 ) ) 
 REPRESENTATION_ITEM ( '' )  );
#3902=EDGE_CURVE ( 'NONE', #8657, #12849, #5103, .T. ) ;
#3903=CARTESIAN_POINT ( 'NONE',  ( 26.86291784143654127, -6.981118157082444320, 4.533357778048659803 ) ) ;
#3907=CARTESIAN_POINT ( 'NONE',  ( 31.88814493096864311, -1.687075024589942407, 5.783357778048668685 ) ) ;
#3909=LINE ( 'NONE', #6883, #17696 ) ;
#3913=CARTESIAN_POINT ( 'NONE',  ( 25.76466184735054910, -2.811881907026620553, 5.318565573966401061 ) ) ;
#3914=DIRECTION ( 'NONE',  ( -0.000000000000000000, -0.000000000000000000, 1.000000000000000000 ) ) ;
#3922=ADVANCED_FACE ( 'NONE', ( #3592 ), #9282, .F. ) ;
#3925=ORIENTED_EDGE ( 'NONE', *, *, #13098, .F. ) ;
#3926=CARTESIAN_POINT ( 'NONE',  ( -15.92260893619738837, -28.39189527176317540, 16.15082599432113142 ) ) ;
#3935=DIRECTION ( 'NONE',  ( -1.000000000000000000, 0.000000000000000000, 0.000000000000000000 ) ) ;
#3940=CARTESIAN_POINT ( 'NONE',  ( 33.16732689266149237, -6.221561368663743430, 4.533357778048659803 ) ) ;
#3941=ORIENTED_EDGE ( 'NONE', *, *, #11895, .T. ) ;
#3943=CARTESIAN_POINT ( 'NONE',  ( 29.13014440709066832, -5.781182818409868140, 3.627061608673662896 ) ) ;
#3947=CARTESIAN_POINT ( 'NONE',  ( 8.968924017731504605, -19.12031538047531853, 16.82773324567541451 ) ) ;
#3948=VERTEX_POINT ( 'NONE', #17668 ) ;
#3954=CARTESIAN_POINT ( 'NONE',  ( 33.00219691583784964, -5.514549477365426888, 8.283357778048660691 ) ) ;
#3956=CARTESIAN_POINT ( 'NONE',  ( 30.67110321781257909, -3.087645581983020637, 3.627061608673666893 ) ) ;
#3959=CARTESIAN_POINT ( 'NONE',  ( -45.00000000000000711, -19.03270077640483038, 5.537981825772250843 ) ) ;
#3960=ORIENTED_EDGE ( 'NONE', *, *, #16801, .T. ) ;
#3961=CARTESIAN_POINT ( 'NONE',  ( 29.12189622942009493, -1.620608325512071568, 5.783357778048668685 ) ) ;
#3962=EDGE_CURVE ( 'NONE', #8890, #7124, #13810, .T. ) ;
#3965=ORIENTED_EDGE ( 'NONE', *, *, #4119, .T. ) ;
#3966=CARTESIAN_POINT ( 'NONE',  ( 30.01874226414561875, -2.539271660970221944, 4.705209693361167567 ) ) ;
#3969=CARTESIAN_POINT ( 'NONE',  ( 28.91547068018125799, -2.672194098943493135, 4.705209693361168455 ) ) ;
#3983=CARTESIAN_POINT ( 'NONE',  ( 31.94462260941237020, -6.706231704719880504, 6.453230759126467042 ) ) ;
#3985=CARTESIAN_POINT ( 'NONE',  ( 34.91600907648203389, -11.88801210197604341, 11.56671555609732671 ) ) ;
#3988=CARTESIAN_POINT ( 'NONE',  ( 32.79901970863393501, -6.593096864778464017, 5.783357778048658915 ) ) ;
#3996=ADVANCED_FACE ( 'NONE', ( #9195 ), #6391, .F. ) ;
#4000=EDGE_LOOP ( 'NONE', ( #14832, #4231, #11714, #6743 ) ) ;
#4002=VECTOR ( 'NONE', #7489, 1000.000000000000000 ) ;
#4011=ORIENTED_EDGE ( 'NONE', *, *, #7966, .F. ) ;
#4016=PLANE ( 'NONE',  #4979 ) ;
#4021=CARTESIAN_POINT ( 'NONE',  ( 31.68992120585416217, -1.700760206360153015, 5.783357778048662468 ) ) ;
#4025=VECTOR ( 'NONE', #2595, 1000.000000000000000 ) ;
#4026=CARTESIAN_POINT ( 'NONE',  ( 29.80442540930208750, -6.953886339277345563, 5.783357778048657138 ) ) ;
#4031=VECTOR ( 'NONE', #11011, 1000.000000000000227 ) ;
#4037=CARTESIAN_POINT ( 'NONE',  ( 30.00264913441657555, -6.940201157507134511, 5.783357778048669573 ) ) ;
#4039=CARTESIAN_POINT ( 'NONE',  ( 26.25801688195511474, -3.619335333876111171, 3.627061608673666893 ) ) ;
#4042=CARTESIAN_POINT ( 'NONE',  ( 27.51889869220010354, -3.467423976192371082, 3.627061608673666893 ) ) ;
#4046=CARTESIAN_POINT ( 'NONE',  ( 32.80318959510331212, -2.203800746085299522, 6.861505862736166250 ) ) ;
#4049=ORIENTED_EDGE ( 'NONE', *, *, #5721, .F. ) ;
#4051=CARTESIAN_POINT ( 'NONE',  ( 30.64918316926811315, -2.463315982128351678, 4.705209693361167567 ) ) ;
#4053=VERTEX_POINT ( 'NONE', #15175 ) ;
#4055=CARTESIAN_POINT ( 'NONE',  ( 28.39010325924584421, -2.735490497978389612, 6.861505862736166250 ) ) ;
#4058=CARTESIAN_POINT ( 'NONE',  ( 28.56587103547553852, -2.077146556768465047, 6.453230759126474148 ) ) ;
#4065=PLANE ( 'NONE',  #13294 ) ;
#4066=DIRECTION ( 'NONE',  ( -0.1196152422706584506, 0.9928203230275515212, 0.000000000000000000 ) ) ;
#4071=ORIENTED_EDGE ( 'NONE', *, *, #16962, .T. ) ;
#4075=CARTESIAN_POINT ( 'NONE',  ( 31.39792096211754924, -4.254019462947003838, 3.627061608673664228 ) ) ;
#4094=DIRECTION ( 'NONE',  ( 1.000000000000000000, 0.000000000000000000, 0.000000000000000000 ) ) ;
#4100=FACE_OUTER_BOUND ( 'NONE', #14740, .T. ) ;
#4106=( BOUNDED_CURVE ( )  B_SPLINE_CURVE ( 2, ( #14864, #2452, #13679, #1080, #6602, #17713, #2712, #5232, #1267 ),
 .UNSPECIFIED., .F., .T. ) 
 B_SPLINE_CURVE_WITH_KNOTS ( ( 3, 2, 2, 2, 3 ),
 ( 0.1730769230769231004, 0.1794871794871794879, 0.1923076923076923184, 0.2051282051282051211, 0.2115384615384615641 ),
 .UNSPECIFIED. ) 
 CURVE ( )  GEOMETRIC_REPRESENTATION_ITEM ( )  RATIONAL_B_SPLINE_CURVE ( ( 0.9330127018922194093, 0.9330127018922196314, 1.000000000000000000, 0.8660254037844387076, 1.000000000000000000, 0.8660254037844387076, 1.000000000000000000, 0.9330127018922190762, 0.9330127018922194093 ) ) 
 REPRESENTATION_ITEM ( '' )  );
#4109=DIRECTION ( 'NONE',  ( 1.000000000000000000, 0.000000000000000000, 0.000000000000000000 ) ) ;
#4113=FACE_OUTER_BOUND ( 'NONE', #6615, .T. ) ;
#4119=EDGE_CURVE ( 'NONE', #4053, #11016, #4210, .T. ) ;
#4120=VECTOR ( 'NONE', #9651, 1000.000000000000000 ) ;
#4121=CARTESIAN_POINT ( 'NONE',  ( 26.19678349485696955, -4.880653813392439311, 7.939653947423662039 ) ) ;
#4122=DIRECTION ( 'NONE',  ( -1.000000000000000000, 0.000000000000000000, 0.000000000000000000 ) ) ;
#4123=CARTESIAN_POINT ( 'NONE',  ( 28.43075721014566781, -2.093425104433228157, 5.113484796970856117 ) ) ;
#4135=DIRECTION ( 'NONE',  ( 0.000000000000000000, 0.000000000000000000, -1.000000000000000000 ) ) ;
#4136=VECTOR ( 'NONE', #6127, 1000.000000000000227 ) ;
#4140=CARTESIAN_POINT ( 'NONE',  ( 30.76748005699505129, -4.329975141788874993, 3.627061608673664228 ) ) ;
#4142=CARTESIAN_POINT ( 'NONE',  ( -14.00000000000000178, 0.000000000000000000, 8.700000000000001066 ) ) ;
#4144=CARTESIAN_POINT ( 'NONE',  ( 33.54323074294813267, -5.249493066516778050, 3.627061608673662896 ) ) ;
#4148=EDGE_LOOP ( 'NONE', ( #10683, #4253, #12480, #15877 ) ) ;
#4149=ADVANCED_FACE ( 'NONE', ( #33 ), #5542, .F. ) ;
#4151=CARTESIAN_POINT ( 'NONE',  ( 26.97161122272022382, -2.906390775372597712, 6.861505862736165362 ) ) ;
#4152=AXIS2_PLACEMENT_3D ( 'NONE', #10385, #10640, #13026 ) ;
#4155=CARTESIAN_POINT ( 'NONE',  ( 27.00222791626931240, -2.275731535614434531, 5.783357778048668685 ) ) ;
#4159=CIRCLE ( 'NONE', #6747, 2.500000000000001776 ) ;
#4166=CARTESIAN_POINT ( 'NONE',  ( 27.11150007966593733, -11.49307575575171469, 13.95470972894434780 ) ) ;
#4167=VERTEX_POINT ( 'NONE', #15721 ) ;
#4170=CARTESIAN_POINT ( 'NONE',  ( 33.18226487515251222, -2.585227674546096033, 8.283357778048664244 ) ) ;
#4172=EDGE_LOOP ( 'NONE', ( #2696, #9296, #8373, #746 ) ) ;
#4174=ORIENTED_EDGE ( 'NONE', *, *, #8934, .T. ) ;
#4175=CARTESIAN_POINT ( 'NONE',  ( 32.01513846370018967, -2.298745344637636912, 6.861505862736165362 ) ) ;
#4182=ADVANCED_FACE ( 'NONE', ( #5814, #13080, #11620 ), #7555, .T. ) ;
#4183=FACE_OUTER_BOUND ( 'NONE', #16924, .T. ) ;
#4186=DIRECTION ( 'NONE',  ( -0.9928203230275514102, -0.1196152422706598939, -0.000000000000000000 ) ) ;
#4187=PLANE ( 'NONE',  #15857 ) ;
#4193=VERTEX_POINT ( 'NONE', #12710 ) ;
#4194=CARTESIAN_POINT ( 'NONE',  ( 45.00000000000000711, -19.03270077640482683, 10.53798182577225084 ) ) ;
#4197=CARTESIAN_POINT ( 'NONE',  ( -45.50000000000000000, -19.03270077640483038, 5.537981825772250843 ) ) ;
#4201=DIRECTION ( 'NONE',  ( -0.000000000000000000, -0.000000000000000000, 1.000000000000000000 ) ) ;
#4205=DIRECTION ( 'NONE',  ( 0.9928203230275512992, 0.1196152422706610180, 4.006172263299093133E-17 ) ) ;
#4209=EDGE_CURVE ( 'NONE', #14073, #17902, #6052, .T. ) ;
#4210=( BOUNDED_CURVE ( )  B_SPLINE_CURVE ( 2, ( #15255, #210, #6914, #10974, #16628, #5719, #13996, #5455, #4021 ),
 .UNSPECIFIED., .F., .T. ) 
 B_SPLINE_CURVE_WITH_KNOTS ( ( 3, 2, 2, 2, 3 ),
 ( 0.1346153846153846367, 0.1410256410256410242, 0.1538461538461538547, 0.1666666666666666574, 0.1730769230769231004 ),
 .UNSPECIFIED. ) 
 CURVE ( )  GEOMETRIC_REPRESENTATION_ITEM ( )  RATIONAL_B_SPLINE_CURVE ( ( 0.9330127018922194093, 0.9330127018922196314, 1.000000000000000000, 0.8660254037844387076, 1.000000000000000000, 0.8660254037844387076, 1.000000000000000000, 0.9330127018922190762, 0.9330127018922194093 ) ) 
 REPRESENTATION_ITEM ( '' )  );
#4212=CARTESIAN_POINT ( 'NONE',  ( 9.099998387031005720, -19.29508120620799971, 16.81964500401478091 ) ) ;
#4213=CARTESIAN_POINT ( 'NONE',  ( 32.97211790677835097, -2.610546234160043610, 3.283357778048666464 ) ) ;
#4215=CARTESIAN_POINT ( 'NONE',  ( 28.79925754835455010, -6.020920669644549861, 3.283357778048663356 ) ) ;
#4220=ADVANCED_FACE ( 'NONE', ( #7464 ), #4732, .T. ) ;
#4221=DIRECTION ( 'NONE',  ( 0.1196152422706605323, -0.9928203230275512992, 0.000000000000000000 ) ) ;
#4224=CARTESIAN_POINT ( 'NONE',  ( 33.50243880635947846, -1.482387629897225390, 5.783357778048663356 ) ) ;
#4225=CARTESIAN_POINT ( 'NONE',  ( 28.34209327568754233, -5.876127416962207306, 3.627061608673662896 ) ) ;
#4227=CARTESIAN_POINT ( 'NONE',  ( 25.76466184735054910, -2.811881907026620553, 5.318565573966401061 ) ) ;
#4228=EDGE_CURVE ( 'NONE', #6312, #12121, #11432, .T. ) ;
#4229=VERTEX_POINT ( 'NONE', #4467 ) ;
#4231=ORIENTED_EDGE ( 'NONE', *, *, #16185, .T. ) ;
#4232=CARTESIAN_POINT ( 'NONE',  ( 28.88938074516742205, -6.437160617781993999, 6.861505862736158257 ) ) ;
#4233=CARTESIAN_POINT ( 'NONE',  ( 27.32822876973539294, -6.198150586942257512, 8.283357778048660691 ) ) ;
#4235=CARTESIAN_POINT ( 'NONE',  ( 25.76466184735054910, -2.811881907026620553, 5.318565573966400173 ) ) ;
#4237=ORIENTED_EDGE ( 'NONE', *, *, #11089, .F. ) ;
#4239=DIRECTION ( 'NONE',  ( 1.000000000000000000, 0.000000000000000000, 0.000000000000000000 ) ) ;
#4248=LINE ( 'NONE', #9748, #11358 ) ;
#4250=ORIENTED_EDGE ( 'NONE', *, *, #17816, .T. ) ;
#4253=ORIENTED_EDGE ( 'NONE', *, *, #9016, .T. ) ;
#4256=CARTESIAN_POINT ( 'NONE',  ( 29.51982165028991645, -6.361204938940122844, 6.861505862736158257 ) ) ;
#4258=CARTESIAN_POINT ( 'NONE',  ( 31.07327543742414022, -2.112412460091767308, 7.033357778048666020 ) ) ;
#4269=EDGE_LOOP ( 'NONE', ( #14110, #4481 ) ) ;
#4274=CARTESIAN_POINT ( 'NONE',  ( 31.43732351782677625, -4.249272233123119413, 8.283357778048662468 ) ) ;
#4278=DIRECTION ( 'NONE',  ( 0.9928203230275512992, 0.1196152422706610180, 4.006172263299093133E-17 ) ) ;
#4282=AXIS2_PLACEMENT_3D ( 'NONE', #15262, #16541, #9805 ) ;
#4284=CARTESIAN_POINT ( 'NONE',  ( 4.081988505578530102, 17.67880197223097127, 16.99999999999999645 ) ) ;
#4287=CARTESIAN_POINT ( 'NONE',  ( 29.84999239022537409, -5.894327871574777333, 8.283357778048660691 ) ) ;
#4292=CARTESIAN_POINT ( 'NONE',  ( 27.99987602667382802, -2.482696394238434578, 7.033357778048666020 ) ) ;
#4293=EDGE_CURVE ( 'NONE', #13470, #3035, #15571, .T. ) ;
#4294=CIRCLE ( 'NONE', #13839, 2.749999999999988454 ) ;
#4296=CARTESIAN_POINT ( 'NONE',  ( 27.75966235412334981, -2.811446176820259879, 6.861505862736166250 ) ) ;
#4298=ORIENTED_EDGE ( 'NONE', *, *, #13736, .T. ) ;
#4300=ORIENTED_EDGE ( 'NONE', *, *, #12281, .F. ) ;
#4301=CARTESIAN_POINT ( 'NONE',  ( 26.63392073224175505, -2.647267031729148012, 4.533357778048667797 ) ) ;
#4310=CARTESIAN_POINT ( 'NONE',  ( 27.93049598394382116, -4.671775696577297410, 7.939653947423662039 ) ) ;
#4314=CARTESIAN_POINT ( 'NONE',  ( 30.81132015408399027, -5.578634341498224458, 7.939653947423658487 ) ) ;
#4317=ORIENTED_EDGE ( 'NONE', *, *, #17947, .F. ) ;
#4319=CARTESIAN_POINT ( 'NONE',  ( 26.86653773853314320, -2.919050055179571945, 4.705209693361167567 ) ) ;
#4320=LINE ( 'NONE', #10106, #4956 ) ;
#4321=DIRECTION ( 'NONE',  ( 0.000000000000000000, 1.000000000000000000, 0.000000000000000000 ) ) ;
#4322=ORIENTED_EDGE ( 'NONE', *, *, #10769, .T. ) ;
#4323=CARTESIAN_POINT ( 'NONE',  ( 28.08810621022444920, -4.652786776866828511, 7.939653947423662039 ) ) ;
#4324=DIRECTION ( 'NONE',  ( 0.9928203230275512992, 0.1196152422706610180, 4.006172263299093133E-17 ) ) ;
#4325=DIRECTION ( 'NONE',  ( 1.000000000000000000, 0.000000000000000000, 0.000000000000000000 ) ) ;
#4330=EDGE_CURVE ( 'NONE', #1468, #15632, #7925, .T. ) ;
#4337=ORIENTED_EDGE ( 'NONE', *, *, #1186, .T. ) ;
#4338=AXIS2_PLACEMENT_3D ( 'NONE', #9112, #6387, #6114 ) ;
#4341=CARTESIAN_POINT ( 'NONE',  ( 28.86293393808771057, -2.678523738846987357, 6.861505862736165362 ) ) ;
#4342=CARTESIAN_POINT ( 'NONE',  ( 32.83754810739938534, -9.116730809865837060, 15.78335777804866424 ) ) ;
#4344=CIRCLE ( 'NONE', #8692, 2.000000000000001776 ) ;
#4349=CARTESIAN_POINT ( 'NONE',  ( 20.00000000000000000, 7.999999999999996447, 12.00000000000000000 ) ) ;
#4351=CARTESIAN_POINT ( 'NONE',  ( 34.43754810739937966, -7.916730809865828888, 5.783357778048663356 ) ) ;
#4356=DIRECTION ( 'NONE',  ( -1.000000000000000000, 0.000000000000000000, 0.000000000000000000 ) ) ;
#4361=AXIS2_PLACEMENT_3D ( 'NONE', #4349, #7260, #13963 ) ;
#4362=CARTESIAN_POINT ( 'NONE',  ( 30.61177514885987350, -5.802548093181622235, 3.283357778048663800 ) ) ;
#4367=ORIENTED_EDGE ( 'NONE', *, *, #6271, .F. ) ;
#4369=DIRECTION ( 'NONE',  ( 1.000000000000000000, 0.000000000000000000, 0.000000000000000000 ) ) ;
#4373=CIRCLE ( 'NONE', #17735, 13.00000000000000178 ) ;
#4374=DIRECTION ( 'NONE',  ( -0.000000000000000000, -0.000000000000000000, 1.000000000000000000 ) ) ;
#4376=VERTEX_POINT ( 'NONE', #4896 ) ;
#4381=CARTESIAN_POINT ( 'NONE',  ( 28.48706592061337162, -2.086641016831144668, 6.453230759126468818 ) ) ;
#4383=CARTESIAN_POINT ( 'NONE',  ( 32.34358231980129261, -4.140085944684206432, 7.939653947423662039 ) ) ;
#4386=CARTESIAN_POINT ( 'NONE',  ( 27.14244485254070938, -4.766720295129625029, 3.627061608673664228 ) ) ;
#4387=CARTESIAN_POINT ( 'NONE',  ( -21.42418507870700850, -22.26964835135415655, 15.24537475165205791 ) ) ;
#4388=ORIENTED_EDGE ( 'NONE', *, *, #15775, .F. ) ;
#4392=CARTESIAN_POINT ( 'NONE',  ( 9.099998387031005720, -19.29508120620799971, 6.000000000000000000 ) ) ;
#4398=CARTESIAN_POINT ( 'NONE',  ( 28.11132641904908169, -7.168068194032743534, 5.783357778048657138 ) ) ;
#4400=CYLINDRICAL_SURFACE ( 'NONE', #8670, 2.749999999999992006 ) ;
#4404=CARTESIAN_POINT ( 'NONE',  ( 31.04338717100262102, -6.177645381738930297, 4.705209693361159573 ) ) ;
#4405=ORIENTED_EDGE ( 'NONE', *, *, #6625, .F. ) ;
#4406=VECTOR ( 'NONE', #773, 1000.000000000000227 ) ;
#4410=CARTESIAN_POINT ( 'NONE',  ( 27.50150540219088313, -5.977401655418042914, 7.939653947423658487 ) ) ;
#4414=CARTESIAN_POINT ( 'NONE',  ( 25.99533317148741318, -3.650983533393564517, 7.939653947423662927 ) ) ;
#4415=CARTESIAN_POINT ( 'NONE',  ( -8.632250723006720250, -18.84644399697197770, 13.00000000000000178 ) ) ;
#4421=ADVANCED_FACE ( 'NONE', ( #2204 ), #7717, .F. ) ;
#4425=CARTESIAN_POINT ( 'NONE',  ( 3.248936832696172505, -15.16081378324841289, 17.00000000000000000 ) ) ;
#4427=VERTEX_POINT ( 'NONE', #10244 ) ;
#4428=AXIS2_PLACEMENT_3D ( 'NONE', #6300, #15919, #3494 ) ;
#4430=CARTESIAN_POINT ( 'NONE',  ( 15.92260893619738837, -28.39189527176317540, 16.15082599432113142 ) ) ;
#4434=ORIENTED_EDGE ( 'NONE', *, *, #11592, .F. ) ;
#4435=CARTESIAN_POINT ( 'NONE',  ( 28.88938074516742205, -6.437160617781993999, 6.861505862736158257 ) ) ;
#4446=CARTESIAN_POINT ( 'NONE',  ( -9.647391702364178201, 16.07861560120820243, 16.78732711007196698 ) ) ;
#4448=EDGE_CURVE ( 'NONE', #4167, #1847, #15792, .T. ) ;
#4452=CARTESIAN_POINT ( 'NONE',  ( -29.25000000000000000, -16.21813761408365195, 13.00000000000000178 ) ) ;
#4453=CARTESIAN_POINT ( 'NONE',  ( 27.85662501549087366, -2.162596695673018043, 6.453230759126474148 ) ) ;
#4454=CARTESIAN_POINT ( 'NONE',  ( 30.17644170758179101, -4.401183590806859947, 8.283357778048662468 ) ) ;
#4456=ORIENTED_EDGE ( 'NONE', *, *, #17544, .F. ) ;
#4459=CARTESIAN_POINT ( 'NONE',  ( 45.50000000000000000, -19.03270077640483038, 5.537981825772250843 ) ) ;
#4462=EDGE_CURVE ( 'NONE', #63, #13752, #2935, .T. ) ;
#4467=CARTESIAN_POINT ( 'NONE',  ( -14.00000000000000178, 0.000000000000000000, 10.50000000000000000 ) ) ;
#4472=CARTESIAN_POINT ( 'NONE',  ( 32.02836186724004364, -4.178063784105134459, 3.627061608673664228 ) ) ;
#4474=CARTESIAN_POINT ( 'NONE',  ( 27.78610916120306129, -6.570083055755264745, 6.861505862736157368 ) ) ;
#4475=CARTESIAN_POINT ( 'NONE',  ( -18.90235488073503944, -20.95521764957430122, 15.70196361584510392 ) ) ;
#4478=CARTESIAN_POINT ( 'NONE',  ( 30.98067518586950442, -1.786210345264705790, 5.783357778048667797 ) ) ;
#4479=ORIENTED_EDGE ( 'NONE', *, *, #3415, .T. ) ;
#4480=LINE ( 'NONE', #8475, #13324 ) ;
#4481=ORIENTED_EDGE ( 'NONE', *, *, #5277, .F. ) ;
#4482=DIRECTION ( 'NONE',  ( -0.9928203230275511881, -0.1196152422706614482, -0.000000000000000000 ) ) ;
#4488=CARTESIAN_POINT ( 'NONE',  ( -20.25000000000001066, -16.21813761408365195, 13.00000000000000355 ) ) ;
#4492=LINE ( 'NONE', #11169, #10065 ) ;
#4493=CARTESIAN_POINT ( 'NONE',  ( 31.69574812466957781, -6.726019302751734763, 5.783357778048657138 ) ) ;
#4497=CARTESIAN_POINT ( 'NONE',  ( 29.51982165028991645, -6.361204938940122844, 6.861505862736158257 ) ) ;
#4501=CARTESIAN_POINT ( 'NONE',  ( 26.65222088368961195, -7.333664733486695120, 5.783357778048657138 ) ) ;
#4512=EDGE_CURVE ( 'NONE', #6446, #4895, #894, .T. ) ;
#4513=CARTESIAN_POINT ( 'NONE',  ( 28.82057243903374655, -7.082618055128190093, 5.783357778048657138 ) ) ;
#4518=VERTEX_POINT ( 'NONE', #8878 ) ;
#4519=CARTESIAN_POINT ( 'NONE',  ( 28.98992747081926069, -3.290194058894681639, 7.939653947423662927 ) ) ;
#4521=CARTESIAN_POINT ( 'NONE',  ( 26.31065902414478686, -7.328232685206446106, 5.254681170202263552 ) ) ;
#4522=LINE ( 'NONE', #14136, #10396 ) ;
#4526=LINE ( 'NONE', #6058, #9290 ) ;
#4529=EDGE_CURVE ( 'NONE', #14120, #11482, #8962, .T. ) ;
#4535=CARTESIAN_POINT ( 'NONE',  ( 27.87986455999572399, -6.131689368163069531, 8.283357778048658915 ) ) ;
#4537=VERTEX_POINT ( 'NONE', #14506 ) ;
#4540=EDGE_CURVE ( 'NONE', #17902, #5885, #6643, .T. ) ;
#4549=CARTESIAN_POINT ( 'NONE',  ( 26.13613979636700080, -5.895191778948487560, 5.783357778048662468 ) ) ;
#4551=CARTESIAN_POINT ( 'NONE',  ( -2.016448651773435938E-27, -20.49999999999999645, 6.000000000000000000 ) ) ;
#4554=CARTESIAN_POINT ( 'NONE',  ( 25.63782166807609997, -6.407846580969937200, 3.746366521588336163 ) ) ;
#4558=CARTESIAN_POINT ( 'NONE',  ( -23.83685604381143364, -22.42490655540755284, 14.74319968589249719 ) ) ;
#4560=VERTEX_POINT ( 'NONE', #14604 ) ;
#4562=ORIENTED_EDGE ( 'NONE', *, *, #2762, .T. ) ;
#4570=CARTESIAN_POINT ( 'NONE',  ( 45.50000000000000000, -19.03270077640483038, 8.287981825772241962 ) ) ;
#4571=ADVANCED_FACE ( 'NONE', ( #2182 ), #8501, .F. ) ;
#4578=CARTESIAN_POINT ( 'NONE',  ( 28.91999743871649997, -5.806501378023834370, 7.939653947423658487 ) ) ;
#4583=CARTESIAN_POINT ( 'NONE',  ( 31.45915434921569798, -2.992700983430681028, 3.627061608673666893 ) ) ;
#4600=CARTESIAN_POINT ( 'NONE',  ( 33.00219691583784964, -5.514549477365426888, 8.283357778048658915 ) ) ;
#4602=EDGE_LOOP ( 'NONE', ( #16336, #10291, #3071, #10243, #5181, #16385, #11330, #9461, #16526 ) ) ;
#4605=CARTESIAN_POINT ( 'NONE',  ( 28.77978050244509944, -3.315512618508630549, 3.627061608673666449 ) ) ;
#4607=CARTESIAN_POINT ( 'NONE',  ( 31.66250999073069750, -5.675955295111850596, 8.283357778048660691 ) ) ;
#4608=FACE_OUTER_BOUND ( 'NONE', #1403, .T. ) ;
#4609=EDGE_CURVE ( 'NONE', #15022, #2542, #17038, .T. ) ;
#4610=DIRECTION ( 'NONE',  ( -1.000000000000000000, 0.000000000000000000, 0.000000000000000000 ) ) ;
#4611=CARTESIAN_POINT ( 'NONE',  ( -23.47400307746860548, -29.47066586337336247, 14.90105725137467552 ) ) ;
#4614=CIRCLE ( 'NONE', #13015, 13.00000000000000178 ) ;
#4615=CARTESIAN_POINT ( 'NONE',  ( 4.906836669863238853, 17.52808241874658890, 16.98904569177533119 ) ) ;
#4617=CARTESIAN_POINT ( 'NONE',  ( -11.90182750357594621, 14.98910623166845646, 16.60584412753037853 ) ) ;
#4623=CARTESIAN_POINT ( 'NONE',  ( 50.00000000000000000, -16.03270077640482683, 5.537981825772250843 ) ) ;
#4624=CIRCLE ( 'NONE', #6935, 25.00000000000000000 ) ;
#4626=CARTESIAN_POINT ( 'NONE',  ( 27.38828526237195504, -6.917821758047558056, 7.033357778048657138 ) ) ;
#4628=AXIS2_PLACEMENT_3D ( 'NONE', #17856, #2768, #5376 ) ;
#4629=ORIENTED_EDGE ( 'NONE', *, *, #14838, .F. ) ;
#4632=EDGE_CURVE ( 'NONE', #11675, #11700, #2763, .T. ) ;
#4634=FACE_BOUND ( 'NONE', #13647, .T. ) ;
#4645=ORIENTED_EDGE ( 'NONE', *, *, #13736, .F. ) ;
#4648=CARTESIAN_POINT ( 'NONE',  ( 32.75517961154501023, -5.344437665069116328, 3.627061608673662896 ) ) ;
#4649=STYLED_ITEM ( 'NONE', ( #16761 ), #755 ) ;
#4650=ORIENTED_EDGE ( 'NONE', *, *, #2857, .T. ) ;
#4652=CARTESIAN_POINT ( 'NONE',  ( -21.03357387009699409, -22.15422581635157684, 15.32066355758547083 ) ) ;
#4656=ORIENTED_EDGE ( 'NONE', *, *, #3902, .T. ) ;
#4659=ORIENTED_EDGE ( 'NONE', *, *, #2382, .T. ) ;
#4662=DIRECTION ( 'NONE',  ( -0.000000000000000000, -0.000000000000000000, 1.000000000000000000 ) ) ;
#4668=FACE_OUTER_BOUND ( 'NONE', #87, .T. ) ;
#4669=CARTESIAN_POINT ( 'NONE',  ( 29.42969845347704450, -5.944964990802679594, 3.283357778048663356 ) ) ;
#4670=CARTESIAN_POINT ( 'NONE',  ( 30.18087924896149588, -5.654590020340094725, 7.939653947423658487 ) ) ;
#4672=CARTESIAN_POINT ( 'NONE',  ( 26.27285561281998483, -7.029948842322404801, 6.856036165127777693 ) ) ;
#4674=CARTESIAN_POINT ( 'NONE',  ( 32.81641299864316608, -4.083119185552795294, 3.627061608673664228 ) ) ;
#4677=EDGE_LOOP ( 'NONE', ( #14561, #4388, #713, #2268 ) ) ;
#4692=CARTESIAN_POINT ( 'NONE',  ( 30.66050125466253107, -2.889050389913576655, 8.283357778048664244 ) ) ;
#4697=CARTESIAN_POINT ( 'NONE',  ( 32.95662993491456660, -6.574107945067995118, 5.783357778048657138 ) ) ;
#4698=( NAMED_UNIT ( * ) PLANE_ANGLE_UNIT ( ) SI_UNIT ( $, .RADIAN. ) );
#4703=DIRECTION ( 'NONE',  ( -0.000000000000000000, -0.000000000000000000, 1.000000000000000000 ) ) ;
#4705=AXIS2_PLACEMENT_3D ( 'NONE', #7949, #786, #16211 ) ;
#4706=FACE_OUTER_BOUND ( 'NONE', #879, .T. ) ;
#4716=CARTESIAN_POINT ( 'NONE',  ( 28.75424055680402802, -6.753251120556833520, 4.533357778048659803 ) ) ;
#4726=CARTESIAN_POINT ( 'NONE',  ( -25.11802603177690330, -19.03270077640482683, 10.53798182577225084 ) ) ;
#4728=LINE ( 'NONE', #12984, #8364 ) ;
#4731=CARTESIAN_POINT ( 'NONE',  ( 20.00000000000000355, 7.999999999999996447, 0.000000000000000000 ) ) ;
#4732=PLANE ( 'NONE',  #1386 ) ;
#4736=CARTESIAN_POINT ( 'NONE',  ( 33.38562051666750818, -5.268481986227246061, 3.627061608673662896 ) ) ;
#4754=CARTESIAN_POINT ( 'NONE',  ( 27.17934203385504333, -30.00000000000000355, 0.000000000000000000 ) ) ;
#4756=CARTESIAN_POINT ( 'NONE',  ( 28.08810621022444920, -4.652786776866828511, 7.939653947423662039 ) ) ;
#4760=CARTESIAN_POINT ( 'NONE',  ( 33.30663696749426350, -1.516174747195733863, 5.783357778048668685 ) ) ;
#4761=CARTESIAN_POINT ( 'NONE',  ( -22.62696978904229184, -9.966234395617776798, 15.00355996101822242 ) ) ;
#4762=LINE ( 'NONE', #17223, #4136 ) ;
#4772=CARTESIAN_POINT ( 'NONE',  ( 31.34233605952372415, -6.778795339760710803, 5.783357778048664244 ) ) ;
#4773=DIRECTION ( 'NONE',  ( 0.000000000000000000, 0.000000000000000000, -1.000000000000000000 ) ) ;
#4776=ORIENTED_EDGE ( 'NONE', *, *, #13426, .F. ) ;
#4777=CARTESIAN_POINT ( 'NONE',  ( 3.538288549924106796, -15.34800872113743431, 16.99955934415557479 ) ) ;
#4778=CARTESIAN_POINT ( 'NONE',  ( 32.93832978346670615, -1.887710243310447567, 4.533357778048667797 ) ) ;
#4783=DIRECTION ( 'NONE',  ( 0.1196152422706621143, -0.9928203230275509661, 0.000000000000000000 ) ) ;
#4800=CARTESIAN_POINT ( 'NONE',  ( 26.66018910156667232, -2.644102211984857842, 7.033357778048666020 ) ) ;
#4801=ORIENTED_EDGE ( 'NONE', *, *, #13442, .F. ) ;
#4804=VERTEX_POINT ( 'NONE', #10264 ) ;
#4807=CARTESIAN_POINT ( 'NONE',  ( -34.91377932259078420, -11.86950488720510322, 11.57182824616228878 ) ) ;
#4815=CARTESIAN_POINT ( 'NONE',  ( 27.19802975513453092, -2.241944418315925613, 5.783357778048667797 ) ) ;
#4818=CARTESIAN_POINT ( 'NONE',  ( 31.08270050955629671, -4.291997302367946077, 7.939653947423662039 ) ) ;
#4822=CARTESIAN_POINT ( 'NONE',  ( 33.23365877489121090, -6.550928303235100891, 5.783357778048664244 ) ) ;
#4823=CARTESIAN_POINT ( 'NONE',  ( 27.29063000668916672, -2.568146533142987575, 7.033357778048666020 ) ) ;
#4825=CARTESIAN_POINT ( 'NONE',  ( 26.21953647431484313, -6.587393835875770876, 3.921931135572711113 ) ) ;
#4831=CARTESIAN_POINT ( 'NONE',  ( 33.01342578063301403, -4.059383036018435753, 3.283357778048664244 ) ) ;
#4835=EDGE_CURVE ( 'NONE', #12650, #14000, #12203, .T. ) ;
#4839=CYLINDRICAL_SURFACE ( 'NONE', #939, 2.500000000000001776 ) ;
#4840=CARTESIAN_POINT ( 'NONE',  ( 33.55383270609817714, -5.448088258586239796, 8.283357778048660691 ) ) ;
#4841=CARTESIAN_POINT ( 'NONE',  ( 26.51200394741821498, -4.842675973971495296, 3.627061608673664228 ) ) ;
#4842=ORIENTED_EDGE ( 'NONE', *, *, #9184, .T. ) ;
#4843=AXIS2_PLACEMENT_3D ( 'NONE', #3842, #17572, #7920 ) ;
#4845=CARTESIAN_POINT ( 'NONE',  ( 26.00079723459025871, -4.771832887959356562, 7.973898148876339853 ) ) ;
#4846=ORIENTED_EDGE ( 'NONE', *, *, #3681, .F. ) ;
#4847=CARTESIAN_POINT ( 'NONE',  ( 26.24062359194589078, -6.129313013101781671, 7.939653947423658487 ) ) ;
#4848=CARTESIAN_POINT ( 'NONE',  ( -22.21636613273916794, -10.00424398458219066, 15.08813622000165466 ) ) ;
#4849=ORIENTED_EDGE ( 'NONE', *, *, #17295, .F. ) ;
#4850=DIRECTION ( 'NONE',  ( 1.000000000000000000, 0.000000000000000000, 0.000000000000000000 ) ) ;
#4852=FACE_OUTER_BOUND ( 'NONE', #10156, .T. ) ;
#4853=ADVANCED_FACE ( 'NONE', ( #8329 ), #6374, .F. ) ;
#4854=DIRECTION ( 'NONE',  ( -0.9928203230275510771, 0.1196152422706621282, 0.000000000000000000 ) ) ;
#4855=CARTESIAN_POINT ( 'NONE',  ( 36.27615609941022257, -23.17738945083361557, 11.07596365154449636 ) ) ;
#4857=CIRCLE ( 'NONE', #9486, 13.00000000000000178 ) ;
#4863=CARTESIAN_POINT ( 'NONE',  ( -35.41536221060850664, -16.03270077640482683, 0.5379818257722508434 ) ) ;
#4865=CARTESIAN_POINT ( 'NONE',  ( 31.88017671309158274, -6.376637546091784792, 7.033357778048657138 ) ) ;
#4871=CARTESIAN_POINT ( 'NONE',  ( 26.36761712467744090, -6.740983333149474177, 6.861505862736158257 ) ) ;
#4873=CARTESIAN_POINT ( 'NONE',  ( 35.41536221060850664, -16.03270077640482683, 0.5379818257722508434 ) ) ;
#4881=LINE ( 'NONE', #117, #2152 ) ;
#4895=VERTEX_POINT ( 'NONE', #10612 ) ;
#4896=CARTESIAN_POINT ( 'NONE',  ( 32.36819060393585801, 0.8990368551114588103, 5.783357778048663356 ) ) ;
#4898=VERTEX_POINT ( 'NONE', #2222 ) ;
#4901=EDGE_CURVE ( 'NONE', #9400, #4376, #14993, .T. ) ;
#4906=CIRCLE ( 'NONE', #1740, 5.500000000000000888 ) ;
#4912=ADVANCED_FACE ( 'NONE', ( #10533 ), #14728, .F. ) ;
#4919=ORIENTED_EDGE ( 'NONE', *, *, #15167, .T. ) ;
#4920=DIRECTION ( 'NONE',  ( 0.000000000000000000, -0.000000000000000000, 1.000000000000000000 ) ) ;
#4921=CLOSED_SHELL ( 'NONE', ( #14723, #11343, #5574, #299, #7162, #12345, #15169, #8943, #5640, #2440, #8741, #4421, #3827, #15310, #1715, #5899, #9694, #9871, #14974, #3996, #17071, #4149, #12517, #7789, #10053, #6574, #16477, #10176, #2580, #11112, #2907, #7430, #16188, #5773, #6399, #7008, #5061, #12655, #3922, #7194, #13967, #5404, #5812, #14815, #17275, #12865, #15795, #6922, #772, #16257, #9813, #7351, #15545, #256, #4220, #14755, #16780, #4958, #15727, #10719, #4182, #16494, #11611, #7671, #6134, #14062, #2279, #14197, #569, #16451, #16677, #12305, #16378, #11528, #13637, #11195, #17590, #14086, #14777, #16409, #9048, #16540, #13841, #850, #7516, #12824, #4912, #16500, #230, #10219, #10986, #9784, #4853, #6605, #6949, #98, #8169, #5788, #5625, #17466, #10433, #173, #12497, #7126, #10625, #10454, #4571, #13728, #1208 ) ) ;
#4926=FACE_OUTER_BOUND ( 'NONE', #11004, .T. ) ;
#4931=CARTESIAN_POINT ( 'NONE',  ( 32.90015225647083952, -1.554951264938056132, 6.453230759126471483 ) ) ;
#4932=CARTESIAN_POINT ( 'NONE',  ( 33.76397967447234549, -5.422769698972272678, 3.283357778048663800 ) ) ;
#4938=CARTESIAN_POINT ( 'NONE',  ( 31.66930131758986988, -2.967382423816733894, 7.939653947423664704 ) ) ;
#4942=VERTEX_POINT ( 'NONE', #14640 ) ;
#4944=CARTESIAN_POINT ( 'NONE',  ( -2.016448651773435938E-27, -20.49999999999999645, 6.000000000000000000 ) ) ;
#4956=VECTOR ( 'NONE', #8576, 1000.000000000000227 ) ;
#4957=CARTESIAN_POINT ( 'NONE',  ( 31.29094215978502547, -2.813094711071706389, 8.283357778048664244 ) ) ;
#4958=ADVANCED_FACE ( 'NONE', ( #16272 ), #7828, .T. ) ;
#4963=VERTEX_POINT ( 'NONE', #1369 ) ;
#4964=CARTESIAN_POINT ( 'NONE',  ( 27.45273115869273539, -7.247415916675651992, 6.453230759126468818 ) ) ;
#4965=CARTESIAN_POINT ( 'NONE',  ( 33.76207435632690590, -3.969185667289998332, 7.939653947423662039 ) ) ;
#4974=CARTESIAN_POINT ( 'NONE',  ( -23.00000000000000000, -16.21813761408365195, 13.00000000000000178 ) ) ;
#4975=CARTESIAN_POINT ( 'NONE',  ( 27.55969062878875064, -7.234529412811931515, 5.783357778048657138 ) ) ;
#4976=CARTESIAN_POINT ( 'NONE',  ( 17.39700462756752231, -13.41815250082780508, 15.94071721526680108 ) ) ;
#4978=ORIENTED_EDGE ( 'NONE', *, *, #12736, .F. ) ;
#4979=AXIS2_PLACEMENT_3D ( 'NONE', #1121, #13889, #6558 ) ;
#4983=ORIENTED_EDGE ( 'NONE', *, *, #431, .T. ) ;
#4984=CARTESIAN_POINT ( 'NONE',  ( -13.00000000000000178, -1.592040838891559293E-15, 12.00000000000000000 ) ) ;
#4990=AXIS2_PLACEMENT_3D ( 'NONE', #8667, #11168, #1788 ) ;
#4992=CARTESIAN_POINT ( 'NONE',  ( 29.37220822929407760, -7.016156836349003001, 5.783357778048657138 ) ) ;
#4996=EDGE_CURVE ( 'NONE', #14967, #17858, #4294, .T. ) ;
#5001=LINE ( 'NONE', #13618, #8686 ) ;
#5003=ORIENTED_EDGE ( 'NONE', *, *, #335, .F. ) ;
#5012=EDGE_LOOP ( 'NONE', ( #8756, #11883, #5023, #1923 ) ) ;
#5021=FACE_BOUND ( 'NONE', #13598, .T. ) ;
#5023=ORIENTED_EDGE ( 'NONE', *, *, #4293, .T. ) ;
#5026=CARTESIAN_POINT ( 'NONE',  ( -2.016448651773435938E-27, -20.49999999999999645, 13.00000000000000178 ) ) ;
#5027=CARTESIAN_POINT ( 'NONE',  ( 26.65222088368961195, -7.333664733486695120, 5.783357778048657138 ) ) ;
#5031=CARTESIAN_POINT ( 'NONE',  ( 28.91999743871649997, -5.806501378023834370, 7.939653947423658487 ) ) ;
#5032=DIRECTION ( 'NONE',  ( -0.000000000000000000, -1.000000000000000000, 3.469446951953614189E-16 ) ) ;
#5034=VERTEX_POINT ( 'NONE', #942 ) ;
#5036=DIRECTION ( 'NONE',  ( -0.000000000000000000, -0.000000000000000000, 1.000000000000000000 ) ) ;
#5038=PLANE ( 'NONE',  #4705 ) ;
#5042=CARTESIAN_POINT ( 'NONE',  ( 33.56434302664245450, -9.029166375164061620, 5.783357778048664244 ) ) ;
#5047=CARTESIAN_POINT ( 'NONE',  ( 26.01652455409633902, -4.902371455920936150, 5.783357778048662468 ) ) ;
#5048=CARTESIAN_POINT ( 'NONE',  ( 28.99436501219896201, -4.543600488427916417, 8.283357778048662468 ) ) ;
#5055=CARTESIAN_POINT ( 'NONE',  ( 28.30694982360322953, -3.372479377640031473, 3.627061608673666449 ) ) ;
#5057=CARTESIAN_POINT ( 'NONE',  ( 50.00000000000000000, -19.03270077640483038, 5.537981825772250843 ) ) ;
#5059=LINE ( 'NONE', #16147, #15088 ) ;
#5061=ADVANCED_FACE ( 'NONE', ( #4608 ), #15500, .F. ) ;
#5064=CARTESIAN_POINT ( 'NONE',  ( 21.62432203902686823, -10.11801842300244125, 15.20615207729255403 ) ) ;
#5072=ORIENTED_EDGE ( 'NONE', *, *, #16660, .F. ) ;
#5075=ORIENTED_EDGE ( 'NONE', *, *, #15167, .F. ) ;
#5078=CARTESIAN_POINT ( 'NONE',  ( -8.632250723006722026, -18.84644399697197770, 16.84735068286508763 ) ) ;
#5086=CARTESIAN_POINT ( 'NONE',  ( 32.83754810739939956, -9.116730809865838836, 5.783357778048664244 ) ) ;
#5095=CARTESIAN_POINT ( 'NONE',  ( 0.000000000000000000, 0.000000000000000000, 0.000000000000000000 ) ) ;
#5098=CARTESIAN_POINT ( 'NONE',  ( 29.78612525785423060, -2.267488637519798012, 4.533357778048667797 ) ) ;
#5101=CARTESIAN_POINT ( 'NONE',  ( 26.01652455409633902, -4.902371455920926380, 5.783357778048663356 ) ) ;
#5102=DIRECTION ( 'NONE',  ( 0.000000000000000000, -1.000000000000000000, 3.469446951953614189E-16 ) ) ;
#5103=LINE ( 'NONE', #11909, #5688 ) ;
#5108=CARTESIAN_POINT ( 'NONE',  ( 26.41562710823574278, -3.600346414165641828, 3.627061608673666893 ) ) ;
#5111=CARTESIAN_POINT ( 'NONE',  ( 30.43486631442457835, -6.877930660435475296, 5.783357778048657138 ) ) ;
#5115=LINE ( 'NONE', #14918, #7074 ) ;
#5118=CARTESIAN_POINT ( 'NONE',  ( 32.32036211097666012, -1.624804527518282748, 5.783357778048663356 ) ) ;
#5122=LINE ( 'NONE', #17318, #12688 ) ;
#5125=CARTESIAN_POINT ( 'NONE',  ( 25.60565592828815440, -3.070961412863312034, 4.705209693361167567 ) ) ;
#5126=VECTOR ( 'NONE', #124, 1000.000000000000000 ) ;
#5127=CARTESIAN_POINT ( 'NONE',  ( 33.40745134805642635, -4.011910736534825439, 8.283357778048662468 ) ) ;
#5130=CARTESIAN_POINT ( 'NONE',  ( 27.50829672905005907, -3.268828784122927100, 8.283357778048664244 ) ) ;
#5135=CARTESIAN_POINT ( 'NONE',  ( 30.62726312072365431, -1.838986382273682718, 5.783357778048668685 ) ) ;
#5136=CARTESIAN_POINT ( 'NONE',  ( 30.92509028327567933, -4.310986222078405206, 3.627061608673664228 ) ) ;
#5138=CARTESIAN_POINT ( 'NONE',  ( 30.61929490284659394, -6.528548903775525325, 7.033357778048657138 ) ) ;
#5141=DIRECTION ( 'NONE',  ( 0.9928203230275512992, 0.1196152422706610180, 4.006172263299093133E-17 ) ) ;
#5144=DIRECTION ( 'NONE',  ( 1.000000000000000000, 0.000000000000000000, 0.000000000000000000 ) ) ;
#5147=CARTESIAN_POINT ( 'NONE',  ( -17.83875296969244673, 10.53491135297441161, 15.87472302800564350 ) ) ;
#5157=VERTEX_POINT ( 'NONE', #15314 ) ;
#5158=CARTESIAN_POINT ( 'NONE',  ( 30.62726312072365431, -1.838986382273682718, 5.783357778048668685 ) ) ;
#5162=EDGE_CURVE ( 'NONE', #17459, #5666, #533, .T. ) ;
#5163=CYLINDRICAL_SURFACE ( 'NONE', #5494, 5.000000000000000000 ) ;
#5164=AXIS2_PLACEMENT_3D ( 'NONE', #13653, #4135, #13741 ) ;
#5168=CARTESIAN_POINT ( 'NONE',  ( 23.00000000000000000, -16.21813761408365195, 13.00000000000000355 ) ) ;
#5169=FACE_OUTER_BOUND ( 'NONE', #11774, .T. ) ;
#5171=CYLINDRICAL_SURFACE ( 'NONE', #6442, 2.749999999999992006 ) ;
#5177=EDGE_CURVE ( 'NONE', #15632, #14031, #14066, .T. ) ;
#5178=CARTESIAN_POINT ( 'NONE',  ( 31.11087420047036289, -5.742416513891037688, 8.283357778048660691 ) ) ;
#5180=B_SPLINE_CURVE_WITH_KNOTS ( 'NONE', 3,
 ( #16151, #16334, #13234, #13424, #8975, #17444, #9328, #4976, #6440, #14518, #12042, #1003, #17629, #14866, #2453, #727, #7624, #10505, #13148, #6252, #5064, #16067, #13329, #17543, #10584, #6961, #5323, #8150, #9575, #13849, #5589, #15301, #4166, #9662, #9410, #11106, #13768, #1347, #6694, #10926, #5676, #6869, #12229, #1534 ),
 .UNSPECIFIED., .F., .F.,
 ( 4, 2, 2, 2, 2, 2, 2, 2, 2, 2, 2, 2, 2, 2, 2, 2, 2, 2, 2, 2, 2, 4 ),
 ( 0.000000000000000000, 0.001235617314710323825, 0.001853425972065488340, 0.002471234629420653289, 0.003706851944130986655, 0.004324660601486156157, 0.004942469258841326527, 0.006178086573551669868, 0.007413703888262013209, 0.008031512545617180976, 0.008649321202972348743, 0.009884938517682682543, 0.01112055583239301808, 0.01235617314710335361, 0.01297398180445852138, 0.01359179046181369088, 0.01482740777652402121, 0.01606302509123435501, 0.01668083374858951584, 0.01729864240594468014, 0.01853425972065500180, 0.01976987703536532692 ),
 .UNSPECIFIED. ) ;
#5181=ORIENTED_EDGE ( 'NONE', *, *, #6884, .T. ) ;
#5182=AXIS2_PLACEMENT_3D ( 'NONE', #8361, #13892, #1485 ) ;
#5189=DIRECTION ( 'NONE',  ( 0.000000000000000000, 0.000000000000000000, -1.000000000000000000 ) ) ;
#5190=CARTESIAN_POINT ( 'NONE',  ( 25.11802603177690330, -19.03270077640483038, 0.5379818257722508434 ) ) ;
#5191=DIRECTION ( 'NONE',  ( 0.000000000000000000, 0.000000000000000000, -1.000000000000000000 ) ) ;
#5194=CARTESIAN_POINT ( 'NONE',  ( 33.83155592109562804, -6.868441680671474536, 5.783357778048657138 ) ) ;
#5197=VECTOR ( 'NONE', #3608, 1000.000000000000114 ) ;
#5198=CARTESIAN_POINT ( 'NONE',  ( 31.44176105920648823, -5.502678662656354192, 7.939653947423658487 ) ) ;
#5199=CARTESIAN_POINT ( 'NONE',  ( -16.79182286896198306, -15.38653328895459893, 16.02976683711036898 ) ) ;
#5200=DIRECTION ( 'NONE',  ( 0.9928203230275510771, 0.1196152422706609902, 4.006172263299092517E-17 ) ) ;
#5213=CARTESIAN_POINT ( 'NONE',  ( 26.47269060886452507, -6.728324053342490174, 4.705209693361160461 ) ) ;
#5217=CARTESIAN_POINT ( 'NONE',  ( 32.93470988637010066, -5.949778345213319497, 4.705209693361159573 ) ) ;
#5218=CARTESIAN_POINT ( 'NONE',  ( 28.52524344760924180, -2.419399995203538101, 4.533357778048667797 ) ) ;
#5221=VERTEX_POINT ( 'NONE', #8701 ) ;
#5222=CARTESIAN_POINT ( 'NONE',  ( 31.38469755857769528, -2.374701023479507178, 6.861505862736165362 ) ) ;
#5224=CARTESIAN_POINT ( 'NONE',  ( 30.17635249042624679, -2.520282741259753045, 4.705209693361168455 ) ) ;
#5225=CARTESIAN_POINT ( 'NONE',  ( 33.95908713831673964, -3.945449517755637903, 5.783357778048663356 ) ) ;
#5227=CARTESIAN_POINT ( 'NONE',  ( 32.24155699611449677, -1.634298987580965923, 5.783357778048662468 ) ) ;
#5230=CARTESIAN_POINT ( 'NONE',  ( 30.17644170758179101, -4.401183590806859947, 8.283357778048662468 ) ) ;
#5232=CARTESIAN_POINT ( 'NONE',  ( 32.00093131988006689, -6.699447617117800569, 5.113484796970852564 ) ) ;
#5243=CARTESIAN_POINT ( 'NONE',  ( 25.92467471225709374, -2.732717170633701453, 4.533357778048667797 ) ) ;
#5245=VERTEX_POINT ( 'NONE', #2362 ) ;
#5246=CARTESIAN_POINT ( 'NONE',  ( 32.54503264317084188, -5.369756224683081669, 7.939653947423658487 ) ) ;
#5249=CARTESIAN_POINT ( 'NONE',  ( 28.20260476654369697, -6.819712339336020612, 4.533357778048659803 ) ) ;
#5255=( BOUNDED_CURVE ( )  B_SPLINE_CURVE ( 2, ( #15451, #3034, #14089, #1676, #9990, #7210, #15535, #12722, #10179 ),
 .UNSPECIFIED., .F., .T. ) 
 B_SPLINE_CURVE_WITH_KNOTS ( ( 3, 2, 2, 2, 3 ),
 ( 0.5192307692307692735, 0.5256410256410256610, 0.5384615384615384359, 0.5512820512820513219, 0.5576923076923077094 ),
 .UNSPECIFIED. ) 
 CURVE ( )  GEOMETRIC_REPRESENTATION_ITEM ( )  RATIONAL_B_SPLINE_CURVE ( ( 0.9330127018922192983, 0.9330127018922198534, 1.000000000000000000, 0.8660254037844387076, 1.000000000000000000, 0.8660254037844387076, 1.000000000000000000, 0.9330127018922194093, 0.9330127018922194093 ) ) 
 REPRESENTATION_ITEM ( '' )  );
#5262=APPLICATION_CONTEXT ( 'automotive_design' ) ;
#5263=DIRECTION ( 'NONE',  ( -0.000000000000000000, 1.000000000000000000, -0.000000000000000000 ) ) ;
#5266=MANIFOLD_SOLID_BREP ( '<Caliper Body Half>-<Thread1>', #4921 ) ;
#5272=ORIENTED_EDGE ( 'NONE', *, *, #265, .F. ) ;
#5277=EDGE_CURVE ( 'NONE', #4804, #825, #4857, .T. ) ;
#5280=CARTESIAN_POINT ( 'NONE',  ( -35.46635924378174565, -16.45598204045937152, 11.37070560279562059 ) ) ;
#5284=CARTESIAN_POINT ( 'NONE',  ( 31.17093069310692499, -6.462087684996337345, 7.033357778048657138 ) ) ;
#5287=CARTESIAN_POINT ( 'NONE',  ( 31.03886041246737548, -3.043338102658604161, 7.939653947423664704 ) ) ;
#5289=CARTESIAN_POINT ( 'NONE',  ( 23.43992347230441453, -22.46596520570847844, 14.83047979245100656 ) ) ;
#5296=EDGE_CURVE ( 'NONE', #15182, #8284, #3132, .T. ) ;
#5300=CARTESIAN_POINT ( 'NONE',  ( 33.20550441965735899, -6.554320347036139971, 6.453230759126467042 ) ) ;
#5302=CARTESIAN_POINT ( 'NONE',  ( 27.49697864365563760, -2.843094376337701679, 4.705209693361167567 ) ) ;
#5304=CARTESIAN_POINT ( 'NONE',  ( 32.50309786422735669, -5.574681056656013212, 3.283357778048663356 ) ) ;
#5305=CARTESIAN_POINT ( 'NONE',  ( 32.30426898124760982, -6.025734024055190652, 4.705209693361159573 ) ) ;
#5307=CARTESIAN_POINT ( 'NONE',  ( 29.49727470010032704, -7.390636972501882340, 5.783357778048657138 ) ) ;
#5311=CARTESIAN_POINT ( 'NONE',  ( 30.90769699326644826, -6.820963901304073929, 5.783357778048658027 ) ) ;
#5313=CARTESIAN_POINT ( 'NONE',  ( 28.89355063163679915, -2.047864499088824175, 5.783357778048668685 ) ) ;
#5314=CARTESIAN_POINT ( 'NONE',  ( 29.82675284572052732, -1.925235199084722959, 6.453230759126469707 ) ) ;
#5315=CARTESIAN_POINT ( 'NONE',  ( 25.29083129957448151, -4.989803161779970964, 5.783357778048662468 ) ) ;
#5323=CARTESIAN_POINT ( 'NONE',  ( 25.01746843935482190, -10.28886876799018246, 14.47312570928799680 ) ) ;
#5331=CARTESIAN_POINT ( 'NONE',  ( 31.71314141467879111, -4.216041623526076698, 7.939653947423662039 ) ) ;
#5334=LINE ( 'NONE', #16251, #10441 ) ;
#5335=LINE ( 'NONE', #10771, #11308 ) ;
#5336=CARTESIAN_POINT ( 'NONE',  ( 16.75000000000000000, -16.21813761408365195, 16.03574476417184513 ) ) ;
#5341=ORIENTED_EDGE ( 'NONE', *, *, #4529, .T. ) ;
#5352=CARTESIAN_POINT ( 'NONE',  ( -9.099998387031003944, -19.29508120620799616, 16.81964500401478091 ) ) ;
#5359=DIRECTION ( 'NONE',  ( 0.000000000000000000, 0.000000000000000000, 1.000000000000000000 ) ) ;
#5363=DIRECTION ( 'NONE',  ( 0.000000000000000000, 0.000000000000000000, 1.000000000000000000 ) ) ;
#5367=DIRECTION ( 'NONE',  ( 0.9928203230275510771, 0.1196152422706609902, 4.006172263299092517E-17 ) ) ;
#5368=EDGE_LOOP ( 'NONE', ( #14706, #14095, #4250, #14788 ) ) ;
#5370=CARTESIAN_POINT ( 'NONE',  ( 29.65098506949083301, -2.583579140294649523, 6.861505862736166250 ) ) ;
#5371=CARTESIAN_POINT ( 'NONE',  ( -17.71052479140136526, -12.88256812061772116, 15.89289657457836746 ) ) ;
#5376=DIRECTION ( 'NONE',  ( 1.000000000000000000, 0.000000000000000000, 0.000000000000000000 ) ) ;
#5377=( BOUNDED_CURVE ( )  B_SPLINE_CURVE ( 2, ( #9835, #11009, #1616, #1525, #3059, #7056, #5667, #2970, #1702 ),
 .UNSPECIFIED., .F., .T. ) 
 B_SPLINE_CURVE_WITH_KNOTS ( ( 3, 2, 2, 2, 3 ),
 ( 0.3269230769230769273, 0.3333333333333333148, 0.3461538461538461453, 0.3589743589743589758, 0.3653846153846154188 ),
 .UNSPECIFIED. ) 
 CURVE ( )  GEOMETRIC_REPRESENTATION_ITEM ( )  RATIONAL_B_SPLINE_CURVE ( ( 0.9330127018922194093, 0.9330127018922194093, 1.000000000000000000, 0.8660254037844387076, 1.000000000000000000, 0.8660254037844387076, 1.000000000000000000, 0.9330127018922190762, 0.9330127018922194093 ) ) 
 REPRESENTATION_ITEM ( '' )  );
#5380=LINE ( 'NONE', #3868, #6161 ) ;
#5387=CARTESIAN_POINT ( 'NONE',  ( 30.65370992780335868, -5.597623261208691581, 7.939653947423658487 ) ) ;
#5389=CARTESIAN_POINT ( 'NONE',  ( 32.26287188679368256, -2.695996373064596607, 3.283357778048666464 ) ) ;
#5390=CARTESIAN_POINT ( 'NONE',  ( -16.75000000000000000, -16.21813761408365195, 16.03574476417183448 ) ) ;
#5392=EDGE_CURVE ( 'NONE', #16872, #7076, #2563, .T. ) ;
#5393=ORIENTED_EDGE ( 'NONE', *, *, #16812, .T. ) ;
#5394=CARTESIAN_POINT ( 'NONE',  ( 31.88814493096863956, -1.687075024589942851, 5.783357778048668685 ) ) ;
#5395=CARTESIAN_POINT ( 'NONE',  ( 8.632250723006720250, -18.84644399697197770, 13.00000000000000178 ) ) ;
#5397=CARTESIAN_POINT ( 'NONE',  ( 29.54591158530375239, -2.596238420101622868, 4.705209693361168455 ) ) ;
#5400=CYLINDRICAL_SURFACE ( 'NONE', #12429, 2.500000000000001776 ) ;
#5401=CARTESIAN_POINT ( 'NONE',  ( 28.76917853929504432, -3.116917426439186123, 8.283357778048666020 ) ) ;
#5404=ADVANCED_FACE ( 'NONE', ( #9318, #6778 ), #16323, .T. ) ;
#5405=B_SPLINE_CURVE_WITH_KNOTS ( 'NONE', 3,
 ( #4425, #5949, #13030, #12759 ),
 .UNSPECIFIED., .F., .F.,
 ( 4, 4 ),
 ( 4.336808689942017736E-19, 0.0003446252387907799432 ),
 .UNSPECIFIED. ) ;
#5408=VECTOR ( 'NONE', #306, 1000.000000000000114 ) ;
#5410=DIRECTION ( 'NONE',  ( 0.9928203230275511881, 0.1196152422706614482, 0.000000000000000000 ) ) ;
#5412=ORIENTED_EDGE ( 'NONE', *, *, #9850, .T. ) ;
#5413=EDGE_CURVE ( 'NONE', #4427, #9967, #16572, .T. ) ;
#5419=ORIENTED_EDGE ( 'NONE', *, *, #1311, .F. ) ;
#5423=CARTESIAN_POINT ( 'NONE',  ( 31.27962407439061110, -2.387360303286481855, 4.705209693361167567 ) ) ;
#5435=DIRECTION ( 'NONE',  ( 0.000000000000000000, 0.000000000000000000, -1.000000000000000000 ) ) ;
#5436=AXIS2_PLACEMENT_3D ( 'NONE', #12341, #11049, #17906 ) ;
#5449=FACE_BOUND ( 'NONE', #17127, .T. ) ;
#5451=EDGE_CURVE ( 'NONE', #1012, #4376, #14943, .T. ) ;
#5453=EDGE_CURVE ( 'NONE', #11482, #9288, #6447, .T. ) ;
#5454=CARTESIAN_POINT ( 'NONE',  ( 21.42601376483257880, 2.765314980223224417, 12.00000000000000000 ) ) ;
#5455=CARTESIAN_POINT ( 'NONE',  ( 31.71807556108801407, -1.697368162559112825, 6.453230759126469707 ) ) ;
#5459=CIRCLE ( 'NONE', #17084, 2.749999999999995559 ) ;
#5460=CARTESIAN_POINT ( 'NONE',  ( 28.08810621022444920, -4.652786776866828511, 7.939653947423662039 ) ) ;
#5463=CARTESIAN_POINT ( 'NONE',  ( 31.00199007654869732, -2.847907730748336697, 3.283357778048666464 ) ) ;
#5465=AXIS2_PLACEMENT_3D ( 'NONE', #539, #6521, #10658 ) ;
#5471=FACE_OUTER_BOUND ( 'NONE', #14129, .T. ) ;
#5474=CARTESIAN_POINT ( 'NONE',  ( 25.58373587974369201, -2.446631813008643075, 5.783357778048668685 ) ) ;
#5475=VECTOR ( 'NONE', #13654, 1000.000000000000227 ) ;
#5476=CARTESIAN_POINT ( 'NONE',  ( 28.56093688906631911, -4.595820017735426255, 7.939653947423662039 ) ) ;
#5480=CARTESIAN_POINT ( 'NONE',  ( 33.13163345120441505, -4.045141346131868154, 7.939653947423662039 ) ) ;
#5482=ORIENTED_EDGE ( 'NONE', *, *, #7086, .T. ) ;
#5483=EDGE_CURVE ( 'NONE', #5547, #1659, #5669, .T. ) ;
#5485=CARTESIAN_POINT ( 'NONE',  ( 32.04158527077989760, -6.057382223572642665, 6.861505862736158257 ) ) ;
#5488=CARTESIAN_POINT ( 'NONE',  ( 27.23882169172318513, -6.009049854935478052, 3.627061608673662896 ) ) ;
#5490=CARTESIAN_POINT ( 'NONE',  ( 27.26436163736424945, -2.571311352887278190, 4.533357778048667797 ) ) ;
#5494=AXIS2_PLACEMENT_3D ( 'NONE', #9954, #1552, #1364 ) ;
#5505=FACE_OUTER_BOUND ( 'NONE', #12742, .T. ) ;
#5507=ORIENTED_EDGE ( 'NONE', *, *, #8777, .T. ) ;
#5511=( GEOMETRIC_REPRESENTATION_CONTEXT ( 3 ) GLOBAL_UNCERTAINTY_ASSIGNED_CONTEXT ( ( #15188 ) ) GLOBAL_UNIT_ASSIGNED_CONTEXT ( ( #14598, #16045, #13128 ) ) REPRESENTATION_CONTEXT ( 'NONE', 'WORKASPACE' ) );
#5512=CARTESIAN_POINT ( 'NONE',  ( 31.93198502805756789, -2.935734224299280548, 3.627061608673666449 ) ) ;
#5514=DIRECTION ( 'NONE',  ( -0.1196152422706597551, 0.9928203230275514102, 0.000000000000000000 ) ) ;
#5528=CARTESIAN_POINT ( 'NONE',  ( 20.00000000000000000, 7.999999999999996447, 15.51150668642334374 ) ) ;
#5536=ORIENTED_EDGE ( 'NONE', *, *, #4293, .F. ) ;
#5541=CARTESIAN_POINT ( 'NONE',  ( 29.16815758536418102, -2.004582921727632971, 5.783357778048662468 ) ) ;
#5542=CYLINDRICAL_SURFACE ( 'NONE', #3115, 2.500000000000001776 ) ;
#5547=VERTEX_POINT ( 'NONE', #5581 ) ;
#5552=CARTESIAN_POINT ( 'NONE',  ( 28.76992167940542799, -7.088720471389836852, 5.113484796970857005 ) ) ;
#5557=CARTESIAN_POINT ( 'NONE',  ( -45.50000000000000000, -16.03270077640482683, 2.787981825772258837 ) ) ;
#5564=DIRECTION ( 'NONE',  ( -0.000000000000000000, -0.000000000000000000, 1.000000000000000000 ) ) ;
#5567=CARTESIAN_POINT ( 'NONE',  ( 28.97253418081003673, -5.800171738120336151, 3.627061608673662896 ) ) ;
#5570=CARTESIAN_POINT ( 'NONE',  ( 33.33308377457396432, -5.274811626130743392, 7.939653947423658487 ) ) ;
#5573=EDGE_LOOP ( 'NONE', ( #1007, #12937, #12723, #5393 ) ) ;
#5574=ADVANCED_FACE ( 'NONE', ( #5759 ), #11274, .F. ) ;
#5575=CARTESIAN_POINT ( 'NONE',  ( 29.39282811755836633, -5.749534618892433002, 7.939653947423658487 ) ) ;
#5577=CARTESIAN_POINT ( 'NONE',  ( 27.53153627355490229, -7.237921456612971483, 6.453230759126462601 ) ) ;
#5578=ORIENTED_EDGE ( 'NONE', *, *, #12618, .F. ) ;
#5579=CARTESIAN_POINT ( 'NONE',  ( 26.41562710823574278, -3.600346414165641828, 3.627061608673666449 ) ) ;
#5580=ORIENTED_EDGE ( 'NONE', *, *, #17011, .F. ) ;
#5581=CARTESIAN_POINT ( 'NONE',  ( -3.248936832696171617, -15.16081378324841111, 17.00000000000000000 ) ) ;
#5589=CARTESIAN_POINT ( 'NONE',  ( 26.29446227649215473, -10.90310086042137350, 14.16253947949896563 ) ) ;
#5595=ORIENTED_EDGE ( 'NONE', *, *, #17, .T. ) ;
#5596=EDGE_LOOP ( 'NONE', ( #16986, #16547 ) ) ;
#5597=CARTESIAN_POINT ( 'NONE',  ( 27.61527553138257574, -4.709753535998224550, 3.627061608673664228 ) ) ;
#5602=DIRECTION ( 'NONE',  ( 0.9928203230275512992, 0.1196152422706610180, 4.006172263299093133E-17 ) ) ;
#5609=EDGE_CURVE ( 'NONE', #9143, #122, #9836, .T. ) ;
#5610=ORIENTED_EDGE ( 'NONE', *, *, #378, .T. ) ;
#5612=PLANE ( 'NONE',  #3687 ) ;
#5614=CARTESIAN_POINT ( 'NONE',  ( 33.69269431359690969, -6.158264969628857166, 7.033357778048657138 ) ) ;
#5618=FACE_OUTER_BOUND ( 'NONE', #11965, .T. ) ;
#5619=CYLINDRICAL_SURFACE ( 'NONE', #17146, 2.000000000000001776 ) ;
#5622=ORIENTED_EDGE ( 'NONE', *, *, #10415, .T. ) ;
#5625=ADVANCED_FACE ( 'NONE', ( #9929 ), #156, .F. ) ;
#5629=DIRECTION ( 'NONE',  ( -0.000000000000000000, -0.000000000000000000, 1.000000000000000000 ) ) ;
#5637=CARTESIAN_POINT ( 'NONE',  ( 26.78782184427022983, -4.809445364374452581, 3.283357778048664244 ) ) ;
#5640=ADVANCED_FACE ( 'NONE', ( #11840 ), #6230, .F. ) ;
#5645=CARTESIAN_POINT ( 'NONE',  ( 31.29168529989541270, -6.784897756022354010, 5.113484796970852564 ) ) ;
#5646=ORIENTED_EDGE ( 'NONE', *, *, #15211, .T. ) ;
#5647=CARTESIAN_POINT ( 'NONE',  ( 26.61823960964035507, -2.311797680896151341, 5.113484796970861446 ) ) ;
#5655=CARTESIAN_POINT ( 'NONE',  ( 29.51982165028991645, -6.361204938940122844, 6.861505862736158257 ) ) ;
#5656=EDGE_CURVE ( 'NONE', #6446, #17327, #5122, .T. ) ;
#5657=LINE ( 'NONE', #5841, #14269 ) ;
#5659=CARTESIAN_POINT ( 'NONE',  ( 29.66420847303068697, -4.462897579762144851, 3.627061608673664228 ) ) ;
#5660=ORIENTED_EDGE ( 'NONE', *, *, #8666, .F. ) ;
#5661=ORIENTED_EDGE ( 'NONE', *, *, #201, .F. ) ;
#5662=CARTESIAN_POINT ( 'NONE',  ( 26.98483462626008134, -4.785709214840094816, 3.627061608673664228 ) ) ;
#5664=CARTESIAN_POINT ( 'NONE',  ( 23.00000000000000000, -16.21813761408365195, 13.00000000000000178 ) ) ;
#5666=VERTEX_POINT ( 'NONE', #14493 ) ;
#5667=CARTESIAN_POINT ( 'NONE',  ( 30.72436838703367812, -6.515889623968540434, 4.533357778048659803 ) ) ;
#5669=LINE ( 'NONE', #12750, #8063 ) ;
#5670=CYLINDRICAL_SURFACE ( 'NONE', #10102, 1.000000000000000000 ) ;
#5676=CARTESIAN_POINT ( 'NONE',  ( 29.04511322243489602, -14.57839366656647506, 13.43065377816253481 ) ) ;
#5682=EDGE_LOOP ( 'NONE', ( #15754, #13604, #16656, #1907 ) ) ;
#5683=ORIENTED_EDGE ( 'NONE', *, *, #17475, .F. ) ;
#5685=CARTESIAN_POINT ( 'NONE',  ( 29.62489513447700062, -6.348545659133139729, 4.705209693361160461 ) ) ;
#5688=VECTOR ( 'NONE', #17756, 1000.000000000000000 ) ;
#5698=FACE_OUTER_BOUND ( 'NONE', #7215, .T. ) ;
#5704=CARTESIAN_POINT ( 'NONE',  ( 31.75254397038802878, -4.211294393702175398, 3.283357778048664244 ) ) ;
#5714=ORIENTED_EDGE ( 'NONE', *, *, #15901, .F. ) ;
#5719=CARTESIAN_POINT ( 'NONE',  ( 31.92138306490751987, -2.737139032229836566, 8.283357778048666020 ) ) ;
#5721=EDGE_CURVE ( 'NONE', #17698, #12650, #3418, .T. ) ;
#5724=CARTESIAN_POINT ( 'NONE',  ( 25.96969170380761582, -2.000386719721422235, 5.783357778048668685 ) ) ;
#5734=CARTESIAN_POINT ( 'NONE',  ( 28.84872679426759845, -7.079226011327149237, 5.113484796970851676 ) ) ;
#5742=FACE_OUTER_BOUND ( 'NONE', #15981, .T. ) ;
#5744=CARTESIAN_POINT ( 'NONE',  ( 45.50000000000000000, -16.03270077640482683, 5.537981825772250843 ) ) ;
#5747=CARTESIAN_POINT ( 'NONE',  ( 32.06776442294927421, -4.173316554281249147, 8.283357778048662468 ) ) ;
#5748=CARTESIAN_POINT ( 'NONE',  ( 30.91186687973582536, -2.431667782610909434, 6.861505862736166250 ) ) ;
#5751=VECTOR ( 'NONE', #2364, 1000.000000000000000 ) ;
#5753=CARTESIAN_POINT ( 'NONE',  ( 28.23249303296521617, -2.754479417688857179, 6.861505862736165362 ) ) ;
#5757=CARTESIAN_POINT ( 'NONE',  ( 28.41655006632555569, -6.494127376913395366, 6.861505862736157368 ) ) ;
#5758=ORIENTED_EDGE ( 'NONE', *, *, #17205, .T. ) ;
#5759=FACE_OUTER_BOUND ( 'NONE', #13693, .T. ) ;
#5768=DIRECTION ( 'NONE',  ( -0.000000000000000000, 1.000000000000000000, -3.469446951953614189E-16 ) ) ;
#5771=ORIENTED_EDGE ( 'NONE', *, *, #3022, .T. ) ;
#5772=AXIS2_PLACEMENT_3D ( 'NONE', #16877, #9950, #4610 ) ;
#5773=ADVANCED_FACE ( 'NONE', ( #16552 ), #15596, .T. ) ;
#5778=ORIENTED_EDGE ( 'NONE', *, *, #5296, .T. ) ;
#5779=CARTESIAN_POINT ( 'NONE',  ( 27.30005507882132676, -4.747731375419166788, 7.939653947423662039 ) ) ;
#5780=CARTESIAN_POINT ( 'NONE',  ( 32.83754810739939956, -9.116730809865838836, 5.783357778048664244 ) ) ;
#5783=FACE_OUTER_BOUND ( 'NONE', #14169, .T. ) ;
#5788=ADVANCED_FACE ( 'NONE', ( #8380, #8029 ), #9466, .T. ) ;
#5793=CARTESIAN_POINT ( 'NONE',  ( -4.914599809708808387, 17.56967244544484075, 17.00000000000000711 ) ) ;
#5794=ORIENTED_EDGE ( 'NONE', *, *, #13749, .T. ) ;
#5799=CARTESIAN_POINT ( 'NONE',  ( 33.32864623319426300, -4.021405196597508613, 8.283357778048662468 ) ) ;
#5804=DIRECTION ( 'NONE',  ( 1.000000000000000000, 0.000000000000000000, 0.000000000000000000 ) ) ;
#5807=ORIENTED_EDGE ( 'NONE', *, *, #11555, .F. ) ;
#5811=AXIS2_PLACEMENT_3D ( 'NONE', #8049, #16231, #17537 ) ;
#5812=ADVANCED_FACE ( 'NONE', ( #2683 ), #1059, .T. ) ;
#5813=CARTESIAN_POINT ( 'NONE',  ( 30.05329989404488700, -6.934098741245490416, 6.453230759126467042 ) ) ;
#5814=FACE_BOUND ( 'NONE', #10746, .T. ) ;
#5818=CARTESIAN_POINT ( 'NONE',  ( 26.27749392786457250, -6.324743385012029151, 3.283357778048663800 ) ) ;
#5819=AXIS2_PLACEMENT_3D ( 'NONE', #12795, #7280, #4369 ) ;
#5821=CARTESIAN_POINT ( 'NONE',  ( -29.25000000000000000, -16.21813761408365195, 13.37255996287876947 ) ) ;
#5824=ORIENTED_EDGE ( 'NONE', *, *, #6253, .T. ) ;
#5830=CARTESIAN_POINT ( 'NONE',  ( 33.95908713831673964, -3.945449517755637014, 5.783357778048663356 ) ) ;
#5841=CARTESIAN_POINT ( 'NONE',  ( 25.74999999999999289, -16.21813761408365195, 13.00000000000000178 ) ) ;
#5842=CARTESIAN_POINT ( 'NONE',  ( 32.52441275490655670, -6.636378442139655220, 5.783357778048664244 ) ) ;
#5843=CARTESIAN_POINT ( 'NONE',  ( 31.45915434921569798, -2.992700983430681028, 3.627061608673666893 ) ) ;
#5844=EDGE_LOOP ( 'NONE', ( #3075, #17873, #7658, #5075 ) ) ;
#5848=CARTESIAN_POINT ( 'NONE',  ( 27.73357241910951743, -6.576412695658750529, 4.705209693361160461 ) ) ;
#5851=ORIENTED_EDGE ( 'NONE', *, *, #7285, .F. ) ;
#5857=CARTESIAN_POINT ( 'NONE',  ( -8.632250723006720250, -18.84644399697197770, 13.00000000000000178 ) ) ;
#5863=CARTESIAN_POINT ( 'NONE',  ( -2.016448651773435938E-27, -20.49999999999999645, 13.00000000000000178 ) ) ;
#5866=DIRECTION ( 'NONE',  ( 0.000000000000000000, 0.000000000000000000, -1.000000000000000000 ) ) ;
#5873=CARTESIAN_POINT ( 'NONE',  ( 29.49337484321020497, -2.602568060005117090, 6.861505862736165362 ) ) ;
#5884=CARTESIAN_POINT ( 'NONE',  ( -10.78415792467453471, 15.55827129984638901, 16.70145112110344598 ) ) ;
#5885=VERTEX_POINT ( 'NONE', #6763 ) ;
#5891=CARTESIAN_POINT ( 'NONE',  ( 27.82847066025702887, -2.165988739474055791, 5.783357778048667797 ) ) ;
#5892=EDGE_CURVE ( 'NONE', #118, #11309, #9553, .T. ) ;
#5893=CARTESIAN_POINT ( 'NONE',  ( 29.91004888286193619, -6.613999042680076990, 7.033357778048657138 ) ) ;
#5899=ADVANCED_FACE ( 'NONE', ( #5471 ), #499, .F. ) ;
#5901=PRODUCT_DEFINITION ( 'UNKNOWN', '', #15858, #6844 ) ;
#5908=CARTESIAN_POINT ( 'NONE',  ( 27.33945763453056088, -4.742984145595265488, 3.283357778048664244 ) ) ;
#5912=CARTESIAN_POINT ( 'NONE',  ( 33.28924367748503244, -4.026152426421394814, 3.627061608673664228 ) ) ;
#5914=CARTESIAN_POINT ( 'NONE',  ( -22.21647589440744142, -22.43199035874600966, 15.08811024704901094 ) ) ;
#5917=ORIENTED_EDGE ( 'NONE', *, *, #3587, .T. ) ;
#5920=DIRECTION ( 'NONE',  ( -0.000000000000000000, -0.000000000000000000, 1.000000000000000000 ) ) ;
#5923=CARTESIAN_POINT ( 'NONE',  ( 13.00000000000000178, 0.000000000000000000, 10.50000000000000000 ) ) ;
#5925=CARTESIAN_POINT ( 'NONE',  ( 26.01652455409633902, -4.902371455920926380, 5.783357778048663356 ) ) ;
#5932=CARTESIAN_POINT ( 'NONE',  ( 33.78529456515154550, -6.484467084455913799, 5.783357778048664244 ) ) ;
#5933=CARTESIAN_POINT ( 'NONE',  ( 30.29464937815318493, -4.386941900920275472, 3.627061608673664228 ) ) ;
#5934=EDGE_CURVE ( 'NONE', #14281, #602, #7648, .T. ) ;
#5938=CARTESIAN_POINT ( 'NONE',  ( 27.47505859511117521, -2.218764776483033163, 5.783357778048668685 ) ) ;
#5941=EDGE_CURVE ( 'NONE', #17858, #14967, #17065, .T. ) ;
#5942=ORIENTED_EDGE ( 'NONE', *, *, #15442, .T. ) ;
#5944=CARTESIAN_POINT ( 'NONE',  ( 27.55969062878875064, -7.234529412811931515, 5.783357778048657138 ) ) ;
#5948=CARTESIAN_POINT ( 'NONE',  ( -3.538288549924106796, -15.34800872113743431, 16.99955934415556769 ) ) ;
#5949=CARTESIAN_POINT ( 'NONE',  ( 3.347071143357317702, -15.22052928361023127, 17.00000000000000000 ) ) ;
#5951=CARTESIAN_POINT ( 'NONE',  ( 28.72797218747911074, -6.756415940301135237, 7.033357778048657138 ) ) ;
#5952=CARTESIAN_POINT ( 'NONE',  ( 29.89119874204131122, -2.254829357712824667, 7.033357778048666020 ) ) ;
#5954=EDGE_LOOP ( 'NONE', ( #16727, #649, #6029 ) ) ;
#5955=ORIENTED_EDGE ( 'NONE', *, *, #3783, .F. ) ;
#5957=CARTESIAN_POINT ( 'NONE',  ( 29.41022140756759029, -3.239556939666760726, 3.627061608673666449 ) ) ;
#5960=CARTESIAN_POINT ( 'NONE',  ( 26.31321956127059636, -7.341867041618697520, 5.319444967946814096 ) ) ;
#5965=DIRECTION ( 'NONE',  ( -0.000000000000000000, 1.000000000000000000, 0.000000000000000000 ) ) ;
#5973=FACE_OUTER_BOUND ( 'NONE', #200, .T. ) ;
#5976=CARTESIAN_POINT ( 'NONE',  ( 28.64916707261694384, -6.765910400363817523, 7.033357778048657138 ) ) ;
#5977=CARTESIAN_POINT ( 'NONE',  ( 28.69037342443288452, -3.126411886501869741, 8.283357778048664244 ) ) ;
#5980=CARTESIAN_POINT ( 'NONE',  ( 26.70901672940806648, -4.818939824437135755, 3.283357778048664244 ) ) ;
#5989=VECTOR ( 'NONE', #17093, 1000.000000000000000 ) ;
#5991=ORIENTED_EDGE ( 'NONE', *, *, #7093, .F. ) ;
#5994=DIRECTION ( 'NONE',  ( 0.7999999999999999334, 0.6000000000000001998, 0.000000000000000000 ) ) ;
#5997=CARTESIAN_POINT ( 'NONE',  ( 3.248936832696173393, -28.97437970944926633, 17.00000000000000000 ) ) ;
#5998=CARTESIAN_POINT ( 'NONE',  ( 33.40754056521197413, -5.892811586081919906, 4.705209693361160461 ) ) ;
#6001=CARTESIAN_POINT ( 'NONE',  ( -19.22707546753401786, -21.21757778339487288, 15.64731278403363035 ) ) ;
#6002=CARTESIAN_POINT ( 'NONE',  ( -35.74085044863416272, -28.97437970944926988, 11.27079897466147607 ) ) ;
#6005=ORIENTED_EDGE ( 'NONE', *, *, #6900, .F. ) ;
#6007=CARTESIAN_POINT ( 'NONE',  ( -20.00000000000000000, 7.999999999999996447, 15.51150668642334374 ) ) ;
#6014=CYLINDRICAL_SURFACE ( 'NONE', #9267, 6.249999999999996447 ) ;
#6022=CARTESIAN_POINT ( 'NONE',  ( 31.66930131758986988, -2.967382423816733894, 7.939653947423664704 ) ) ;
#6023=ORIENTED_EDGE ( 'NONE', *, *, #17256, .T. ) ;
#6024=CARTESIAN_POINT ( 'NONE',  ( 26.17715024865823281, -6.235583268514393929, 7.666572473558731282 ) ) ;
#6026=CARTESIAN_POINT ( 'NONE',  ( 33.54323074294813267, -5.249493066516778050, 3.627061608673662896 ) ) ;
#6029=ORIENTED_EDGE ( 'NONE', *, *, #6464, .F. ) ;
#6034=ORIENTED_EDGE ( 'NONE', *, *, #13553, .F. ) ;
#6036=CARTESIAN_POINT ( 'NONE',  ( 32.83754810739939956, -9.116730809865838836, 5.783357778048664244 ) ) ;
#6041=FILL_AREA_STYLE ('',( #11284 ) ) ;
#6045=CARTESIAN_POINT ( 'NONE',  ( 31.78252145740879797, -2.026962321187214311, 7.033357778048666020 ) ) ;
#6047=ORIENTED_EDGE ( 'NONE', *, *, #17295, .T. ) ;
#6050=CARTESIAN_POINT ( 'NONE',  ( 27.02423718196931546, -4.780961985016209503, 8.283357778048662468 ) ) ;
#6051=DIRECTION ( 'NONE',  ( 0.000000000000000000, 0.000000000000000000, 1.000000000000000000 ) ) ;
#6052=( BOUNDED_CURVE ( )  B_SPLINE_CURVE ( 2, ( #4815, #12988, #11334, #485, #5908, #6186, #11708, #16912, #14168 ),
 .UNSPECIFIED., .F., .T. ) 
 B_SPLINE_CURVE_WITH_KNOTS ( ( 3, 2, 2, 2, 3 ),
 ( 0.7884615384615384359, 0.7948717948717948234, 0.8076923076923077094, 0.8205128205128204844, 0.8269230769230769829 ),
 .UNSPECIFIED. ) 
 CURVE ( )  GEOMETRIC_REPRESENTATION_ITEM ( )  RATIONAL_B_SPLINE_CURVE ( ( 0.9330127018922194093, 0.9330127018922194093, 1.000000000000000000, 0.8660254037844387076, 1.000000000000000000, 0.8660254037844387076, 1.000000000000000000, 0.9330127018922187432, 0.9330127018922192983 ) ) 
 REPRESENTATION_ITEM ( '' )  );
#6058=CARTESIAN_POINT ( 'NONE',  ( 25.71748644841968456, -2.420320648352046078, 5.783357778048663356 ) ) ;
#6059=ORIENTED_EDGE ( 'NONE', *, *, #6971, .T. ) ;
#6060=AXIS2_PLACEMENT_3D ( 'NONE', #6687, #12220, #12310 ) ;
#6065=ORIENTED_EDGE ( 'NONE', *, *, #9691, .F. ) ;
#6069=CARTESIAN_POINT ( 'NONE',  ( -8.812506826975363694, -18.97024042328638416, 16.83711976780714181 ) ) ;
#6074=CARTESIAN_POINT ( 'NONE',  ( 28.48022645605872327, -3.151730446115816875, 3.283357778048666464 ) ) ;
#6080=( BOUNDED_CURVE ( )  B_SPLINE_CURVE ( 3, ( #16107, #3669, #5280, #1042 ),
 .UNSPECIFIED., .F., .T. ) 
 B_SPLINE_CURVE_WITH_KNOTS ( ( 4, 4 ),
 ( 5.052230418047667371, 5.061454830783549852 ),
 .UNSPECIFIED. ) 
 CURVE ( )  GEOMETRIC_REPRESENTATION_ITEM ( )  RATIONAL_B_SPLINE_CURVE ( ( 1.000000000000000000, 0.9999929091967096895, 0.9999929091967096895, 1.000000000000000000 ) ) 
 REPRESENTATION_ITEM ( '' )  );
#6083=CARTESIAN_POINT ( 'NONE',  ( -23.00000000000000000, -16.21813761408365195, 13.00000000000000178 ) ) ;
#6084=EDGE_CURVE ( 'NONE', #1473, #2720, #9327, .T. ) ;
#6095=CARTESIAN_POINT ( 'NONE',  ( 25.33925079868512498, -2.076342398563292058, 5.783357778048668685 ) ) ;
#6096=AXIS2_PLACEMENT_3D ( 'NONE', #14470, #16106, #11642 ) ;
#6097=EDGE_CURVE ( 'NONE', #10514, #11624, #4728, .T. ) ;
#6099=ORIENTED_EDGE ( 'NONE', *, *, #16567, .F. ) ;
#6101=PLANE ( 'NONE',  #2052 ) ;
#6105=ORIENTED_EDGE ( 'NONE', *, *, #2930, .T. ) ;
#6110=AXIS2_PLACEMENT_3D ( 'NONE', #9339, #16507, #13698 ) ;
#6112=AXIS2_PLACEMENT_3D ( 'NONE', #1352, #1183, #16589 ) ;
#6114=DIRECTION ( 'NONE',  ( 0.6000000000000001998, 0.7999999999999999334, 0.000000000000000000 ) ) ;
#6120=CARTESIAN_POINT ( 'NONE',  ( 27.67650891848073158, -3.448435056481901295, 3.627061608673666893 ) ) ;
#6123=CARTESIAN_POINT ( 'NONE',  ( 26.31176419598820360, -7.352894575460818594, 5.384699358761103838 ) ) ;
#6125=CARTESIAN_POINT ( 'NONE',  ( 25.58373587974369201, -2.446631813008643075, 5.783357778048668685 ) ) ;
#6126=CARTESIAN_POINT ( 'NONE',  ( -28.91489957058744409, -14.18850833160549207, 13.46727466850441601 ) ) ;
#6127=DIRECTION ( 'NONE',  ( 0.9928203230275510771, 0.1196152422706609902, 4.006172263299092517E-17 ) ) ;
#6131=VECTOR ( 'NONE', #4374, 1000.000000000000000 ) ;
#6134=ADVANCED_FACE ( 'NONE', ( #9661 ), #4065, .F. ) ;
#6139=VECTOR ( 'NONE', #6522, 1000.000000000000000 ) ;
#6145=AXIS2_PLACEMENT_3D ( 'NONE', #10547, #17301, #2329 ) ;
#6146=CARTESIAN_POINT ( 'NONE',  ( 32.34167700165585302, -2.686501913001913433, 3.283357778048666464 ) ) ;
#6152=CARTESIAN_POINT ( 'NONE',  ( 26.88845778707760914, -3.543379655034240905, 3.627061608673666449 ) ) ;
#6154=CARTESIAN_POINT ( 'NONE',  ( 32.81641299864316608, -4.083119185552795294, 3.627061608673664228 ) ) ;
#6161=VECTOR ( 'NONE', #14923, 1000.000000000000000 ) ;
#6162=VECTOR ( 'NONE', #13108, 1000.000000000000000 ) ;
#6171=CARTESIAN_POINT ( 'NONE',  ( 28.01872616749444944, -6.841866079205687790, 7.033357778048657138 ) ) ;
#6182=CARTESIAN_POINT ( 'NONE',  ( 26.01652455409633902, -4.902371455920926380, 5.783357778048663356 ) ) ;
#6186=CARTESIAN_POINT ( 'NONE',  ( 27.45957062324739084, -6.182326487390971792, 3.283357778048663356 ) ) ;
#6189=CARTESIAN_POINT ( 'NONE',  ( 31.28415083292585663, -5.521667582366822202, 7.939653947423658487 ) ) ;
#6191=ORIENTED_EDGE ( 'NONE', *, *, #5451, .T. ) ;
#6193=FACE_OUTER_BOUND ( 'NONE', #6396, .T. ) ;
#6198=CARTESIAN_POINT ( 'NONE',  ( 26.30098629108390895, -7.263436720211717379, 4.952770188466288026 ) ) ;
#6200=DIRECTION ( 'NONE',  ( 0.000000000000000000, 0.000000000000000000, -1.000000000000000000 ) ) ;
#6201=CARTESIAN_POINT ( 'NONE',  ( -34.91600907648203389, -11.88801210197604341, 11.56671555609732671 ) ) ;
#6202=VERTEX_POINT ( 'NONE', #13029 ) ;
#6207=LINE ( 'NONE', #17581, #12163 ) ;
#6210=EDGE_LOOP ( 'NONE', ( #4849, #12012, #12675, #15454 ) ) ;
#6214=CARTESIAN_POINT ( 'NONE',  ( 28.40332666278570173, -4.614808937445885384, 3.627061608673664228 ) ) ;
#6216=ORIENTED_EDGE ( 'NONE', *, *, #883, .F. ) ;
#6218=VECTOR ( 'NONE', #1471, 1000.000000000000000 ) ;
#6220=CARTESIAN_POINT ( 'NONE',  ( 25.62757597683262034, -3.695291012717980994, 3.627061608673666893 ) ) ;
#6221=CARTESIAN_POINT ( 'NONE',  ( -29.25000000000000000, -15.80023397548365871, 13.37255996287876592 ) ) ;
#6224=CARTESIAN_POINT ( 'NONE',  ( 30.35023428074701002, -1.862166024106576057, 5.783357778048662468 ) ) ;
#6230=CYLINDRICAL_SURFACE ( 'NONE', #248, 2.500000000000001776 ) ;
#6234=CARTESIAN_POINT ( 'NONE',  ( 33.04340326765378677, -1.875050963503474222, 7.033357778048666020 ) ) ;
#6241=CARTESIAN_POINT ( 'NONE',  ( 26.56758885001203652, -2.317900097157796324, 5.783357778048657138 ) ) ;
#6242=CARTESIAN_POINT ( 'NONE',  ( 32.91278983782564183, -5.325448745358647429, 3.627061608673662896 ) ) ;
#6243=CARTESIAN_POINT ( 'NONE',  ( 0.000000000000000000, 0.000000000000000000, 12.00000000000000000 ) ) ;
#6247=CARTESIAN_POINT ( 'NONE',  ( 29.07687923786957285, -2.352938776424351008, 4.533357778048667797 ) ) ;
#6249=CARTESIAN_POINT ( 'NONE',  ( 16.03720890403358013, 12.19600435288735341, 16.13737481314213440 ) ) ;
#6252=CARTESIAN_POINT ( 'NONE',  ( 21.42418217458643070, -10.16661967303011771, 15.24537580551290183 ) ) ;
#6253=EDGE_CURVE ( 'NONE', #4537, #5547, #7768, .T. ) ;
#6262=ORIENTED_EDGE ( 'NONE', *, *, #10328, .F. ) ;
#6271=EDGE_CURVE ( 'NONE', #4942, #172, #1739, .T. ) ;
#6277=CARTESIAN_POINT ( 'NONE',  ( 14.00000000000000178, -1.714505518806294835E-15, 8.700000000000001066 ) ) ;
#6284=DIRECTION ( 'NONE',  ( 0.000000000000000000, 0.000000000000000000, 1.000000000000000000 ) ) ;
#6286=CARTESIAN_POINT ( 'NONE',  ( -5.500000000000000888, -20.49999999999999645, 13.00000000000000178 ) ) ;
#6292=CARTESIAN_POINT ( 'NONE',  ( 30.09392748191118017, -6.591845302810410701, 4.533357778048659803 ) ) ;
#6295=DIRECTION ( 'NONE',  ( -0.1196152422706621143, -0.9928203230275509661, -0.000000000000000000 ) ) ;
#6298=DIRECTION ( 'NONE',  ( 0.9928203230275512992, 0.1196152422706610180, 4.006172263299093133E-17 ) ) ;
#6300=CARTESIAN_POINT ( 'NONE',  ( 45.50000000000000000, -19.03270077640483038, 5.537981825772250843 ) ) ;
#6302=CARTESIAN_POINT ( 'NONE',  ( 33.59503905791412137, -1.808589744724287129, 7.033357778048666020 ) ) ;
#6303=EDGE_CURVE ( 'NONE', #9649, #3432, #10695, .T. ) ;
#6306=CARTESIAN_POINT ( 'NONE',  ( 26.30054492745255246, -7.259773351106303174, 6.331581338229590017 ) ) ;
#6308=CARTESIAN_POINT ( 'NONE',  ( 32.93018312783485158, -2.815471066132994249, 7.939653947423664704 ) ) ;
#6312=VERTEX_POINT ( 'NONE', #10807 ) ;
#6317=AXIS2_PLACEMENT_3D ( 'NONE', #9059, #7523, #11678 ) ;
#6322=DIRECTION ( 'NONE',  ( -0.9928203230275512992, -0.1196152422706610180, -4.006172263299093133E-17 ) ) ;
#6323=CARTESIAN_POINT ( 'NONE',  ( 31.51612863268893960, -4.239777773060436239, 8.283357778048662468 ) ) ;
#6325=ORIENTED_EDGE ( 'NONE', *, *, #3962, .T. ) ;
#6326=ORIENTED_EDGE ( 'NONE', *, *, #9588, .F. ) ;
#6327=AXIS2_PLACEMENT_3D ( 'NONE', #5225, #16404, #3886 ) ;
#6330=CARTESIAN_POINT ( 'NONE',  ( 26.23609683341064525, -2.995005734021441768, 4.705209693361167567 ) ) ;
#6332=CARTESIAN_POINT ( 'NONE',  ( 33.54323074294813267, -5.249493066516778050, 3.627061608673662896 ) ) ;
#6337=CARTESIAN_POINT ( 'NONE',  ( 29.35089333861488115, -5.954459450865362768, 3.283357778048663356 ) ) ;
#6341=CARTESIAN_POINT ( 'NONE',  ( -2.749999999999988454, -20.49999999999999645, 13.00000000000000355 ) ) ;
#6351=AXIS2_PLACEMENT_3D ( 'NONE', #14293, #7748, #2235 ) ;
#6355=EDGE_CURVE ( 'NONE', #5547, #4193, #7218, .T. ) ;
#6358=DIRECTION ( 'NONE',  ( -0.000000000000000000, -0.000000000000000000, -1.000000000000000000 ) ) ;
#6364=VECTOR ( 'NONE', #2304, 1000.000000000000227 ) ;
#6370=AXIS2_PLACEMENT_3D ( 'NONE', #11468, #14309, #4325 ) ;
#6372=EDGE_CURVE ( 'NONE', #4560, #14000, #17679, .T. ) ;
#6374=PLANE ( 'NONE',  #4843 ) ;
#6378=ORIENTED_EDGE ( 'NONE', *, *, #6, .F. ) ;
#6379=CARTESIAN_POINT ( 'NONE',  ( 33.95908713831674675, -3.945449517755637903, 5.783357778048663356 ) ) ;
#6381=ORIENTED_EDGE ( 'NONE', *, *, #7718, .F. ) ;
#6382=VECTOR ( 'NONE', #743, 1000.000000000000000 ) ;
#6384=CARTESIAN_POINT ( 'NONE',  ( 29.79859849048667897, -1.928627242885762705, 5.783357778048662468 ) ) ;
#6385=EDGE_CURVE ( 'NONE', #825, #16104, #13813, .T. ) ;
#6387=DIRECTION ( 'NONE',  ( 0.7999999999999999334, -0.6000000000000001998, 0.000000000000000000 ) ) ;
#6391=CYLINDRICAL_SURFACE ( 'NONE', #15852, 2.500000000000001776 ) ;
#6395=CARTESIAN_POINT ( 'NONE',  ( 27.02867472334902033, -6.034368414549446058, 7.939653947423658487 ) ) ;
#6396=EDGE_LOOP ( 'NONE', ( #7632, #1696, #7456, #17026 ) ) ;
#6399=ADVANCED_FACE ( 'NONE', ( #1588 ), #3118, .T. ) ;
#6401=CARTESIAN_POINT ( 'NONE',  ( 28.93739072872572393, -3.296523698798161650, 3.627061608673666893 ) ) ;
#6402=CARTESIAN_POINT ( 'NONE',  ( -25.76257153370368869, -10.59741316493651730, 14.29454127969954591 ) ) ;
#6405=ORIENTED_EDGE ( 'NONE', *, *, #738, .F. ) ;
#6409=DIRECTION ( 'NONE',  ( -0.9928203230275512992, -0.1196152422706610180, -4.006172263299093133E-17 ) ) ;
#6412=VECTOR ( 'NONE', #7305, 999.9999999999998863 ) ;
#6421=CARTESIAN_POINT ( 'NONE',  ( 26.90793483298706690, -6.248787706170159773, 3.283357778048663800 ) ) ;
#6423=VERTEX_POINT ( 'NONE', #11154 ) ;
#6427=CARTESIAN_POINT ( 'NONE',  ( 26.66961417369883591, -4.823687054261037055, 7.939653947423662039 ) ) ;
#6428=CARTESIAN_POINT ( 'NONE',  ( 7.499998387031003411, -20.49508120620799900, 17.00000000000000000 ) ) ;
#6440=CARTESIAN_POINT ( 'NONE',  ( 17.59269349951685157, -13.05689734314391970, 15.91118832497637570 ) ) ;
#6442=AXIS2_PLACEMENT_3D ( 'NONE', #2305, #750, #7996 ) ;
#6446=VERTEX_POINT ( 'NONE', #15263 ) ;
#6447=( BOUNDED_CURVE ( )  B_SPLINE_CURVE ( 2, ( #1426, #3799, #5138, #8046, #6685, #13584, #1166, #5314, #12219 ),
 .UNSPECIFIED., .F., .T. ) 
 B_SPLINE_CURVE_WITH_KNOTS ( ( 3, 2, 2, 2, 3 ),
 ( 0.3653846153846154188, 0.3717948717948718063, 0.3846153846153846367, 0.3974358974358974117, 0.4038461538461538547 ),
 .UNSPECIFIED. ) 
 CURVE ( )  GEOMETRIC_REPRESENTATION_ITEM ( )  RATIONAL_B_SPLINE_CURVE ( ( 0.9330127018922194093, 0.9330127018922196314, 1.000000000000000000, 0.8660254037844387076, 1.000000000000000000, 0.8660254037844387076, 1.000000000000000000, 0.9330127018922190762, 0.9330127018922194093 ) ) 
 REPRESENTATION_ITEM ( '' )  );
#6452=CARTESIAN_POINT ( 'NONE',  ( 26.01652455409633902, -4.902371455920926380, 5.783357778048663356 ) ) ;
#6459=CARTESIAN_POINT ( 'NONE',  ( 25.83973938098743162, -3.435034105423888207, 7.359589145280891032 ) ) ;
#6464=EDGE_CURVE ( 'NONE', #6423, #6659, #3208, .T. ) ;
#6467=LINE ( 'NONE', #6628, #12208 ) ;
#6473=ORIENTED_EDGE ( 'NONE', *, *, #1159, .T. ) ;
#6474=AXIS2_PLACEMENT_3D ( 'NONE', #16581, #5410, #4066 ) ;
#6477=CARTESIAN_POINT ( 'NONE',  ( 30.42903939560917337, -1.852671564043892660, 5.783357778048667797 ) ) ;
#6480=CARTESIAN_POINT ( 'NONE',  ( 0.000000000000000000, 0.000000000000000000, 10.50000000000000000 ) ) ;
#6483=EDGE_CURVE ( 'NONE', #2940, #11624, #8279, .T. ) ;
#6487=CYLINDRICAL_SURFACE ( 'NONE', #2863, 95.00000000000000000 ) ;
#6491=CARTESIAN_POINT ( 'NONE',  ( 32.93004296264515318, -25.68697430340742471, 12.29384923381407546 ) ) ;
#6492=CARTESIAN_POINT ( 'NONE',  ( 27.75966235412334981, -2.811446176820259879, 6.861505862736166250 ) ) ;
#6494=CARTESIAN_POINT ( 'NONE',  ( 30.82871344409320713, -3.068656662272551738, 3.627061608673666893 ) ) ;
#6495=CARTESIAN_POINT ( 'NONE',  ( -27.94356719068602146, -12.38857420186734970, 13.73436385264702153 ) ) ;
#6506=CARTESIAN_POINT ( 'NONE',  ( 27.09860475545177039, -3.518061095420291995, 7.939653947423664704 ) ) ;
#6513=CARTESIAN_POINT ( 'NONE',  ( 27.73348320195396965, -4.695511846111656062, 8.283357778048662468 ) ) ;
#6516=ORIENTED_EDGE ( 'NONE', *, *, #10213, .T. ) ;
#6517=CARTESIAN_POINT ( 'NONE',  ( 32.56242593318007295, -2.859778545457410281, 3.627061608673666893 ) ) ;
#6518=CARTESIAN_POINT ( 'NONE',  ( 30.81132015408399027, -5.578634341498224458, 7.939653947423658487 ) ) ;
#6520=SURFACE_STYLE_FILL_AREA ( #10307 ) ;
#6521=DIRECTION ( 'NONE',  ( 0.000000000000000000, 1.000000000000000000, -0.000000000000000000 ) ) ;
#6522=DIRECTION ( 'NONE',  ( 0.1195020427801297691, -0.9918807541847894926, -0.04349518650597276187 ) ) ;
#6524=CARTESIAN_POINT ( 'NONE',  ( 30.40162818048570514, -5.827866652795590241, 8.283357778048660691 ) ) ;
#6525=DIRECTION ( 'NONE',  ( 0.000000000000000000, 0.000000000000000000, -1.000000000000000000 ) ) ;
#6529=EDGE_CURVE ( 'NONE', #10739, #13209, #5255, .T. ) ;
#6538=CARTESIAN_POINT ( 'NONE',  ( 33.40754056521197413, -5.892811586081919906, 4.705209693361160461 ) ) ;
#6542=FACE_OUTER_BOUND ( 'NONE', #13460, .T. ) ;
#6544=ORIENTED_EDGE ( 'NONE', *, *, #7732, .F. ) ;
#6556=CARTESIAN_POINT ( 'NONE',  ( 9.099998387031005720, -19.29508120620799971, 16.81964500401478091 ) ) ;
#6558=DIRECTION ( 'NONE',  ( 0.000000000000000000, 0.000000000000000000, -1.000000000000000000 ) ) ;
#6561=DIRECTION ( 'NONE',  ( -0.000000000000000000, -0.000000000000000000, 1.000000000000000000 ) ) ;
#6566=CARTESIAN_POINT ( 'NONE',  ( 33.79776779778399032, -6.145605689821873163, 4.533357778048659803 ) ) ;
#6568=ORIENTED_EDGE ( 'NONE', *, *, #5656, .F. ) ;
#6571=CARTESIAN_POINT ( 'NONE',  ( 28.71854711534694715, -4.576831098024959132, 7.939653947423662039 ) ) ;
#6573=CARTESIAN_POINT ( 'NONE',  ( 17.71310509092289465, -19.55788671310905613, 15.89250038334901305 ) ) ;
#6574=ADVANCED_FACE ( 'NONE', ( #11531 ), #13181, .F. ) ;
#6577=CARTESIAN_POINT ( 'NONE',  ( -25.11802603177690330, -19.03270077640483038, 0.5379818257722508434 ) ) ;
#6583=CARTESIAN_POINT ( 'NONE',  ( 33.23365877489121090, -6.550928303235100891, 5.783357778048664244 ) ) ;
#6584=ORIENTED_EDGE ( 'NONE', *, *, #7690, .F. ) ;
#6586=CARTESIAN_POINT ( 'NONE',  ( 23.00000000000000000, -16.21813761408365195, 13.00000000000000178 ) ) ;
#6587=CARTESIAN_POINT ( 'NONE',  ( 28.13873763417254992, -3.192873105281056390, 8.283357778048664244 ) ) ;
#6592=CARTESIAN_POINT ( 'NONE',  ( 31.49429780130001433, -5.496349022752856861, 3.627061608673662896 ) ) ;
#6593=DIRECTION ( 'NONE',  ( 0.9928203230275511881, 0.1196152422706614482, 0.000000000000000000 ) ) ;
#6594=CARTESIAN_POINT ( 'NONE',  ( 29.97942892559193950, -4.424919740341219487, 7.939653947423662039 ) ) ;
#6600=CARTESIAN_POINT ( 'NONE',  ( 30.60493568430522160, -6.867637522466304212, 6.453230759126467042 ) ) ;
#6602=CARTESIAN_POINT ( 'NONE',  ( 31.83134908525019213, -4.201799933639492224, 3.283357778048664244 ) ) ;
#6603=CARTESIAN_POINT ( 'NONE',  ( 20.00000000000000355, 7.999999999999996447, 6.000000000000000000 ) ) ;
#6605=ADVANCED_FACE ( 'NONE', ( #7473, #17100 ), #12996, .T. ) ;
#6615=EDGE_LOOP ( 'NONE', ( #16898, #11139, #4322, #2199 ) ) ;
#6616=CARTESIAN_POINT ( 'NONE',  ( 32.34358231980129261, -4.140085944684206432, 7.939653947423662039 ) ) ;
#6620=DIRECTION ( 'NONE',  ( 0.000000000000000000, 0.000000000000000000, 1.000000000000000000 ) ) ;
#6622=VECTOR ( 'NONE', #17939, 1000.000000000000000 ) ;
#6625=EDGE_CURVE ( 'NONE', #6841, #14073, #15710, .T. ) ;
#6628=CARTESIAN_POINT ( 'NONE',  ( 14.00000000000000178, -1.714505518806294835E-15, 8.700000000000001066 ) ) ;
#6631=VERTEX_POINT ( 'NONE', #15906 ) ;
#6635=VECTOR ( 'NONE', #17714, 1000.000000000000114 ) ;
#6641=CIRCLE ( 'NONE', #8685, 5.000000000000000000 ) ;
#6643=( BOUNDED_CURVE ( )  B_SPLINE_CURVE ( 2, ( #7612, #4964, #13137, #10305, #6050, #15861, #716, #17333, #6241 ),
 .UNSPECIFIED., .F., .T. ) 
 B_SPLINE_CURVE_WITH_KNOTS ( ( 3, 2, 2, 2, 3 ),
 ( 0.8269230769230769829, 0.8333333333333333703, 0.8461538461538461453, 0.8589743589743589203, 0.8653846153846154188 ),
 .UNSPECIFIED. ) 
 CURVE ( )  GEOMETRIC_REPRESENTATION_ITEM ( )  RATIONAL_B_SPLINE_CURVE ( ( 0.9330127018922192983, 0.9330127018922198534, 1.000000000000000000, 0.8660254037844387076, 1.000000000000000000, 0.8660254037844387076, 1.000000000000000000, 0.9330127018922187432, 0.9330127018922192983 ) ) 
 REPRESENTATION_ITEM ( '' )  );
#6652=CARTESIAN_POINT ( 'NONE',  ( 32.92339180097568629, -5.524043937428110063, 8.283357778048658915 ) ) ;
#6654=VECTOR ( 'NONE', #46, 1000.000000000000000 ) ;
#6656=CARTESIAN_POINT ( 'NONE',  ( 29.03376756790819613, -4.538853258604016006, 3.627061608673664228 ) ) ;
#6657=FACE_OUTER_BOUND ( 'NONE', #8161, .T. ) ;
#6658=CARTESIAN_POINT ( 'NONE',  ( 16.75000000000000000, -16.21813761408365195, 16.03574476417184513 ) ) ;
#6659=VERTEX_POINT ( 'NONE', #16005 ) ;
#6662=DIRECTION ( 'NONE',  ( 0.000000000000000000, 0.000000000000000000, -1.000000000000000000 ) ) ;
#6671=CARTESIAN_POINT ( 'NONE',  ( 27.30005507882132676, -4.747731375419166788, 7.939653947423662039 ) ) ;
#6672=CARTESIAN_POINT ( 'NONE',  ( 29.36638131047866196, -1.990897739957422807, 5.783357778048668685 ) ) ;
#6674=CARTESIAN_POINT ( 'NONE',  ( 20.25000000000001066, -16.21813761408365195, 13.00000000000000355 ) ) ;
#6675=CARTESIAN_POINT ( 'NONE',  ( 32.24155699611449677, -1.634298987580965923, 5.783357778048662468 ) ) ;
#6676=CARTESIAN_POINT ( 'NONE',  ( 32.18597209352066812, -4.159074864394664672, 3.627061608673664228 ) ) ;
#6678=CARTESIAN_POINT ( 'NONE',  ( 28.55903157092087952, -3.142235986053133256, 3.283357778048666464 ) ) ;
#6679=ORIENTED_EDGE ( 'NONE', *, *, #7482, .T. ) ;
#6681=CARTESIAN_POINT ( 'NONE',  ( 33.30246708102489350, -5.905470865888903020, 6.861505862736158257 ) ) ;
#6683=CARTESIAN_POINT ( 'NONE',  ( 29.55043834383900148, -5.730545699181964991, 7.939653947423658487 ) ) ;
#6685=CARTESIAN_POINT ( 'NONE',  ( 30.25524682244395436, -4.391689130744175884, 8.283357778048662468 ) ) ;
#6687=CARTESIAN_POINT ( 'NONE',  ( -2.016448651773435938E-27, -20.49999999999999645, 12.00000000000000000 ) ) ;
#6694=CARTESIAN_POINT ( 'NONE',  ( 28.68570264635560463, -13.61469575198669624, 13.53129406029897730 ) ) ;
#6695=AXIS2_PLACEMENT_3D ( 'NONE', #15042, #6701, #16498 ) ;
#6696=EDGE_CURVE ( 'NONE', #4963, #16104, #4614, .T. ) ;
#6699=CARTESIAN_POINT ( 'NONE',  ( 31.15208055228630357, -2.102918000029084578, 7.033357778048666020 ) ) ;
#6701=DIRECTION ( 'NONE',  ( -0.000000000000000000, -0.000000000000000000, -1.000000000000000000 ) ) ;
#6704=CARTESIAN_POINT ( 'NONE',  ( 30.45225960443380231, -4.367952981209816343, 7.939653947423662039 ) ) ;
#6711=VECTOR ( 'NONE', #832, 1000.000000000000000 ) ;
#6717=CARTESIAN_POINT ( 'NONE',  ( 33.95908713831674675, -3.945449517755637903, 5.783357778048663356 ) ) ;
#6718=CARTESIAN_POINT ( 'NONE',  ( 30.58169613980036772, -2.898544849976259385, 8.283357778048666020 ) ) ;
#6725=EDGE_CURVE ( 'NONE', #15379, #13857, #3909, .T. ) ;
#6729=CARTESIAN_POINT ( 'NONE',  ( 25.80383423833348999, -3.137017275366889457, 4.425119566059311893 ) ) ;
#6730=VERTEX_POINT ( 'NONE', #17815 ) ;
#6733=FACE_OUTER_BOUND ( 'NONE', #14725, .T. ) ;
#6739=CARTESIAN_POINT ( 'NONE',  ( 31.59864285835955400, -2.049116061056871274, 4.533357778048667797 ) ) ;
#6743=ORIENTED_EDGE ( 'NONE', *, *, #4901, .T. ) ;
#6744=CARTESIAN_POINT ( 'NONE',  ( 30.07408527595748282, -27.82894256842317660, 13.18310524188698452 ) ) ;
#6747=AXIS2_PLACEMENT_3D ( 'NONE', #6379, #13457, #10537 ) ;
#6751=CARTESIAN_POINT ( 'NONE',  ( 29.76058531221316628, -5.705227139567997874, 3.627061608673662896 ) ) ;
#6752=DIRECTION ( 'NONE',  ( -0.5999999999999999778, -0.7999999999999999334, -0.000000000000000000 ) ) ;
#6753=CARTESIAN_POINT ( 'NONE',  ( 25.01460733971720529, -22.13799366862516038, 14.47321228143779415 ) ) ;
#6755=DIRECTION ( 'NONE',  ( -1.000000000000000000, 0.000000000000000000, 0.000000000000000000 ) ) ;
#6757=FACE_OUTER_BOUND ( 'NONE', #5954, .T. ) ;
#6763=CARTESIAN_POINT ( 'NONE',  ( 26.56758885001203652, -2.317900097157796324, 5.783357778048657138 ) ) ;
#6765=CARTESIAN_POINT ( 'NONE',  ( 32.41296236253129592, -1.951006642345344044, 7.033357778048666020 ) ) ;
#6766=CARTESIAN_POINT ( 'NONE',  ( 30.15026255541241440, -6.285249260098253465, 6.861505862736158257 ) ) ;
#6767=EDGE_CURVE ( 'NONE', #8284, #15182, #17092, .T. ) ;
#6770=DIRECTION ( 'NONE',  ( -0.000000000000000000, -1.000000000000000000, 3.469446951953614189E-16 ) ) ;
#6773=CARTESIAN_POINT ( 'NONE',  ( 31.93198502805756789, -2.935734224299280548, 3.627061608673666893 ) ) ;
#6776=CARTESIAN_POINT ( 'NONE',  ( 28.91999743871649997, -5.806501378023834370, 7.939653947423658487 ) ) ;
#6778=FACE_BOUND ( 'NONE', #3110, .T. ) ;
#6779=FACE_OUTER_BOUND ( 'NONE', #4172, .T. ) ;
#6784=DIRECTION ( 'NONE',  ( 0.9928203230275511881, 0.1196152422706614482, 0.000000000000000000 ) ) ;
#6790=EDGE_LOOP ( 'NONE', ( #1976, #15935, #560, #14603 ) ) ;
#6791=EDGE_CURVE ( 'NONE', #11389, #2070, #16686, .T. ) ;
#6799=CARTESIAN_POINT ( 'NONE',  ( 33.38562051666750818, -5.268481986227246949, 3.627061608673662896 ) ) ;
#6803=CARTESIAN_POINT ( 'NONE',  ( 27.87912141988533676, -2.159886323212414361, 5.113484796970856117 ) ) ;
#6817=LINE ( 'NONE', #12342, #3426 ) ;
#6825=CARTESIAN_POINT ( 'NONE',  ( 20.00000000000000355, 7.999999999999996447, 6.000000000000000000 ) ) ;
#6829=CARTESIAN_POINT ( 'NONE',  ( 31.90644508241650357, -6.373472726347483963, 4.533357778048659803 ) ) ;
#6833=CARTESIAN_POINT ( 'NONE',  ( 26.63030083514515312, -6.709335133632020387, 4.705209693361159573 ) ) ;
#6836=ORIENTED_EDGE ( 'NONE', *, *, #16676, .T. ) ;
#6837=CARTESIAN_POINT ( 'NONE',  ( 28.52524344760924180, -2.419399995203538101, 4.533357778048667797 ) ) ;
#6838=VERTEX_POINT ( 'NONE', #8703 ) ;
#6840=EDGE_CURVE ( 'NONE', #6841, #9483, #3262, .T. ) ;
#6841=VERTEX_POINT ( 'NONE', #12955 ) ;
#6844=PRODUCT_DEFINITION_CONTEXT ( 'detailed design', #15714, 'design' ) ;
#6845=CARTESIAN_POINT ( 'NONE',  ( -25.11802603177690330, -19.03270077640483038, 0.5379818257722508434 ) ) ;
#6846=DIRECTION ( 'NONE',  ( 1.000000000000000000, 0.000000000000000000, 0.000000000000000000 ) ) ;
#6848=CARTESIAN_POINT ( 'NONE',  ( 26.36761712467744090, -6.740983333149474177, 6.861505862736158257 ) ) ;
#6850=CARTESIAN_POINT ( 'NONE',  ( 30.86385689617752348, -5.572304701594726239, 3.627061608673662896 ) ) ;
#6853=DIRECTION ( 'NONE',  ( -1.000000000000000000, 0.000000000000000000, 0.000000000000000000 ) ) ;
#6854=VERTEX_POINT ( 'NONE', #13045 ) ;
#6858=CARTESIAN_POINT ( 'NONE',  ( 30.76748005699505129, -4.329975141788874993, 3.627061608673664228 ) ) ;
#6859=LINE ( 'NONE', #12385, #14843 ) ;
#6861=CARTESIAN_POINT ( 'NONE',  ( 29.02054416436834217, -2.659534819136519790, 6.861505862736166250 ) ) ;
#6869=CARTESIAN_POINT ( 'NONE',  ( 29.20802265909081896, -15.38590642643731066, 13.38453386482100171 ) ) ;
#6874=CARTESIAN_POINT ( 'NONE',  ( -5.500000000000000000, -20.49999999999999645, 6.000000000000000000 ) ) ;
#6880=CARTESIAN_POINT ( 'NONE',  ( 31.28415083292585663, -5.521667582366822202, 7.939653947423658487 ) ) ;
#6882=CARTESIAN_POINT ( 'NONE',  ( 32.96626681528915981, -4.065064760026301016, 5.783357778048663356 ) ) ;
#6883=CARTESIAN_POINT ( 'NONE',  ( -20.25000000000000711, -16.21813761408365195, 13.00000000000000178 ) ) ;
#6884=EDGE_CURVE ( 'NONE', #9143, #2135, #13607, .T. ) ;
#6888=CARTESIAN_POINT ( 'NONE',  ( 32.46178999037268653, -4.125844254797621957, 3.283357778048664244 ) ) ;
#6892=AXIS2_PLACEMENT_3D ( 'NONE', #16095, #13780, #7737 ) ;
#6900=EDGE_CURVE ( 'NONE', #4898, #16224, #4522, .T. ) ;
#6907=ORIENTED_EDGE ( 'NONE', *, *, #1216, .T. ) ;
#6914=CARTESIAN_POINT ( 'NONE',  ( 32.51061761821408425, -6.300681867249914525, 7.033357778048657138 ) ) ;
#6916=VECTOR ( 'NONE', #13904, 1000.000000000000000 ) ;
#6920=CARTESIAN_POINT ( 'NONE',  ( 27.26074174026764751, -6.633379454790151009, 4.705209693361159573 ) ) ;
#6921=CARTESIAN_POINT ( 'NONE',  ( 17.31832318566733164, -18.83027996791590652, 15.95242868103980172 ) ) ;
#6922=ADVANCED_FACE ( 'NONE', ( #1998 ), #11298, .T. ) ;
#6924=CARTESIAN_POINT ( 'NONE',  ( 30.98067518586950442, -1.786210345264705790, 5.783357778048667797 ) ) ;
#6926=CIRCLE ( 'NONE', #5465, 2.749999999999988454 ) ;
#6934=CARTESIAN_POINT ( 'NONE',  ( 33.79776779778399032, -6.145605689821873163, 4.533357778048659803 ) ) ;
#6935=AXIS2_PLACEMENT_3D ( 'NONE', #1410, #5564, #6846 ) ;
#6936=CARTESIAN_POINT ( 'NONE',  ( 28.24571643650507369, -4.633797857156355171, 3.627061608673664228 ) ) ;
#6937=CARTESIAN_POINT ( 'NONE',  ( 19.43845002722867221, 2.988003976273734263, 0.000000000000000000 ) ) ;
#6939=CARTESIAN_POINT ( 'NONE',  ( 32.17274868998081416, -2.279756424927169345, 6.861505862736166250 ) ) ;
#6944=CARTESIAN_POINT ( 'NONE',  ( 28.97253418081003673, -5.800171738120336151, 3.627061608673662896 ) ) ;
#6948=CARTESIAN_POINT ( 'NONE',  ( 27.28266178881210280, -7.257709054644825741, 5.783357778048657138 ) ) ;
#6949=ADVANCED_FACE ( 'NONE', ( #5783 ), #17056, .F. ) ;
#6950=EDGE_LOOP ( 'NONE', ( #4645, #16916, #17348, #673 ) ) ;
#6956=VECTOR ( 'NONE', #8820, 1000.000000000000000 ) ;
#6961=CARTESIAN_POINT ( 'NONE',  ( 24.63290760229943643, -10.17177306796459035, 14.56289668145355698 ) ) ;
#6971=EDGE_CURVE ( 'NONE', #8875, #10810, #6926, .T. ) ;
#6974=ORIENTED_EDGE ( 'NONE', *, *, #7118, .T. ) ;
#6975=CARTESIAN_POINT ( 'NONE',  ( 27.51889869220010354, -3.467423976192371526, 3.627061608673666449 ) ) ;
#6978=CARTESIAN_POINT ( 'NONE',  ( 30.88568772756644520, -4.315733451902305617, 8.283357778048662468 ) ) ;
#6991=DIRECTION ( 'NONE',  ( -0.000000000000000000, -0.000000000000000000, -1.000000000000000000 ) ) ;
#6994=CARTESIAN_POINT ( 'NONE',  ( 32.38298487551052318, -4.135338714860305132, 3.283357778048664244 ) ) ;
#6997=AXIS2_PLACEMENT_3D ( 'NONE', #7328, #11464, #17030 ) ;
#7001=FACE_OUTER_BOUND ( 'NONE', #13560, .T. ) ;
#7002=VECTOR ( 'NONE', #17343, 1000.000000000000114 ) ;
#7008=ADVANCED_FACE ( 'NONE', ( #1074 ), #3801, .F. ) ;
#7019=ORIENTED_EDGE ( 'NONE', *, *, #2742, .T. ) ;
#7020=EDGE_CURVE ( 'NONE', #10514, #9531, #13993, .T. ) ;
#7021=LINE ( 'NONE', #12541, #5126 ) ;
#7024=CARTESIAN_POINT ( 'NONE',  ( 26.63392073224175505, -2.647267031729148012, 4.533357778048667797 ) ) ;
#7026=AXIS2_PLACEMENT_3D ( 'NONE', #17125, #151, #12929 ) ;
#7028=CARTESIAN_POINT ( 'NONE',  ( 27.28266178881210280, -7.257709054644824853, 5.783357778048657138 ) ) ;
#7029=CARTESIAN_POINT ( 'NONE',  ( -17.08586189024356727, -18.24992599651649527, 15.98693133205340189 ) ) ;
#7044=CARTESIAN_POINT ( 'NONE',  ( 33.76397967447234549, -5.422769698972272678, 3.283357778048663356 ) ) ;
#7045=CARTESIAN_POINT ( 'NONE',  ( 30.04066231269008469, -3.163601260824890904, 3.627061608673666893 ) ) ;
#7047=FACE_OUTER_BOUND ( 'NONE', #4148, .T. ) ;
#7049=CARTESIAN_POINT ( 'NONE',  ( 28.39010325924584421, -2.735490497978389612, 6.861505862736166250 ) ) ;
#7051=ORIENTED_EDGE ( 'NONE', *, *, #4540, .F. ) ;
#7052=CARTESIAN_POINT ( 'NONE',  ( 28.56093688906631911, -4.595820017735426255, 7.939653947423662039 ) ) ;
#7054=CARTESIAN_POINT ( 'NONE',  ( -50.00000000000000000, -16.03270077640482683, 5.537981825772250843 ) ) ;
#7056=CARTESIAN_POINT ( 'NONE',  ( 30.69058026372202974, -5.793053633118939061, 3.283357778048663356 ) ) ;
#7074=VECTOR ( 'NONE', #3683, 1000.000000000000000 ) ;
#7076=VERTEX_POINT ( 'NONE', #5057 ) ;
#7078=CARTESIAN_POINT ( 'NONE',  ( 29.36638131047866906, -1.990897739957422807, 5.783357778048668685 ) ) ;
#7085=DIRECTION ( 'NONE',  ( -0.1196152422706610735, 0.9928203230275511881, 0.000000000000000000 ) ) ;
#7086=EDGE_CURVE ( 'NONE', #15383, #12849, #10577, .T. ) ;
#7093=EDGE_CURVE ( 'NONE', #1236, #9636, #1731, .T. ) ;
#7095=CARTESIAN_POINT ( 'NONE',  ( 30.93441382992541477, -1.402235749049144609, 5.783357778048668685 ) ) ;
#7098=ORIENTED_EDGE ( 'NONE', *, *, #9184, .F. ) ;
#7117=CARTESIAN_POINT ( 'NONE',  ( 32.67202617590239555, -5.981426544730773287, 6.861505862736158257 ) ) ;
#7118=EDGE_CURVE ( 'NONE', #11071, #17243, #9655, .T. ) ;
#7119=CARTESIAN_POINT ( 'NONE',  ( 26.60838078660069428, -6.085005533777348319, 3.627061608673662896 ) ) ;
#7120=CARTESIAN_POINT ( 'NONE',  ( -27.94765010173961883, -20.05889348609997924, 13.73347386810006832 ) ) ;
#7121=DIRECTION ( 'NONE',  ( -0.1196152422706611151, 0.9928203230275511881, 0.000000000000000000 ) ) ;
#7124=VERTEX_POINT ( 'NONE', #11099 ) ;
#7125=CARTESIAN_POINT ( 'NONE',  ( 26.95740407890011170, -7.307093047852763590, 5.113484796970857005 ) ) ;
#7126=ADVANCED_FACE ( 'NONE', ( #157 ), #5670, .T. ) ;
#7128=FACE_OUTER_BOUND ( 'NONE', #12946, .T. ) ;
#7131=CARTESIAN_POINT ( 'NONE',  ( -5.499998387031001634, -20.49508120620799900, 6.000000000000000000 ) ) ;
#7137=CARTESIAN_POINT ( 'NONE',  ( 29.97942892559193950, -4.424919740341219487, 7.939653947423662039 ) ) ;
#7142=CARTESIAN_POINT ( 'NONE',  ( 28.99445422935450267, -6.424501337975009996, 4.705209693361160461 ) ) ;
#7146=CARTESIAN_POINT ( 'NONE',  ( 27.26074174026764751, -6.633379454790151009, 4.705209693361159573 ) ) ;
#7148=ORIENTED_EDGE ( 'NONE', *, *, #17475, .T. ) ;
#7155=DIRECTION ( 'NONE',  ( 0.000000000000000000, 0.000000000000000000, 1.000000000000000000 ) ) ;
#7162=ADVANCED_FACE ( 'NONE', ( #6779 ), #5400, .F. ) ;
#7164=CIRCLE ( 'NONE', #13527, 2.500000000000001776 ) ;
#7167=CARTESIAN_POINT ( 'NONE',  ( 27.73357241910951743, -6.576412695658750529, 4.705209693361160461 ) ) ;
#7171=VECTOR ( 'NONE', #11339, 1000.000000000000114 ) ;
#7176=DIRECTION ( 'NONE',  ( -1.000000000000000000, 0.000000000000000000, 0.000000000000000000 ) ) ;
#7179=LINE ( 'NONE', #12687, #12831 ) ;
#7182=CARTESIAN_POINT ( 'NONE',  ( 23.00000000000000000, -16.21813761408365195, 13.00000000000000178 ) ) ;
#7186=CARTESIAN_POINT ( 'NONE',  ( 32.85952466860454280, -1.897204703373130741, 4.533357778048667797 ) ) ;
#7188=EDGE_CURVE ( 'NONE', #7756, #3522, #12577, .T. ) ;
#7194=ADVANCED_FACE ( 'NONE', ( #14944 ), #8048, .T. ) ;
#7199=CARTESIAN_POINT ( 'NONE',  ( -36.27615609941022257, -23.17738945083361202, 11.07596365154449636 ) ) ;
#7201=ORIENTED_EDGE ( 'NONE', *, *, #6767, .T. ) ;
#7205=ORIENTED_EDGE ( 'NONE', *, *, #12952, .F. ) ;
#7206=CARTESIAN_POINT ( 'NONE',  ( 32.97402322492378346, -4.064130265842336165, 7.939653947423662039 ) ) ;
#7209=CARTESIAN_POINT ( 'NONE',  ( 25.93489015466116854, -5.606035894254070229, 3.627061608673662896 ) ) ;
#7210=CARTESIAN_POINT ( 'NONE',  ( 29.32081432955537537, -3.050456207659999475, 8.283357778048666020 ) ) ;
#7212=CARTESIAN_POINT ( 'NONE',  ( 28.82057243903374655, -7.082618055128190093, 5.783357778048657138 ) ) ;
#7215=EDGE_LOOP ( 'NONE', ( #5610, #8542, #14504, #7712 ) ) ;
#7218=CIRCLE ( 'NONE', #14156, 6.249999999999996447 ) ;
#7226=CARTESIAN_POINT ( 'NONE',  ( 29.02054416436834217, -2.659534819136519790, 6.861505862736166250 ) ) ;
#7230=CARTESIAN_POINT ( 'NONE',  ( 28.12741954877813555, -2.767138697495831856, 4.705209693361167567 ) ) ;
#7231=CYLINDRICAL_SURFACE ( 'NONE', #15687, 2.500000000000001776 ) ;
#7232=LINE ( 'NONE', #7054, #15408 ) ;
#7234=CARTESIAN_POINT ( 'NONE',  ( 27.77288575766320378, -4.690764616287755651, 3.627061608673664228 ) ) ;
#7246=AXIS2_PLACEMENT_3D ( 'NONE', #6577, #9129, #10292 ) ;
#7248=DIRECTION ( 'NONE',  ( 0.9928203230275512992, 0.1196152422706614482, 0.000000000000000000 ) ) ;
#7253=CARTESIAN_POINT ( 'NONE',  ( 28.23249303296521617, -2.754479417688857179, 6.861505862736165362 ) ) ;
#7255=DIRECTION ( 'NONE',  ( -1.000000000000000000, 0.000000000000000000, 0.000000000000000000 ) ) ;
#7260=DIRECTION ( 'NONE',  ( 0.7999999999999999334, 0.6000000000000000888, 0.000000000000000000 ) ) ;
#7265=EDGE_CURVE ( 'NONE', #6202, #2263, #12575, .T. ) ;
#7270=CARTESIAN_POINT ( 'NONE',  ( -2.016448651773435938E-27, -20.49999999999999645, 13.00000000000000178 ) ) ;
#7271=CARTESIAN_POINT ( 'NONE',  ( 26.61898274975073164, -6.283600725846810953, 8.283357778048660691 ) ) ;
#7274=CARTESIAN_POINT ( 'NONE',  ( 28.41265020943543362, -1.706058464416624787, 5.783357778048668685 ) ) ;
#7275=CARTESIAN_POINT ( 'NONE',  ( 26.01652455409633902, -4.902371455920926380, 5.783357778048663356 ) ) ;
#7280=DIRECTION ( 'NONE',  ( -0.000000000000000000, -0.000000000000000000, 1.000000000000000000 ) ) ;
#7285=EDGE_CURVE ( 'NONE', #14407, #8284, #8860, .T. ) ;
#7290=DIRECTION ( 'NONE',  ( -0.000000000000000000, -0.000000000000000000, 1.000000000000000000 ) ) ;
#7294=ORIENTED_EDGE ( 'NONE', *, *, #8798, .T. ) ;
#7295=CARTESIAN_POINT ( 'NONE',  ( 26.47260139170898441, -4.847423203795396596, 8.283357778048662468 ) ) ;
#7298=CARTESIAN_POINT ( 'NONE',  ( -17.70832741558421830, -19.55032950225749389, 15.89323616604937328 ) ) ;
#7300=AXIS2_PLACEMENT_3D ( 'NONE', #9931, #1428, #15481 ) ;
#7302=CARTESIAN_POINT ( 'NONE',  ( -8.632250723006722026, -18.84644399697197770, 16.84735068286508763 ) ) ;
#7305=DIRECTION ( 'NONE',  ( 0.6000000000000001998, 0.7999999999999999334, 0.000000000000000000 ) ) ;
#7319=CARTESIAN_POINT ( 'NONE',  ( 29.14000323013032556, -2.007974965528672495, 5.113484796970859669 ) ) ;
#7321=CARTESIAN_POINT ( 'NONE',  ( 29.04699097144805364, -6.418171698071525100, 6.861505862736157368 ) ) ;
#7322=ORIENTED_EDGE ( 'NONE', *, *, #10507, .F. ) ;
#7323=AXIS2_PLACEMENT_3D ( 'NONE', #8179, #13619, #4094 ) ;
#7324=CARTESIAN_POINT ( 'NONE',  ( 25.41044654184514329, -5.982623484807521486, 5.783357778048662468 ) ) ;
#7327=CARTESIAN_POINT ( 'NONE',  ( 28.13194630731337753, -5.901445976576171759, 7.939653947423658487 ) ) ;
#7328=CARTESIAN_POINT ( 'NONE',  ( -2.016448651773435938E-27, -20.49999999999999645, 13.00000000000000178 ) ) ;
#7331=CARTESIAN_POINT ( 'NONE',  ( 28.52162355051263987, -6.481468097106410475, 4.705209693361159573 ) ) ;
#7337=CARTESIAN_POINT ( 'NONE',  ( 25.90934487712385348, 0.1208734971681838660, 5.783357778048663356 ) ) ;
#7340=LINE ( 'NONE', #355, #9256 ) ;
#7345=CARTESIAN_POINT ( 'NONE',  ( 28.79241808379989465, -7.086010098929231837, 6.453230759126462601 ) ) ;
#7351=ADVANCED_FACE ( 'NONE', ( #440 ), #11377, .F. ) ;
#7352=CARTESIAN_POINT ( 'NONE',  ( 30.02326902268086428, -5.673578940050561847, 7.939653947423658487 ) ) ;
#7353=LINE ( 'NONE', #16963, #7922 ) ;
#7354=( BOUNDED_CURVE ( )  B_SPLINE_CURVE ( 2, ( #14828, #9198, #16112, #3596, #12181 ),
 .UNSPECIFIED., .F., .T. ) 
 B_SPLINE_CURVE_WITH_KNOTS ( ( 3, 2, 3 ),
 ( 0.000000000000000000, 0.01282051282051282007, 0.01923076923076925265 ),
 .UNSPECIFIED. ) 
 CURVE ( )  GEOMETRIC_REPRESENTATION_ITEM ( )  RATIONAL_B_SPLINE_CURVE ( ( 1.000000000000000000, 0.8660254037844387076, 1.000000000000000000, 0.9330127018922191873, 0.9330127018922194093 ) ) 
 REPRESENTATION_ITEM ( '' )  );
#7360=DIRECTION ( 'NONE',  ( 0.000000000000000000, 0.000000000000000000, -1.000000000000000000 ) ) ;
#7361=CARTESIAN_POINT ( 'NONE',  ( 16.75000000000000000, -16.21813761408365195, 13.00000000000000178 ) ) ;
#7363=VERTEX_POINT ( 'NONE', #10110 ) ;
#7364=AXIS2_PLACEMENT_3D ( 'NONE', #10843, #12038, #13325 ) ;
#7370=CARTESIAN_POINT ( 'NONE',  ( 29.27960797773944179, -6.689954721521948144, 7.033357778048657138 ) ) ;
#7379=ORIENTED_EDGE ( 'NONE', *, *, #12885, .T. ) ;
#7390=CARTESIAN_POINT ( 'NONE',  ( 32.54050588463559990, -2.235448945602741766, 4.705209693361167567 ) ) ;
#7391=VERTEX_POINT ( 'NONE', #14030 ) ;
#7394=LINE ( 'NONE', #129, #9833 ) ;
#7397=CARTESIAN_POINT ( 'NONE',  ( 31.05948030073166066, -1.776715885202022394, 5.783357778048665132 ) ) ;
#7398=ORIENTED_EDGE ( 'NONE', *, *, #5453, .F. ) ;
#7406=FACE_OUTER_BOUND ( 'NONE', #624, .T. ) ;
#7410=CARTESIAN_POINT ( 'NONE',  ( 30.92509028327567933, -4.310986222078405206, 3.627061608673664228 ) ) ;
#7411=ORIENTED_EDGE ( 'NONE', *, *, #6271, .T. ) ;
#7412=DIRECTION ( 'NONE',  ( 0.9928203230275510771, 0.1196152422706610596, 9.614813431917826478E-17 ) ) ;
#7413=EDGE_CURVE ( 'NONE', #2945, #14967, #10637, .T. ) ;
#7415=CARTESIAN_POINT ( 'NONE',  ( 26.36761712467744090, -6.740983333149474177, 6.861505862736158257 ) ) ;
#7416=CARTESIAN_POINT ( 'NONE',  ( -50.00000000000000000, -19.03270077640483038, 5.537981825772250843 ) ) ;
#7419=CARTESIAN_POINT ( 'NONE',  ( 45.00000000000000711, -16.03270077640482683, 10.53798182577225084 ) ) ;
#7425=DIRECTION ( 'NONE',  ( 0.9928203230275510771, 0.1196152422706609902, 4.006172263299092517E-17 ) ) ;
#7427=CARTESIAN_POINT ( 'NONE',  ( 28.13873763417255347, -3.192873105281056390, 8.283357778048666020 ) ) ;
#7428=CARTESIAN_POINT ( 'NONE',  ( 31.67744797322171735, -2.039621600994187656, 4.533357778048667797 ) ) ;
#7429=EDGE_LOOP ( 'NONE', ( #11610, #11507, #8209, #9876, #9648, #1385 ) ) ;
#7430=ADVANCED_FACE ( 'NONE', ( #4852 ), #2072, .F. ) ;
#7433=CARTESIAN_POINT ( 'NONE',  ( 31.54230778485832332, -2.355712103769039611, 6.861505862736166250 ) ) ;
#7442=CYLINDRICAL_SURFACE ( 'NONE', #11070, 2.500000000000001776 ) ;
#7444=EDGE_CURVE ( 'NONE', #4560, #14120, #9439, .T. ) ;
#7450=CARTESIAN_POINT ( 'NONE',  ( 28.51030546511822195, -6.055733689321201041, 8.283357778048658915 ) ) ;
#7451=ORIENTED_EDGE ( 'NONE', *, *, #11508, .F. ) ;
#7456=ORIENTED_EDGE ( 'NONE', *, *, #17205, .F. ) ;
#7464=FACE_OUTER_BOUND ( 'NONE', #16664, .T. ) ;
#7466=LINE ( 'NONE', #14171, #7171 ) ;
#7468=CARTESIAN_POINT ( 'NONE',  ( 32.65880277236253448, -4.102108105263264193, 3.627061608673664228 ) ) ;
#7472=DIRECTION ( 'NONE',  ( -0.9937818688019538493, -0.1113444980252557837, 0.000000000000000000 ) ) ;
#7473=FACE_BOUND ( 'NONE', #15221, .T. ) ;
#7482=EDGE_CURVE ( 'NONE', #60, #602, #11927, .T. ) ;
#7487=CARTESIAN_POINT ( 'NONE',  ( 26.31556265977298992, -7.384422263489805793, 5.783357778048663356 ) ) ;
#7489=DIRECTION ( 'NONE',  ( 0.000000000000000000, 0.000000000000000000, -1.000000000000000000 ) ) ;
#7490=CARTESIAN_POINT ( 'NONE',  ( 26.60838078660069428, -6.085005533777348319, 3.627061608673662896 ) ) ;
#7493=CARTESIAN_POINT ( 'NONE',  ( 26.31308423962587995, -7.363851090081250383, 5.766985353495324595 ) ) ;
#7495=CARTESIAN_POINT ( 'NONE',  ( 32.06767520579373354, -2.292415704734142690, 4.705209693361168455 ) ) ;
#7496=CARTESIAN_POINT ( 'NONE',  ( -24.42951923951777005, -10.13045284482685382, 14.60898600760630472 ) ) ;
#7499=CYLINDRICAL_SURFACE ( 'NONE', #10788, 2.749999999999992895 ) ;
#7500=VECTOR ( 'NONE', #12126, 1000.000000000000000 ) ;
#7506=CARTESIAN_POINT ( 'NONE',  ( 27.11643206945770146, -20.93856092459426677, 13.95341982493238753 ) ) ;
#7513=CARTESIAN_POINT ( 'NONE',  ( 32.61569110240115776, -6.288022587442930522, 4.533357778048659803 ) ) ;
#7516=ADVANCED_FACE ( 'NONE', ( #1055 ), #12014, .T. ) ;
#7521=VECTOR ( 'NONE', #15847, 1000.000000000000227 ) ;
#7522=CARTESIAN_POINT ( 'NONE',  ( 32.70264286945147347, -5.350767304972614546, 7.939653947423658487 ) ) ;
#7523=DIRECTION ( 'NONE',  ( -0.000000000000000000, -1.000000000000000000, -0.000000000000000000 ) ) ;
#7527=DIRECTION ( 'NONE',  ( 0.000000000000000000, 0.000000000000000000, -1.000000000000000000 ) ) ;
#7537=DIRECTION ( 'NONE',  ( -0.1196152422706610735, 0.9928203230275511881, 0.000000000000000000 ) ) ;
#7539=CARTESIAN_POINT ( 'NONE',  ( 27.18555652250208610, -2.580805812949960920, 4.533357778048667797 ) ) ;
#7542=ORIENTED_EDGE ( 'NONE', *, *, #2762, .F. ) ;
#7545=ORIENTED_EDGE ( 'NONE', *, *, #8798, .F. ) ;
#7546=EDGE_CURVE ( 'NONE', #2213, #4427, #9207, .T. ) ;
#7555=PLANE ( 'NONE',  #16170 ) ;
#7558=CARTESIAN_POINT ( 'NONE',  ( 27.17934203385504333, -30.00000000000000355, 13.93658524716016878 ) ) ;
#7560=CARTESIAN_POINT ( 'NONE',  ( 30.88125018618674744, -3.062327022369072171, 7.939653947423664704 ) ) ;
#7562=VECTOR ( 'NONE', #5965, 1000.000000000000000 ) ;
#7577=DIRECTION ( 'NONE',  ( 0.9928203230275510771, 0.1196152422706609902, 4.006172263299092517E-17 ) ) ;
#7583=CARTESIAN_POINT ( 'NONE',  ( 27.78610916120306129, -6.570083055755264745, 6.861505862736157368 ) ) ;
#7590=CARTESIAN_POINT ( 'NONE',  ( 32.19919549706052209, -6.038393303862174655, 6.861505862736157368 ) ) ;
#7594=AXIS2_PLACEMENT_3D ( 'NONE', #6825, #12271, #17919 ) ;
#7606=CARTESIAN_POINT ( 'NONE',  ( 32.51061761821408425, -6.300681867249914525, 7.033357778048657138 ) ) ;
#7608=VERTEX_POINT ( 'NONE', #9548 ) ;
#7609=ORIENTED_EDGE ( 'NONE', *, *, #11922, .F. ) ;
#7611=ORIENTED_EDGE ( 'NONE', *, *, #17011, .T. ) ;
#7612=CARTESIAN_POINT ( 'NONE',  ( 27.48088551392658729, -7.244023872874614689, 5.783357778048669573 ) ) ;
#7615=LINE ( 'NONE', #12951, #1264 ) ;
#7617=EDGE_CURVE ( 'NONE', #15284, #11466, #12236, .T. ) ;
#7623=CARTESIAN_POINT ( 'NONE',  ( 17.88061427385022739, 10.54987872837076601, 15.87467694953868502 ) ) ;
#7624=CARTESIAN_POINT ( 'NONE',  ( 20.27684169284606241, -10.57794632788464995, 15.46227570229628689 ) ) ;
#7627=ORIENTED_EDGE ( 'NONE', *, *, #11811, .F. ) ;
#7632=ORIENTED_EDGE ( 'NONE', *, *, #3776, .T. ) ;
#7634=CARTESIAN_POINT ( 'NONE',  ( 27.24942365487322959, -6.207645047004941574, 8.283357778048658915 ) ) ;
#7636=ORIENTED_EDGE ( 'NONE', *, *, #17816, .F. ) ;
#7641=LINE ( 'NONE', #4807, #906 ) ;
#7643=CARTESIAN_POINT ( 'NONE',  ( 33.60446413004628141, -3.988174587000466342, 7.939653947423662039 ) ) ;
#7647=EDGE_CURVE ( 'NONE', #11700, #1184, #13033, .T. ) ;
#7648=LINE ( 'NONE', #13171, #16766 ) ;
#7653=LINE ( 'NONE', #14361, #2527 ) ;
#7657=CARTESIAN_POINT ( 'NONE',  ( 27.87986455999572399, -6.131689368163070419, 8.283357778048660691 ) ) ;
#7658=ORIENTED_EDGE ( 'NONE', *, *, #14300, .T. ) ;
#7663=EDGE_LOOP ( 'NONE', ( #7201, #5778 ) ) ;
#7671=ADVANCED_FACE ( 'NONE', ( #6757 ), #8114, .F. ) ;
#7674=CARTESIAN_POINT ( 'NONE',  ( 28.54354359905709870, -7.105797696961086096, 5.783357778048657138 ) ) ;
#7677=ORIENTED_EDGE ( 'NONE', *, *, #15004, .F. ) ;
#7678=CARTESIAN_POINT ( 'NONE',  ( 32.67619606237177265, -1.592130426037603907, 5.783357778048668685 ) ) ;
#7679=CARTESIAN_POINT ( 'NONE',  ( -19.91444112663254984, -10.77903654349075246, 15.52697452096630748 ) ) ;
#7682=DIRECTION ( 'NONE',  ( -0.000000000000000000, -0.000000000000000000, 1.000000000000000000 ) ) ;
#7683=CARTESIAN_POINT ( 'NONE',  ( 30.33776104811456165, -2.201027418740610919, 4.533357778048667797 ) ) ;
#7690=EDGE_CURVE ( 'NONE', #11059, #16386, #4344, .T. ) ;
#7693=CARTESIAN_POINT ( 'NONE',  ( 30.75815651034531584, -7.238725614818142695, 5.783357778048657138 ) ) ;
#7695=EDGE_LOOP ( 'NONE', ( #5771, #16921 ) ) ;
#7697=CARTESIAN_POINT ( 'NONE',  ( 33.60446413004628141, -3.988174587000466342, 7.939653947423662039 ) ) ;
#7698=CARTESIAN_POINT ( 'NONE',  ( 33.35047706458318828, -2.764833946905070672, 3.627061608673666449 ) ) ;
#7705=FACE_OUTER_BOUND ( 'NONE', #3215, .T. ) ;
#7709=EDGE_CURVE ( 'NONE', #11389, #17262, #10971, .T. ) ;
#7712=ORIENTED_EDGE ( 'NONE', *, *, #15724, .F. ) ;
#7713=( BOUNDED_CURVE ( )  B_SPLINE_CURVE ( 2, ( #16304, #9554, #15100, #12465, #1323, #12373, #11450, #14099, #4398 ),
 .UNSPECIFIED., .F., .T. ) 
 B_SPLINE_CURVE_WITH_KNOTS ( ( 3, 2, 2, 2, 3 ),
 ( 0.7115384615384615641, 0.7179487179487179516, 0.7307692307692307265, 0.7435897435897436125, 0.7500000000000000000 ),
 .UNSPECIFIED. ) 
 CURVE ( )  GEOMETRIC_REPRESENTATION_ITEM ( )  RATIONAL_B_SPLINE_CURVE ( ( 0.9330127018922194093, 0.9330127018922194093, 1.000000000000000000, 0.8660254037844387076, 1.000000000000000000, 0.8660254037844387076, 1.000000000000000000, 0.9330127018922194093, 0.9330127018922194093 ) ) 
 REPRESENTATION_ITEM ( '' )  );
#7717=CYLINDRICAL_SURFACE ( 'NONE', #14122, 2.500000000000001776 ) ;
#7718=EDGE_CURVE ( 'NONE', #9693, #15182, #9635, .T. ) ;
#7720=ORIENTED_EDGE ( 'NONE', *, *, #17594, .T. ) ;
#7721=ORIENTED_EDGE ( 'NONE', *, *, #16962, .F. ) ;
#7722=DIRECTION ( 'NONE',  ( 0.1195020427801297691, 0.9918807541847894926, 0.04349518650597275493 ) ) ;
#7724=CARTESIAN_POINT ( 'NONE',  ( -19.43845002722867221, 2.988003976273734708, 0.000000000000000000 ) ) ;
#7732=EDGE_CURVE ( 'NONE', #8890, #10810, #13561, .T. ) ;
#7733=( BOUNDED_CURVE ( )  B_SPLINE_CURVE ( 3, ( #3926, #9438, #14978, #5352 ),
 .UNSPECIFIED., .F., .T. ) 
 B_SPLINE_CURVE_WITH_KNOTS ( ( 4, 4 ),
 ( 1.436990331221392081, 1.509167199807614601 ),
 .UNSPECIFIED. ) 
 CURVE ( )  GEOMETRIC_REPRESENTATION_ITEM ( )  RATIONAL_B_SPLINE_CURVE ( ( 1.000000000000000000, 0.9995659220841806025, 0.9995659220841806025, 1.000000000000000000 ) ) 
 REPRESENTATION_ITEM ( '' )  );
#7734=CARTESIAN_POINT ( 'NONE',  ( 15.92260893619738837, -28.39189527176317540, 16.15082599432113142 ) ) ;
#7737=DIRECTION ( 'NONE',  ( 0.7999999999999999334, -0.6000000000000001998, 0.000000000000000000 ) ) ;
#7746=PLANE ( 'NONE',  #4338 ) ;
#7748=DIRECTION ( 'NONE',  ( 0.000000000000000000, 0.000000000000000000, -1.000000000000000000 ) ) ;
#7751=CARTESIAN_POINT ( 'NONE',  ( -20.25000000000000355, -16.21813761408365195, 0.000000000000000000 ) ) ;
#7753=CARTESIAN_POINT ( 'NONE',  ( 26.62577407660990758, -3.575027854551694695, 7.939653947423664704 ) ) ;
#7755=VERTEX_POINT ( 'NONE', #4392 ) ;
#7756=VERTEX_POINT ( 'NONE', #3038 ) ;
#7757=CARTESIAN_POINT ( 'NONE',  ( 26.03917326857634151, -4.899642733102906433, 7.939653947423662039 ) ) ;
#7763=CARTESIAN_POINT ( 'NONE',  ( 30.61177514885986639, -5.802548093181622235, 3.283357778048663356 ) ) ;
#7764=EDGE_CURVE ( 'NONE', #9531, #15791, #8754, .T. ) ;
#7768=B_SPLINE_CURVE_WITH_KNOTS ( 'NONE', 3,
 ( #5948, #14037, #10024, #9843 ),
 .UNSPECIFIED., .F., .F.,
 ( 4, 4 ),
 ( 0.000000000000000000, 0.0003446252387907819490 ),
 .UNSPECIFIED. ) ;
#7771=CARTESIAN_POINT ( 'NONE',  ( 31.35480929215617252, -6.439933945126671055, 4.533357778048659803 ) ) ;
#7772=AXIS2_PLACEMENT_3D ( 'NONE', #12693, #8531, #190 ) ;
#7775=FACE_BOUND ( 'NONE', #6210, .T. ) ;
#7779=CARTESIAN_POINT ( 'NONE',  ( 27.23057351405260818, -1.848475362037681480, 5.783357778048668685 ) ) ;
#7784=CARTESIAN_POINT ( 'NONE',  ( 26.87106449706838873, -6.053357334259913181, 7.939653947423658487 ) ) ;
#7786=ORIENTED_EDGE ( 'NONE', *, *, #11266, .F. ) ;
#7789=ADVANCED_FACE ( 'NONE', ( #12823 ), #14009, .F. ) ;
#7802=EDGE_LOOP ( 'NONE', ( #16163, #16973, #8246, #3429 ) ) ;
#7803=LINE ( 'NONE', #4984, #240 ) ;
#7807=EDGE_LOOP ( 'NONE', ( #6405, #7294, #14683, #13994 ) ) ;
#7809=ORIENTED_EDGE ( 'NONE', *, *, #9154, .T. ) ;
#7812=CARTESIAN_POINT ( 'NONE',  ( 27.92859066579839222, -3.218191664895003523, 3.283357778048666464 ) ) ;
#7815=CARTESIAN_POINT ( 'NONE',  ( 25.81704846941310194, -3.246696919197676223, 7.157325878379703354 ) ) ;
#7821=CARTESIAN_POINT ( 'NONE',  ( 8.632250723006720250, -18.84644399697197770, 13.00000000000000178 ) ) ;
#7822=CARTESIAN_POINT ( 'NONE',  ( -15.92260893619738837, -28.39189527176317540, -0.000000000000000000 ) ) ;
#7828=PLANE ( 'NONE',  #6892 ) ;
#7829=DIRECTION ( 'NONE',  ( 0.1113444980252557837, -0.9937818688019538493, 0.000000000000000000 ) ) ;
#7831=CARTESIAN_POINT ( 'NONE',  ( 26.08205926866326863, -5.446317154234561642, 3.408606443870483282 ) ) ;
#7833=AXIS2_PLACEMENT_3D ( 'NONE', #12779, #12417, #3001 ) ;
#7840=CARTESIAN_POINT ( 'NONE',  ( 23.02601376483258022, 3.965314980223224151, 0.000000000000000000 ) ) ;
#7842=EDGE_CURVE ( 'NONE', #6854, #2179, #4480, .T. ) ;
#7850=CARTESIAN_POINT ( 'NONE',  ( 25.99533317148741318, -3.650983533393564517, 7.939653947423664704 ) ) ;
#7853=ORIENTED_EDGE ( 'NONE', *, *, #5162, .T. ) ;
#7854=CARTESIAN_POINT ( 'NONE',  ( 28.91547068018125799, -2.672194098943493135, 4.705209693361168455 ) ) ;
#7859=CARTESIAN_POINT ( 'NONE',  ( 30.63309003953906995, -6.864245478665264244, 5.783357778048664244 ) ) ;
#7863=VECTOR ( 'NONE', #8313, 1000.000000000000227 ) ;
#7869=CARTESIAN_POINT ( 'NONE',  ( -8.632250723006722026, -18.84644399697197770, 16.84735068286508763 ) ) ;
#7872=CARTESIAN_POINT ( 'NONE',  ( 28.86683379497783264, -7.466592651343750831, 5.783357778048657138 ) ) ;
#7877=ORIENTED_EDGE ( 'NONE', *, *, #14911, .T. ) ;
#7878=CARTESIAN_POINT ( 'NONE',  ( 32.97402322492378346, -4.064130265842336165, 7.939653947423662039 ) ) ;
#7879=CARTESIAN_POINT ( 'NONE',  ( 31.56875459193803124, -6.114348982704044921, 6.861505862736157368 ) ) ;
#7882=DIRECTION ( 'NONE',  ( 0.000000000000000000, 0.000000000000000000, -1.000000000000000000 ) ) ;
#7883=CARTESIAN_POINT ( 'NONE',  ( 26.01652455409633902, -4.902371455920926380, 5.783357778048663356 ) ) ;
#7890=DIRECTION ( 'NONE',  ( 4.179998415399335043E-17, -3.469446951953615175E-16, -1.000000000000000000 ) ) ;
#7895=CARTESIAN_POINT ( 'NONE',  ( 31.97277696464621854, -6.702839660918840536, 5.783357778048664244 ) ) ;
#7898=AXIS2_PLACEMENT_3D ( 'NONE', #15360, #9633, #8285 ) ;
#7899=ORIENTED_EDGE ( 'NONE', *, *, #7709, .T. ) ;
#7900=DIRECTION ( 'NONE',  ( -0.1196152422706610735, 0.9928203230275511881, 0.000000000000000000 ) ) ;
#7903=CARTESIAN_POINT ( 'NONE',  ( 27.89480254248674740, -2.495355674045408367, 4.533357778048667797 ) ) ;
#7913=EDGE_CURVE ( 'NONE', #16382, #7391, #10268, .T. ) ;
#7920=DIRECTION ( 'NONE',  ( -0.8243186046180107640, -0.5661261679878573094, -0.000000000000000000 ) ) ;
#7922=VECTOR ( 'NONE', #3162, 1000.000000000000114 ) ;
#7925=( BOUNDED_CURVE ( )  B_SPLINE_CURVE ( 2, ( #9249, #8900, #17455, #2383, #3458, #16161, #737, #16076, #822 ),
 .UNSPECIFIED., .F., .T. ) 
 B_SPLINE_CURVE_WITH_KNOTS ( ( 3, 2, 2, 2, 3 ),
 ( 0.8653846153846154188, 0.8717948717948718063, 0.8846153846153845812, 0.8974358974358974672, 0.9012882778258578531 ),
 .UNSPECIFIED. ) 
 CURVE ( )  GEOMETRIC_REPRESENTATION_ITEM ( )  RATIONAL_B_SPLINE_CURVE ( ( 0.9330127018922192983, 0.9330127018922198534, 1.000000000000000000, 0.8660254037844387076, 1.000000000000000000, 0.8660254037844387076, 1.000000000000000000, 0.9597425536373320742, 0.9436786787937823107 ) ) 
 REPRESENTATION_ITEM ( '' )  );
#7936=CARTESIAN_POINT ( 'NONE',  ( 30.58169613980036772, -2.898544849976259385, 8.283357778048664244 ) ) ;
#7940=CARTESIAN_POINT ( 'NONE',  ( 30.19827253897071273, -3.144612341114420673, 3.627061608673666893 ) ) ;
#7944=ORIENTED_EDGE ( 'NONE', *, *, #3467, .F. ) ;
#7949=CARTESIAN_POINT ( 'NONE',  ( -1.917618200156724081E-28, -7.000000000000001776, 0.000000000000000000 ) ) ;
#7951=CARTESIAN_POINT ( 'NONE',  ( 15.92260893619738837, -28.39189527176317540, 6.000000000000000000 ) ) ;
#7952=CARTESIAN_POINT ( 'NONE',  ( 26.23609683341064525, -2.995005734021441768, 4.705209693361167567 ) ) ;
#7956=CARTESIAN_POINT ( 'NONE',  ( 32.38298487551052318, -4.135338714860305132, 3.283357778048664244 ) ) ;
#7958=CARTESIAN_POINT ( 'NONE',  ( 27.60595198473284384, -7.618504009027492252, 5.783357778048657138 ) ) ;
#7963=ORIENTED_EDGE ( 'NONE', *, *, #3605, .T. ) ;
#7964=CARTESIAN_POINT ( 'NONE',  ( 32.65880277236253448, -4.102108105263264193, 3.627061608673664228 ) ) ;
#7965=CARTESIAN_POINT ( 'NONE',  ( 31.69574812466957781, -6.726019302751734763, 5.783357778048657138 ) ) ;
#7966=EDGE_CURVE ( 'NONE', #9791, #2265, #14646, .T. ) ;
#7980=CARTESIAN_POINT ( 'NONE',  ( -35.74085044863416272, -23.57886868891566223, 11.27079897466147607 ) ) ;
#7982=DIRECTION ( 'NONE',  ( 0.9928203230275510771, 0.1196152422706609902, 4.006172263299092517E-17 ) ) ;
#7985=CARTESIAN_POINT ( 'NONE',  ( 32.56242593318006584, -2.859778545457409837, 3.627061608673666449 ) ) ;
#7988=DIRECTION ( 'NONE',  ( 0.9928203230275510771, 0.1196152422706609902, 4.006172263299092517E-17 ) ) ;
#7994=CARTESIAN_POINT ( 'NONE',  ( 35.77680296528374271, -19.03270077640483038, 0.5379818257722508434 ) ) ;
#7996=DIRECTION ( 'NONE',  ( -1.000000000000000000, 0.000000000000000000, 0.000000000000000000 ) ) ;
#8003=CARTESIAN_POINT ( 'NONE',  ( 26.03655646321512052, -5.068638614726477698, 3.378836190363221803 ) ) ;
#8006=CARTESIAN_POINT ( 'NONE',  ( 0.000000000000000000, 0.000000000000000000, 8.700000000000001066 ) ) ;
#8012=DIRECTION ( 'NONE',  ( 0.000000000000000000, 0.000000000000000000, 1.000000000000000000 ) ) ;
#8014=CARTESIAN_POINT ( 'NONE',  ( 31.00199007654869732, -2.847907730748336252, 3.283357778048666464 ) ) ;
#8016=CARTESIAN_POINT ( 'NONE',  ( 28.40332666278570173, -4.614808937445885384, 3.627061608673664228 ) ) ;
#8018=CARTESIAN_POINT ( 'NONE',  ( 22.62413451274595388, -22.47014588436322668, 15.00416998627796694 ) ) ;
#8022=CARTESIAN_POINT ( 'NONE',  ( 45.50000000000000000, -16.03270077640482683, 8.287981825772241962 ) ) ;
#8029=FACE_OUTER_BOUND ( 'NONE', #3768, .T. ) ;
#8032=CARTESIAN_POINT ( 'NONE',  ( 27.08121146544255353, -6.028038774645947839, 3.627061608673662896 ) ) ;
#8033=CARTESIAN_POINT ( 'NONE',  ( 28.13194630731337753, -5.901445976576171759, 7.939653947423658487 ) ) ;
#8035=CARTESIAN_POINT ( 'NONE',  ( 8.632250723006720250, -18.84644399697197770, 16.84735068286506987 ) ) ;
#8036=CARTESIAN_POINT ( 'NONE',  ( 32.53688598753899441, -6.297517047505613697, 4.533357778048659803 ) ) ;
#8037=CARTESIAN_POINT ( 'NONE',  ( 33.58707084003705745, -6.498152266226123963, 5.783357778048657138 ) ) ;
#8038=CARTESIAN_POINT ( 'NONE',  ( 26.87785582392756467, -3.344784462964796479, 8.283357778048664244 ) ) ;
#8040=ORIENTED_EDGE ( 'NONE', *, *, #5177, .T. ) ;
#8041=EDGE_LOOP ( 'NONE', ( #13363, #1443, #13774, #16870 ) ) ;
#8042=CARTESIAN_POINT ( 'NONE',  ( 31.30154412293507349, -3.011689903141150815, 3.627061608673666893 ) ) ;
#8044=CARTESIAN_POINT ( 'NONE',  ( 31.06530721954707985, -6.801974981593605918, 5.783357778048657138 ) ) ;
#8046=CARTESIAN_POINT ( 'NONE',  ( 30.48043329534786849, -5.818372192732907067, 8.283357778048660691 ) ) ;
#8047=STYLED_ITEM ( 'NONE', ( #11952 ), #5266 ) ;
#8048=CYLINDRICAL_SURFACE ( 'NONE', #6060, 5.500000000000000888 ) ;
#8049=CARTESIAN_POINT ( 'NONE',  ( 26.01652455409633902, -4.902371455920926380, 5.783357778048663356 ) ) ;
#8053=EDGE_CURVE ( 'NONE', #2135, #9636, #16569, .T. ) ;
#8063=VECTOR ( 'NONE', #14116, 1000.000000000000000 ) ;
#8067=ORIENTED_EDGE ( 'NONE', *, *, #4609, .F. ) ;
#8068=CARTESIAN_POINT ( 'NONE',  ( 32.77257290155422709, -2.834459985843462260, 7.939653947423662927 ) ) ;
#8078=ORIENTED_EDGE ( 'NONE', *, *, #6464, .T. ) ;
#8079=VERTEX_POINT ( 'NONE', #5395 ) ;
#8081=EDGE_CURVE ( 'NONE', #2247, #17429, #11045, .T. ) ;
#8083=CARTESIAN_POINT ( 'NONE',  ( 25.71748644841968456, -2.420320648352046078, 5.783357778048663356 ) ) ;
#8093=CARTESIAN_POINT ( 'NONE',  ( 26.18940075748478691, -6.337263906362392341, 3.743184633113769699 ) ) ;
#8094=CIRCLE ( 'NONE', #5182, 5.500000000000000000 ) ;
#8100=DIRECTION ( 'NONE',  ( 0.000000000000000000, -1.000000000000000000, 0.000000000000000000 ) ) ;
#8104=ORIENTED_EDGE ( 'NONE', *, *, #11460, .F. ) ;
#8106=EDGE_CURVE ( 'NONE', #5157, #8560, #16481, .T. ) ;
#8107=AXIS2_PLACEMENT_3D ( 'NONE', #14183, #17009, #14373 ) ;
#8108=CARTESIAN_POINT ( 'NONE',  ( 30.92509028327567933, -4.310986222078405206, 3.627061608673664228 ) ) ;
#8110=CARTESIAN_POINT ( 'NONE',  ( 17.07932405232147488, -18.26192153598439205, 15.98801167710370663 ) ) ;
#8112=CARTESIAN_POINT ( 'NONE',  ( 23.00000000000000000, -16.21813761408365195, 0.000000000000000000 ) ) ;
#8113=VERTEX_POINT ( 'NONE', #17792 ) ;
#8114=PLANE ( 'NONE',  #217 ) ;
#8118=EDGE_CURVE ( 'NONE', #2263, #16382, #15810, .T. ) ;
#8121=CARTESIAN_POINT ( 'NONE',  ( 28.19013153391124860, -7.158573733970061248, 5.783357778048669573 ) ) ;
#8122=CARTESIAN_POINT ( 'NONE',  ( 25.95642634701329499, -4.403549397486667516, 7.880302681851837576 ) ) ;
#8123=CARTESIAN_POINT ( 'NONE',  ( 28.88938074516742205, -6.437160617781993999, 6.861505862736158257 ) ) ;
#8127=FACE_OUTER_BOUND ( 'NONE', #892, .T. ) ;
#8128=ORIENTED_EDGE ( 'NONE', *, *, #15704, .T. ) ;
#8129=CARTESIAN_POINT ( 'NONE',  ( 28.67914455963771303, -4.581578327848842669, 3.283357778048664244 ) ) ;
#8133=EDGE_CURVE ( 'NONE', #8657, #8474, #6859, .T. ) ;
#8134=AXIS2_PLACEMENT_3D ( 'NONE', #13690, #12238, #17810 ) ;
#8136=ORIENTED_EDGE ( 'NONE', *, *, #14036, .T. ) ;
#8137=CARTESIAN_POINT ( 'NONE',  ( 30.04066231269008469, -3.163601260824890904, 3.627061608673666893 ) ) ;
#8138=CARTESIAN_POINT ( 'NONE',  ( 26.87785582392756112, -3.344784462964796035, 8.283357778048666020 ) ) ;
#8139=ORIENTED_EDGE ( 'NONE', *, *, #6900, .T. ) ;
#8140=CARTESIAN_POINT ( 'NONE',  ( 29.15206445563513071, -6.405512418264540209, 4.705209693361159573 ) ) ;
#8150=CARTESIAN_POINT ( 'NONE',  ( 25.57853536445108489, -10.52124088318384310, 14.33864855032055985 ) ) ;
#8151=ORIENTED_EDGE ( 'NONE', *, *, #1871, .F. ) ;
#8160=EDGE_CURVE ( 'NONE', #9636, #14428, #15712, .T. ) ;
#8161=EDGE_LOOP ( 'NONE', ( #4776, #17720, #9877, #2121 ) ) ;
#8162=CARTESIAN_POINT ( 'NONE',  ( 32.65880277236253448, -4.102108105263264193, 3.627061608673664228 ) ) ;
#8166=CARTESIAN_POINT ( 'NONE',  ( -35.62429925076629189, -17.76690233603958902, 0.5379818257722508434 ) ) ;
#8169=ADVANCED_FACE ( 'NONE', ( #17031 ), #15753, .F. ) ;
#8174=ORIENTED_EDGE ( 'NONE', *, *, #7413, .T. ) ;
#8179=CARTESIAN_POINT ( 'NONE',  ( 7.499998387031003411, -20.49508120620799900, 6.000000000000000000 ) ) ;
#8183=VECTOR ( 'NONE', #3049, 1000.000000000000000 ) ;
#8190=VERTEX_POINT ( 'NONE', #3143 ) ;
#8194=FACE_BOUND ( 'NONE', #9415, .T. ) ;
#8199=ORIENTED_EDGE ( 'NONE', *, *, #14396, .T. ) ;
#8202=CARTESIAN_POINT ( 'NONE',  ( 30.40841950734487753, -3.119293781500474427, 7.939653947423664704 ) ) ;
#8208=CARTESIAN_POINT ( 'NONE',  ( 8.809730593168891843, -18.96833375928839516, 16.83727734034771473 ) ) ;
#8209=ORIENTED_EDGE ( 'NONE', *, *, #1381, .F. ) ;
#8216=CARTESIAN_POINT ( 'NONE',  ( 32.77701044293393551, -4.087866415376695706, 8.283357778048662468 ) ) ;
#8217=CARTESIAN_POINT ( 'NONE',  ( 27.61527553138257574, -4.709753535998224550, 3.627061608673664228 ) ) ;
#8223=CARTESIAN_POINT ( 'NONE',  ( 32.77257290155422709, -2.834459985843461816, 7.939653947423664704 ) ) ;
#8224=CARTESIAN_POINT ( 'NONE',  ( 26.64639396487419987, -2.308405637095112706, 5.783357778048667797 ) ) ;
#8226=CARTESIAN_POINT ( 'NONE',  ( 29.52399153675929355, -1.971908820246954130, 5.783357778048668685 ) ) ;
#8233=CARTESIAN_POINT ( 'NONE',  ( 26.01652455409633902, -4.902371455920926380, 5.783357778048663356 ) ) ;
#8234=EDGE_CURVE ( 'NONE', #11271, #1184, #7232, .T. ) ;
#8242=CARTESIAN_POINT ( 'NONE',  ( 26.07857582428556853, -4.894895503279006022, 3.283357778048664244 ) ) ;
#8246=ORIENTED_EDGE ( 'NONE', *, *, #6483, .F. ) ;
#8247=CARTESIAN_POINT ( 'NONE',  ( 33.42946061375642586, -6.517141185936593750, 5.783357778048658915 ) ) ;
#8250=FACE_OUTER_BOUND ( 'NONE', #11588, .T. ) ;
#8252=CARTESIAN_POINT ( 'NONE',  ( 32.29220775574281532, -1.628196571319322050, 5.113484796970859669 ) ) ;
#8266=LINE ( 'NONE', #4194, #6218 ) ;
#8271=LINE ( 'NONE', #17159, #16550 ) ;
#8274=DIRECTION ( 'NONE',  ( 0.000000000000000000, 0.000000000000000000, 1.000000000000000000 ) ) ;
#8277=CARTESIAN_POINT ( 'NONE',  ( 29.34405387406022570, -7.019548880150045633, 6.453230759126462601 ) ) ;
#8279=( BOUNDED_CURVE ( )  B_SPLINE_CURVE ( 2, ( #12907, #10081, #12634, #4213, #9714, #11244, #2843, #15358, #2938 ),
 .UNSPECIFIED., .F., .T. ) 
 B_SPLINE_CURVE_WITH_KNOTS ( ( 3, 2, 2, 2, 3 ),
 ( 0.01923076923076925265, 0.02564102564102564014, 0.03846153846153846367, 0.05128205128205128027, 0.05769230769230771633 ),
 .UNSPECIFIED. ) 
 CURVE ( )  GEOMETRIC_REPRESENTATION_ITEM ( )  RATIONAL_B_SPLINE_CURVE ( ( 0.9330127018922194093, 0.9330127018922196314, 1.000000000000000000, 0.8660254037844387076, 1.000000000000000000, 0.8660254037844387076, 1.000000000000000000, 0.9330127018922190762, 0.9330127018922194093 ) ) 
 REPRESENTATION_ITEM ( '' )  );
#8281=CARTESIAN_POINT ( 'NONE',  ( 27.12922144900085186, -2.887401855662130146, 6.861505862736166250 ) ) ;
#8284=VERTEX_POINT ( 'NONE', #12745 ) ;
#8285=DIRECTION ( 'NONE',  ( -1.000000000000000000, 0.000000000000000000, 0.000000000000000000 ) ) ;
#8288=ORIENTED_EDGE ( 'NONE', *, *, #14300, .F. ) ;
#8297=CARTESIAN_POINT ( 'NONE',  ( 29.39282811755836633, -5.749534618892433002, 7.939653947423658487 ) ) ;
#8301=FACE_OUTER_BOUND ( 'NONE', #3541, .T. ) ;
#8305=CARTESIAN_POINT ( 'NONE',  ( 27.10313151398701947, -6.652368374500619908, 4.705209693361160461 ) ) ;
#8308=CARTESIAN_POINT ( 'NONE',  ( 27.89118264539014547, -6.557423775948280742, 4.705209693361159573 ) ) ;
#8309=CARTESIAN_POINT ( 'NONE',  ( -38.15522249139979749, -7.597641695372263193, 5.783357778048663356 ) ) ;
#8313=DIRECTION ( 'NONE',  ( 0.9928203230275510771, 0.1196152422706609902, 4.006172263299092517E-17 ) ) ;
#8319=CARTESIAN_POINT ( 'NONE',  ( 26.01595305975170547, -2.384361315936983416, 5.783357778048657138 ) ) ;
#8324=EDGE_LOOP ( 'NONE', ( #3941, #5942 ) ) ;
#8327=CARTESIAN_POINT ( 'NONE',  ( 32.77709966008947617, -5.968767264923789284, 4.705209693361160461 ) ) ;
#8329=FACE_OUTER_BOUND ( 'NONE', #1818, .T. ) ;
#8333=CARTESIAN_POINT ( 'NONE',  ( 32.63137222500256485, -6.623491938275930302, 5.113484796970852564 ) ) ;
#8336=VECTOR ( 'NONE', #10322, 1000.000000000000227 ) ;
#8347=CARTESIAN_POINT ( 'NONE',  ( 31.27600417729400917, -6.449428405189353342, 4.533357778048659803 ) ) ;
#8356=ORIENTED_EDGE ( 'NONE', *, *, #9412, .F. ) ;
#8358=DIRECTION ( 'NONE',  ( -1.000000000000000000, 0.000000000000000000, 0.000000000000000000 ) ) ;
#8361=CARTESIAN_POINT ( 'NONE',  ( -2.016448651773435938E-27, -20.49999999999999645, 6.000000000000000000 ) ) ;
#8364=VECTOR ( 'NONE', #3376, 1000.000000000000227 ) ;
#8367=ORIENTED_EDGE ( 'NONE', *, *, #3653, .F. ) ;
#8370=CARTESIAN_POINT ( 'NONE',  ( 27.77288575766320378, -4.690764616287755651, 3.627061608673664228 ) ) ;
#8371=CARTESIAN_POINT ( 'NONE',  ( -25.76436512043297711, -21.83811057962065405, 14.29411090273705831 ) ) ;
#8372=CARTESIAN_POINT ( 'NONE',  ( -37.55714628004649569, -12.56174331051002113, 5.783357778048663356 ) ) ;
#8373=ORIENTED_EDGE ( 'NONE', *, *, #17630, .F. ) ;
#8374=PLANE ( 'NONE',  #7898 ) ;
#8380=FACE_BOUND ( 'NONE', #5596, .T. ) ;
#8381=CARTESIAN_POINT ( 'NONE',  ( 29.86122125502053848, -4.439161430227785310, 3.283357778048664244 ) ) ;
#8385=( BOUNDED_CURVE ( )  B_SPLINE_CURVE ( 2, ( #6675, #9558, #10649, #5389, #7956, #5304, #8036, #16393, #12206 ),
 .UNSPECIFIED., .F., .F. ) 
 B_SPLINE_CURVE_WITH_KNOTS ( ( 3, 2, 2, 2, 3 ),
 ( 0.1730769230769231004, 0.1794871794871794879, 0.1923076923076923184, 0.2051282051282051211, 0.2115384615384615641 ),
 .UNSPECIFIED. ) 
 CURVE ( )  GEOMETRIC_REPRESENTATION_ITEM ( )  RATIONAL_B_SPLINE_CURVE ( ( 0.9330127018922194093, 0.9330127018922196314, 1.000000000000000000, 0.8660254037844387076, 1.000000000000000000, 0.8660254037844387076, 1.000000000000000000, 0.9330127018922190762, 0.9330127018922194093 ) ) 
 REPRESENTATION_ITEM ( '' )  );
#8386=CARTESIAN_POINT ( 'NONE',  ( 28.36401332423200827, -6.500457016816879374, 4.705209693361160461 ) ) ;
#8388=CARTESIAN_POINT ( 'NONE',  ( 28.91547068018125799, -2.672194098943493135, 4.705209693361168455 ) ) ;
#8389=VECTOR ( 'NONE', #2341, 1000.000000000000114 ) ;
#8391=EDGE_CURVE ( 'NONE', #3302, #4053, #4762, .T. ) ;
#8392=ORIENTED_EDGE ( 'NONE', *, *, #9625, .T. ) ;
#8393=CARTESIAN_POINT ( 'NONE',  ( 27.30005507882132676, -4.747731375419166788, 7.939653947423662039 ) ) ;
#8395=AXIS2_PLACEMENT_3D ( 'NONE', #17765, #13730, #4122 ) ;
#8396=ORIENTED_EDGE ( 'NONE', *, *, #14838, .T. ) ;
#8397=CARTESIAN_POINT ( 'NONE',  ( 27.02414796481377124, -2.900061135469103490, 4.705209693361168455 ) ) ;
#8398=CARTESIAN_POINT ( 'NONE',  ( 26.01652455409633902, -4.902371455920926380, 5.783357778048663356 ) ) ;
#8419=CARTESIAN_POINT ( 'NONE',  ( 28.75786045390062995, -2.691183018653962034, 4.705209693361167567 ) ) ;
#8424=CARTESIAN_POINT ( 'NONE',  ( 0.000000000000000000, 0.000000000000000000, 8.700000000000001066 ) ) ;
#8427=FACE_BOUND ( 'NONE', #679, .T. ) ;
#8440=CARTESIAN_POINT ( 'NONE',  ( 33.55383270609817714, -5.448088258586239796, 8.283357778048658915 ) ) ;
#8446=CARTESIAN_POINT ( 'NONE',  ( 26.82912971812489644, -6.258282166232842947, 3.283357778048663356 ) ) ;
#8448=AXIS2_PLACEMENT_3D ( 'NONE', #13545, #5359, #8358 ) ;
#8456=ORIENTED_EDGE ( 'NONE', *, *, #1098, .F. ) ;
#8468=CARTESIAN_POINT ( 'NONE',  ( 25.59340017005574097, -5.757764245108966783, 3.283357778048662468 ) ) ;
#8469=CARTESIAN_POINT ( 'NONE',  ( 25.88156304229571703, -4.918631652813365562, 3.627061608673664228 ) ) ;
#8471=ORIENTED_EDGE ( 'NONE', *, *, #1186, .F. ) ;
#8473=CARTESIAN_POINT ( 'NONE',  ( 28.83304567166618781, -6.743756660494150346, 4.533357778048659803 ) ) ;
#8474=VERTEX_POINT ( 'NONE', #10633 ) ;
#8475=CARTESIAN_POINT ( 'NONE',  ( -2.749999999999992895, -20.49999999999999645, 13.00000000000000178 ) ) ;
#8479=DIRECTION ( 'NONE',  ( -0.1196152422706610735, 0.9928203230275511881, 0.000000000000000000 ) ) ;
#8480=LINE ( 'NONE', #422, #16226 ) ;
#8487=CARTESIAN_POINT ( 'NONE',  ( 29.77797860222238313, -3.195249460342344250, 7.939653947423664704 ) ) ;
#8491=CARTESIAN_POINT ( 'NONE',  ( 30.02326902268086428, -5.673578940050561847, 7.939653947423658487 ) ) ;
#8501=( BOUNDED_SURFACE ( )  B_SPLINE_SURFACE ( 1, 2, ( 
 ( #7697, #535, #9147, #10225, #1256, #9397, #10654, #990, #12123, #17700, #6681, #1162, #7878, #8223, #13667, #3700, #16225, #6517, #7964, #3795, #2517, #12384, #2608, #15020, #13754, #17871, #9315, #5394, #16480, #6773, #12029, #17951, #1070, #9481, #5485, #17615, #14771, #1334, #5222, #13497, #14854, #8042, #2442, #6592, #9225, #10912, #11006, #2698, #12216, #17790, #16318, #5135, #4051, #16399, #6858, #13580, #10743, #5311, #2359, #9564, #3883, #14938, #13410, #10833, #3966, #8137, #12306, #15113, #3141, #13926, #11173, #8491, #11267, #15559, #242, #9830, #15200, #15380, #1422, #14025, #16746, #1612, #4497, #5575, #8575, #14111, #10012, #8676, #14201, #2965, #1522, #6944, #7142, #12743, #4232, #12653, #7052, #13833, #5753, #12478, #7230, #12567, #149, #3055, #434, #2867, #1796, #7327, #12844, #9731, #64, #5938, #1697, #16845, #341, #15286, #5848, #16568, #11371, #4410, #8393, #16939, #4151, #9650, #4319, #2782, #5662, #11093, #8305, #16658, #9923, #15473, #14305, #10286, #8854, #3602, #14663, #12927, #10204, #1888, #695, #2244, #7415, #4847, #7757, #14389, #9124, #6125, #3501, #6220, #14585, #10376, #15930 ),
 ( #11654, #779, #513, #4760, #13018, #13289, #869, #6026, #17221, #15836, #11556, #9033, #2161, #6308, #17123, #7678, #11828, #10469, #4674, #13203, #8772, #11737, #1973, #3409, #8940, #15751, #11463, #3327, #7495, #17408, #14482, #3234, #604, #2066, #7590, #13115, #17310, #4938, #16031, #15654, #17029, #4583, #10105, #965, #3678, #10631, #13383, #5198, #15090, #5287, #17764, #10889, #2581, #6494, #8108, #1230, #9458, #9202, #2672, #3770, #12185, #8202, #2336, #17510, #16458, #7940, #16205, #17591, #10720, #5111, #12010, #11919, #13640, #13729, #5370, #3861, #9372, #1050, #14749, #6751, #1130, #4026, #16292, #14833, #2493, #9542, #12282, #9292, #7854, #6401, #6656, #3943, #2418, #10805, #13475, #5031, #6571, #10553, #12092, #16379, #14913, #17677, #8016, #13554, #14994, #16118, #17850, #3116, #5460, #13902, #4296, #40, #11243, #15449, #8370, #16918, #14003, #1399, #4474, #10980, #314, #16819, #8281, #11346, #15179, #1493, #4386, #8555, #6920, #7028, #14087, #9988, #16634, #12364, #13811, #9900, #3032, #12720, #1586, #7119, #6833, #1674, #11152, #16724, #4121, #12546, #8649, #17930, #9629, #12454, #8469, #7209, #1312 ) ),
 .UNSPECIFIED., .F., .F., .T. ) 
 B_SPLINE_SURFACE_WITH_KNOTS ( ( 2, 2 ),
 ( 3, 2, 2, 2, 2, 2, 2, 2, 2, 2, 2, 2, 2, 2, 2, 2, 2, 2, 2, 2, 2, 2, 2, 2, 2, 2, 2, 2, 2, 2, 2, 2, 2, 2, 2, 2, 2, 2, 2, 2, 2, 2, 2, 2, 2, 2, 2, 2, 2, 2, 2, 2, 2, 2, 2, 2, 2, 2, 2, 2, 2, 2, 2, 2, 2, 2, 2, 2, 2, 2, 2, 2, 2, 2, 2, 2, 3 ),
 ( 0.000000000000000000, 1.000000000000000000 ),
 ( 0.000000000000000000, 0.01282051282051282007, 0.02564102564102564014, 0.03846153846153846367, 0.05128205128205128027, 0.06410256410256409687, 0.07692307692307692735, 0.08974358974358974395, 0.1025641025641025605, 0.1153846153846153910, 0.1282051282051281937, 0.1410256410256410242, 0.1538461538461538547, 0.1666666666666666574, 0.1794871794871794879, 0.1923076923076923184, 0.2051282051282051211, 0.2179487179487179516, 0.2307692307692307820, 0.2435897435897435848, 0.2564102564102563875, 0.2692307692307692180, 0.2820512820512820484, 0.2948717948717948789, 0.3076923076923077094, 0.3205128205128205399, 0.3333333333333333148, 0.3461538461538461453, 0.3589743589743589758, 0.3717948717948718063, 0.3846153846153846367, 0.3974358974358974117, 0.4102564102564102422, 0.4230769230769230727, 0.4358974358974359031, 0.4487179487179487336, 0.4615384615384615641, 0.4743589743589743390, 0.4871794871794871695, 0.5000000000000000000, 0.5128205128205127750, 0.5256410256410256610, 0.5384615384615384359, 0.5512820512820513219, 0.5641025641025640969, 0.5769230769230768718, 0.5897435897435897578, 0.6025641025641025328, 0.6153846153846154188, 0.6282051282051281937, 0.6410256410256410797, 0.6538461538461538547, 0.6666666666666666297, 0.6794871794871795156, 0.6923076923076922906, 0.7051282051282051766, 0.7179487179487179516, 0.7307692307692307265, 0.7435897435897436125, 0.7564102564102563875, 0.7692307692307692735, 0.7820512820512820484, 0.7948717948717948234, 0.8076923076923077094, 0.8205128205128204844, 0.8333333333333333703, 0.8461538461538461453, 0.8589743589743589203, 0.8717948717948718063, 0.8846153846153845812, 0.8974358974358974672, 0.9102564102564102422, 0.9230769230769231282, 0.9358974358974359031, 0.9487179487179486781, 0.9615384615384615641, 0.9690838366659333403 ),
 .UNSPECIFIED. ) 
 GEOMETRIC_REPRESENTATION_ITEM ( )  RATIONAL_B_SPLINE_SURFACE ( (
 ( 1.000000000000000000, 0.8660254037844387076, 1.000000000000000000, 0.8660254037844387076, 1.000000000000000000, 0.8660254037844387076, 1.000000000000000000, 0.8660254037844387076, 1.000000000000000000, 0.8660254037844387076, 1.000000000000000000, 0.8660254037844387076, 1.000000000000000000, 0.8660254037844387076, 1.000000000000000000, 0.8660254037844387076, 1.000000000000000000, 0.8660254037844387076, 1.000000000000000000, 0.8660254037844387076, 1.000000000000000000, 0.8660254037844387076, 1.000000000000000000, 0.8660254037844387076, 1.000000000000000000, 0.8660254037844387076, 1.000000000000000000, 0.8660254037844387076, 1.000000000000000000, 0.8660254037844387076, 1.000000000000000000, 0.8660254037844387076, 1.000000000000000000, 0.8660254037844387076, 1.000000000000000000, 0.8660254037844387076, 1.000000000000000000, 0.8660254037844387076, 1.000000000000000000, 0.8660254037844387076, 1.000000000000000000, 0.8660254037844387076, 1.000000000000000000, 0.8660254037844387076, 1.000000000000000000, 0.8660254037844387076, 1.000000000000000000, 0.8660254037844387076, 1.000000000000000000, 0.8660254037844387076, 1.000000000000000000, 0.8660254037844387076, 1.000000000000000000, 0.8660254037844387076, 1.000000000000000000, 0.8660254037844387076, 1.000000000000000000, 0.8660254037844387076, 1.000000000000000000, 0.8660254037844387076, 1.000000000000000000, 0.8660254037844387076, 1.000000000000000000, 0.8660254037844387076, 1.000000000000000000, 0.8660254037844387076, 1.000000000000000000, 0.8660254037844387076, 1.000000000000000000, 0.8660254037844387076, 1.000000000000000000, 0.8660254037844387076, 1.000000000000000000, 0.8660254037844387076, 1.000000000000000000, 0.8660254037844387076, 1.000000000000000000, 0.8660254037844387076, 1.000000000000000000, 0.8660254037844387076, 1.000000000000000000, 0.8660254037844387076, 1.000000000000000000, 0.8660254037844387076, 1.000000000000000000, 0.8660254037844387076, 1.000000000000000000, 0.8660254037844387076, 1.000000000000000000, 0.8660254037844387076, 1.000000000000000000, 0.8660254037844387076, 1.000000000000000000, 0.8660254037844387076, 1.000000000000000000, 0.8660254037844387076, 1.000000000000000000, 0.8660254037844387076, 1.000000000000000000, 0.8660254037844387076, 1.000000000000000000, 0.8660254037844387076, 1.000000000000000000, 0.8660254037844387076, 1.000000000000000000, 0.8660254037844387076, 1.000000000000000000, 0.8660254037844387076, 1.000000000000000000, 0.8660254037844387076, 1.000000000000000000, 0.8660254037844387076, 1.000000000000000000, 0.8660254037844387076, 1.000000000000000000, 0.8660254037844387076, 1.000000000000000000, 0.8660254037844387076, 1.000000000000000000, 0.8660254037844387076, 1.000000000000000000, 0.8660254037844387076, 1.000000000000000000, 0.8660254037844387076, 1.000000000000000000, 0.8660254037844387076, 1.000000000000000000, 0.8660254037844387076, 1.000000000000000000, 0.8660254037844387076, 1.000000000000000000, 0.8660254037844387076, 1.000000000000000000, 0.8660254037844387076, 1.000000000000000000, 0.8660254037844387076, 1.000000000000000000, 0.8660254037844387076, 1.000000000000000000, 0.8660254037844387076, 1.000000000000000000, 0.8660254037844387076, 1.000000000000000000, 0.8660254037844387076, 1.000000000000000000, 0.8660254037844387076, 1.000000000000000000, 0.8660254037844387076, 1.000000000000000000, 0.8660254037844387076, 1.000000000000000000, 0.9211506902921580142, 0.9351132093492240394),
 ( 1.000000000000000000, 0.8660254037844387076, 1.000000000000000000, 0.8660254037844387076, 1.000000000000000000, 0.8660254037844387076, 1.000000000000000000, 0.8660254037844387076, 1.000000000000000000, 0.8660254037844387076, 1.000000000000000000, 0.8660254037844387076, 1.000000000000000000, 0.8660254037844387076, 1.000000000000000000, 0.8660254037844387076, 1.000000000000000000, 0.8660254037844387076, 1.000000000000000000, 0.8660254037844387076, 1.000000000000000000, 0.8660254037844387076, 1.000000000000000000, 0.8660254037844387076, 1.000000000000000000, 0.8660254037844387076, 1.000000000000000000, 0.8660254037844387076, 1.000000000000000000, 0.8660254037844387076, 1.000000000000000000, 0.8660254037844387076, 1.000000000000000000, 0.8660254037844387076, 1.000000000000000000, 0.8660254037844387076, 1.000000000000000000, 0.8660254037844387076, 1.000000000000000000, 0.8660254037844387076, 1.000000000000000000, 0.8660254037844387076, 1.000000000000000000, 0.8660254037844387076, 1.000000000000000000, 0.8660254037844387076, 1.000000000000000000, 0.8660254037844387076, 1.000000000000000000, 0.8660254037844387076, 1.000000000000000000, 0.8660254037844387076, 1.000000000000000000, 0.8660254037844387076, 1.000000000000000000, 0.8660254037844387076, 1.000000000000000000, 0.8660254037844387076, 1.000000000000000000, 0.8660254037844387076, 1.000000000000000000, 0.8660254037844387076, 1.000000000000000000, 0.8660254037844387076, 1.000000000000000000, 0.8660254037844387076, 1.000000000000000000, 0.8660254037844387076, 1.000000000000000000, 0.8660254037844387076, 1.000000000000000000, 0.8660254037844387076, 1.000000000000000000, 0.8660254037844387076, 1.000000000000000000, 0.8660254037844387076, 1.000000000000000000, 0.8660254037844387076, 1.000000000000000000, 0.8660254037844387076, 1.000000000000000000, 0.8660254037844387076, 1.000000000000000000, 0.8660254037844387076, 1.000000000000000000, 0.8660254037844387076, 1.000000000000000000, 0.8660254037844387076, 1.000000000000000000, 0.8660254037844387076, 1.000000000000000000, 0.8660254037844387076, 1.000000000000000000, 0.8660254037844387076, 1.000000000000000000, 0.8660254037844387076, 1.000000000000000000, 0.8660254037844387076, 1.000000000000000000, 0.8660254037844387076, 1.000000000000000000, 0.8660254037844387076, 1.000000000000000000, 0.8660254037844387076, 1.000000000000000000, 0.8660254037844387076, 1.000000000000000000, 0.8660254037844387076, 1.000000000000000000, 0.8660254037844387076, 1.000000000000000000, 0.8660254037844387076, 1.000000000000000000, 0.8660254037844387076, 1.000000000000000000, 0.8660254037844387076, 1.000000000000000000, 0.8660254037844387076, 1.000000000000000000, 0.8660254037844387076, 1.000000000000000000, 0.8660254037844387076, 1.000000000000000000, 0.8660254037844387076, 1.000000000000000000, 0.8660254037844387076, 1.000000000000000000, 0.8660254037844387076, 1.000000000000000000, 0.8660254037844387076, 1.000000000000000000, 0.8660254037844387076, 1.000000000000000000, 0.8660254037844387076, 1.000000000000000000, 0.8660254037844387076, 1.000000000000000000, 0.8660254037844387076, 1.000000000000000000, 0.8660254037844387076, 1.000000000000000000, 0.8660254037844387076, 1.000000000000000000, 0.8660254037844387076, 1.000000000000000000, 0.8660254037844387076, 1.000000000000000000, 0.8660254037844387076, 1.000000000000000000, 0.8660254037844387076, 1.000000000000000000, 0.9211506902921580142, 0.9351132093492240394) ) ) 
 REPRESENTATION_ITEM ( '' )  SURFACE ( )  );
#8503=CARTESIAN_POINT ( 'NONE',  ( 29.25000000000000000, -16.63088773646508756, 13.37255996287878013 ) ) ;
#8506=ORIENTED_EDGE ( 'NONE', *, *, #11427, .F. ) ;
#8509=FACE_OUTER_BOUND ( 'NONE', #16440, .T. ) ;
#8515=CARTESIAN_POINT ( 'NONE',  ( 28.36401332423200827, -6.500457016816879374, 4.705209693361160461 ) ) ;
#8516=CARTESIAN_POINT ( 'NONE',  ( 25.90934487712387480, 0.1208734971681841297, 15.78335777804866424 ) ) ;
#8524=( BOUNDED_CURVE ( )  B_SPLINE_CURVE ( 3, ( #6556, #9360, #1036, #13459 ),
 .UNSPECIFIED., .F., .T. ) 
 B_SPLINE_CURVE_WITH_KNOTS ( ( 4, 4 ),
 ( 4.774018107371971631, 4.846194975958193929 ),
 .UNSPECIFIED. ) 
 CURVE ( )  GEOMETRIC_REPRESENTATION_ITEM ( )  RATIONAL_B_SPLINE_CURVE ( ( 1.000000000000000000, 0.9995659220841806025, 0.9995659220841806025, 1.000000000000000000 ) ) 
 REPRESENTATION_ITEM ( '' )  );
#8531=DIRECTION ( 'NONE',  ( -0.000000000000000000, -0.000000000000000000, 1.000000000000000000 ) ) ;
#8534=CARTESIAN_POINT ( 'NONE',  ( 30.54048978798443059, -6.538043363838207611, 7.033357778048657138 ) ) ;
#8536=ORIENTED_EDGE ( 'NONE', *, *, #17191, .F. ) ;
#8537=ORIENTED_EDGE ( 'NONE', *, *, #14655, .F. ) ;
#8538=CARTESIAN_POINT ( 'NONE',  ( 26.56758885001203652, -2.317900097157796324, 5.783357778048657138 ) ) ;
#8542=ORIENTED_EDGE ( 'NONE', *, *, #1611, .T. ) ;
#8552=ORIENTED_EDGE ( 'NONE', *, *, #8965, .T. ) ;
#8553=CARTESIAN_POINT ( 'NONE',  ( 32.77257290155422709, -2.834459985843461816, 7.939653947423664704 ) ) ;
#8555=CARTESIAN_POINT ( 'NONE',  ( 27.23882169172318513, -6.009049854935478052, 3.627061608673662896 ) ) ;
#8556=CARTESIAN_POINT ( 'NONE',  ( -29.04317620846695647, -17.86624673319742840, 13.43120144060744003 ) ) ;
#8557=CARTESIAN_POINT ( 'NONE',  ( 13.00000000000000178, 0.000000000000000000, 12.00000000000000000 ) ) ;
#8558=ORIENTED_EDGE ( 'NONE', *, *, #6767, .F. ) ;
#8560=VERTEX_POINT ( 'NONE', #8584 ) ;
#8571=CARTESIAN_POINT ( 'NONE',  ( 30.40841950734487753, -3.119293781500474427, 7.939653947423664704 ) ) ;
#8573=EDGE_LOOP ( 'NONE', ( #8891, #4846, #5272, #16291 ) ) ;
#8575=CARTESIAN_POINT ( 'NONE',  ( 29.19137779418881351, -4.519864338893556877, 7.939653947423662039 ) ) ;
#8576=DIRECTION ( 'NONE',  ( 0.9928203230275510771, 0.1196152422706609902, 4.006172263299092517E-17 ) ) ;
#8577=DIRECTION ( 'NONE',  ( -0.000000000000000000, -0.000000000000000000, 1.000000000000000000 ) ) ;
#8584=CARTESIAN_POINT ( 'NONE',  ( -45.00000000000000711, -19.03270077640482683, 10.53798182577225084 ) ) ;
#8586=CARTESIAN_POINT ( 'NONE',  ( 29.20951391065003122, -17.04067956308641030, 13.38411038749911697 ) ) ;
#8587=CARTESIAN_POINT ( 'NONE',  ( 25.71748644841968456, -2.420320648352046078, 5.783357778048663356 ) ) ;
#8595=ORIENTED_EDGE ( 'NONE', *, *, #16722, .F. ) ;
#8599=CARTESIAN_POINT ( 'NONE',  ( 27.93049598394382116, -4.671775696577297410, 7.939653947423662039 ) ) ;
#8612=EDGE_CURVE ( 'NONE', #14557, #1012, #14440, .T. ) ;
#8620=CARTESIAN_POINT ( 'NONE',  ( 28.60033944477555323, -4.591072787911525843, 3.283357778048664244 ) ) ;
#8622=ORIENTED_EDGE ( 'NONE', *, *, #7647, .F. ) ;
#8633=VECTOR ( 'NONE', #14250, 1000.000000000000000 ) ;
#8637=CARTESIAN_POINT ( 'NONE',  ( 29.98885399772409954, -6.604504582617394703, 7.033357778048657138 ) ) ;
#8644=CARTESIAN_POINT ( 'NONE',  ( 32.16857880351144416, -6.669052543620333395, 5.783357778048658027 ) ) ;
#8649=CARTESIAN_POINT ( 'NONE',  ( 25.86833963875586306, -3.039313213345869791, 6.861505862736166250 ) ) ;
#8650=CARTESIAN_POINT ( 'NONE',  ( -16.79042544672876858, -17.04069398696883297, 16.02996823657058911 ) ) ;
#8652=ORIENTED_EDGE ( 'NONE', *, *, #7764, .F. ) ;
#8656=CARTESIAN_POINT ( 'NONE',  ( 26.94172295629870462, -6.971623697019761146, 4.533357778048659803 ) ) ;
#8657=VERTEX_POINT ( 'NONE', #4855 ) ;
#8666=EDGE_CURVE ( 'NONE', #13857, #12121, #12253, .T. ) ;
#8667=CARTESIAN_POINT ( 'NONE',  ( 26.01652455409633902, -4.902371455920926380, 5.783357778048663356 ) ) ;
#8669=CARTESIAN_POINT ( 'NONE',  ( 29.54591158530375239, -2.596238420101622868, 4.705209693361168455 ) ) ;
#8670=AXIS2_PLACEMENT_3D ( 'NONE', #5744, #12560, #10002 ) ;
#8676=CARTESIAN_POINT ( 'NONE',  ( 28.73594040535616756, -2.066853418799292630, 5.783357778048668685 ) ) ;
#8680=ORIENTED_EDGE ( 'NONE', *, *, #11541, .F. ) ;
#8681=CARTESIAN_POINT ( 'NONE',  ( 27.91310269393460430, -7.181753375802955475, 5.783357778048657138 ) ) ;
#8685=AXIS2_PLACEMENT_3D ( 'NONE', #3069, #5768, #15573 ) ;
#8686=VECTOR ( 'NONE', #9350, 1000.000000000000000 ) ;
#8692=AXIS2_PLACEMENT_3D ( 'NONE', #13909, #1237, #16641 ) ;
#8697=ORIENTED_EDGE ( 'NONE', *, *, #6725, .F. ) ;
#8699=CARTESIAN_POINT ( 'NONE',  ( 27.72904566057427189, -3.442105416578421284, 7.939653947423662927 ) ) ;
#8701=CARTESIAN_POINT ( 'NONE',  ( 33.48062616923409252, 0.02583177435456097265, 5.783357778048664244 ) ) ;
#8702=AXIS2_PLACEMENT_3D ( 'NONE', #13524, #16167, #17731 ) ;
#8703=CARTESIAN_POINT ( 'NONE',  ( 31.26353094466156080, -6.788289799823394866, 5.783357778048664244 ) ) ;
#8708=CARTESIAN_POINT ( 'NONE',  ( -5.499998387031001634, -20.49508120620799900, 13.00000000000000178 ) ) ;
#8719=MECHANICAL_DESIGN_GEOMETRIC_PRESENTATION_REPRESENTATION('',(#4649),#5511);
#8720=CARTESIAN_POINT ( 'NONE',  ( 27.49335874655903567, -6.905162478240574053, 4.533357778048659803 ) ) ;
#8726=ORIENTED_EDGE ( 'NONE', *, *, #3564, .T. ) ;
#8741=ADVANCED_FACE ( 'NONE', ( #3172 ), #7442, .F. ) ;
#8743=VECTOR ( 'NONE', #11380, 1000.000000000000114 ) ;
#8744=CARTESIAN_POINT ( 'NONE',  ( 31.88814493096863956, -1.687075024589942851, 5.783357778048668685 ) ) ;
#8745=VECTOR ( 'NONE', #377, 999.9999999999998863 ) ;
#8748=CARTESIAN_POINT ( 'NONE',  ( -22.62145100412528009, -22.46994790986326151, 15.00472644746570694 ) ) ;
#8754=LINE ( 'NONE', #11353, #8986 ) ;
#8756=ORIENTED_EDGE ( 'NONE', *, *, #9257, .F. ) ;
#8767=CARTESIAN_POINT ( 'NONE',  ( 31.43723430067123914, -2.368371383576012956, 4.705209693361168455 ) ) ;
#8769=AXIS2_PLACEMENT_3D ( 'NONE', #11837, #4854, #9040 ) ;
#8772=CARTESIAN_POINT ( 'NONE',  ( 32.93470988637010066, -5.949778345213319497, 4.705209693361159573 ) ) ;
#8777=EDGE_CURVE ( 'NONE', #6631, #11016, #545, .T. ) ;
#8778=FACE_OUTER_BOUND ( 'NONE', #12879, .T. ) ;
#8788=CARTESIAN_POINT ( 'NONE',  ( 19.71718888926881164, -28.93397812220195675, 15.64003640126281347 ) ) ;
#8789=CARTESIAN_POINT ( 'NONE',  ( 32.14656953781143756, -4.163822094218565972, 8.283357778048662468 ) ) ;
#8794=DIRECTION ( 'NONE',  ( 0.9928203230275510771, 0.1196152422706609902, 4.006172263299092517E-17 ) ) ;
#8795=CARTESIAN_POINT ( 'NONE',  ( 33.44685390376565692, -4.007163506710925027, 3.627061608673664228 ) ) ;
#8798=EDGE_CURVE ( 'NONE', #16186, #5245, #7179, .T. ) ;
#8801=CARTESIAN_POINT ( 'NONE',  ( 45.00000000000000711, -16.03270077640482683, 0.5379818257722508434 ) ) ;
#8807=ORIENTED_EDGE ( 'NONE', *, *, #17630, .T. ) ;
#8813=CARTESIAN_POINT ( 'NONE',  ( 29.07687923786957285, -2.352938776424351008, 4.533357778048667797 ) ) ;
#8815=ORIENTED_EDGE ( 'NONE', *, *, #12160, .F. ) ;
#8818=EDGE_CURVE ( 'NONE', #1659, #10101, #12122, .T. ) ;
#8820=DIRECTION ( 'NONE',  ( -1.000000000000000000, 0.000000000000000000, 0.000000000000000000 ) ) ;
#8830=CARTESIAN_POINT ( 'NONE',  ( 31.38469755857769528, -2.374701023479507178, 6.861505862736165362 ) ) ;
#8832=CARTESIAN_POINT ( 'NONE',  ( -35.41536221060850664, -16.03270077640482683, 0.5379818257722508434 ) ) ;
#8833=CARTESIAN_POINT ( 'NONE',  ( 28.11132641904908169, -7.168068194032743534, 5.783357778048657138 ) ) ;
#8849=CARTESIAN_POINT ( 'NONE',  ( 33.95908713831676096, -3.945449517755638791, 8.283357778048662468 ) ) ;
#8851=B_SPLINE_CURVE_WITH_KNOTS ( 'NONE', 1,
 ( #16287, #14657 ),
 .UNSPECIFIED., .F., .F.,
 ( 2, 2 ),
 ( 0.000000000000000000, 1.000000000000000000 ),
 .UNSPECIFIED. ) ;
#8854=CARTESIAN_POINT ( 'NONE',  ( 26.34117031759772942, -2.982346454214467535, 6.861505862736165362 ) ) ;
#8860=LINE ( 'NONE', #11659, #290 ) ;
#8861=EDGE_CURVE ( 'NONE', #4895, #11071, #17715, .T. ) ;
#8866=CARTESIAN_POINT ( 'NONE',  ( 27.95193767517966776, -20.05341752217977103, 13.73231903009881627 ) ) ;
#8870=VERTEX_POINT ( 'NONE', #16239 ) ;
#8872=CARTESIAN_POINT ( 'NONE',  ( 31.92138306490751987, -2.737139032229836122, 8.283357778048664244 ) ) ;
#8875=VERTEX_POINT ( 'NONE', #10756 ) ;
#8876=( BOUNDED_CURVE ( )  B_SPLINE_CURVE ( 2, ( #2386, #6803, #7903, #7812, #1095, #17895, #5249, #13341, #9422 ),
 .UNSPECIFIED., .F., .T. ) 
 B_SPLINE_CURVE_WITH_KNOTS ( ( 3, 2, 2, 2, 3 ),
 ( 0.6346153846153846922, 0.6410256410256410797, 0.6538461538461538547, 0.6666666666666666297, 0.6730769230769231282 ),
 .UNSPECIFIED. ) 
 CURVE ( )  GEOMETRIC_REPRESENTATION_ITEM ( )  RATIONAL_B_SPLINE_CURVE ( ( 0.9330127018922192983, 0.9330127018922198534, 1.000000000000000000, 0.8660254037844387076, 1.000000000000000000, 0.8660254037844387076, 1.000000000000000000, 0.9330127018922187432, 0.9330127018922192983 ) ) 
 REPRESENTATION_ITEM ( '' )  );
#8878=CARTESIAN_POINT ( 'NONE',  ( -23.02601376483258022, 3.965314980223224151, 0.000000000000000000 ) ) ;
#8879=CARTESIAN_POINT ( 'NONE',  ( -23.00000000000000000, -16.21813761408365195, -0.000000000000000000 ) ) ;
#8890=VERTEX_POINT ( 'NONE', #3812 ) ;
#8891=ORIENTED_EDGE ( 'NONE', *, *, #6355, .T. ) ;
#8896=EDGE_CURVE ( 'NONE', #172, #4942, #5180, .T. ) ;
#8897=CARTESIAN_POINT ( 'NONE',  ( 29.98133424373737910, -5.878503772023492502, 3.283357778048663800 ) ) ;
#8900=CARTESIAN_POINT ( 'NONE',  ( 25.98779870451785001, -2.387753359738024272, 5.113484796970856117 ) ) ;
#8903=ORIENTED_EDGE ( 'NONE', *, *, #4901, .F. ) ;
#8906=VERTEX_POINT ( 'NONE', #1437 ) ;
#8916=LINE ( 'NONE', #17189, #12954 ) ;
#8917=CARTESIAN_POINT ( 'NONE',  ( 30.62726312072365431, -1.838986382273682718, 5.783357778048668685 ) ) ;
#8925=CARTESIAN_POINT ( 'NONE',  ( 33.13353876934985465, -5.498725377814142057, 3.283357778048663356 ) ) ;
#8929=CARTESIAN_POINT ( 'NONE',  ( -23.00000000000000000, -16.21813761408365195, -0.000000000000000000 ) ) ;
#8934=EDGE_CURVE ( 'NONE', #7391, #1468, #17741, .T. ) ;
#8935=CARTESIAN_POINT ( 'NONE',  ( 25.96860978910007844, -6.167287525404733017, 4.026412830637841722 ) ) ;
#8940=CARTESIAN_POINT ( 'NONE',  ( 32.50119254608192421, -4.121097024973739309, 7.939653947423662039 ) ) ;
#8941=CARTESIAN_POINT ( 'NONE',  ( -28.41103551745680633, -13.06362195986656616, 13.60745115249024728 ) ) ;
#8943=ADVANCED_FACE ( 'NONE', ( #11021 ), #2622, .F. ) ;
#8946=AXIS2_PLACEMENT_3D ( 'NONE', #5168, #16434, #2647 ) ;
#8956=CARTESIAN_POINT ( 'NONE',  ( 32.41296236253129592, -1.951006642345344044, 7.033357778048666020 ) ) ;
#8961=VERTEX_POINT ( 'NONE', #79 ) ;
#8962=LINE ( 'NONE', #16140, #13543 ) ;
#8964=CARTESIAN_POINT ( 'NONE',  ( 32.04575515724927470, -1.668086104879473730, 5.783357778048668685 ) ) ;
#8965=EDGE_CURVE ( 'NONE', #17429, #2247, #1257, .T. ) ;
#8971=DIRECTION ( 'NONE',  ( 0.9928203230275510771, 0.1196152422706609902, 4.006172263299092517E-17 ) ) ;
#8975=CARTESIAN_POINT ( 'NONE',  ( 16.96391960790757736, -14.58372395263535282, 16.00480323547922978 ) ) ;
#8982=CIRCLE ( 'NONE', #6096, 3.999999999999994671 ) ;
#8984=DIRECTION ( 'NONE',  ( 0.000000000000000000, 0.000000000000000000, -1.000000000000000000 ) ) ;
#8985=CARTESIAN_POINT ( 'NONE',  ( 28.72045243349238675, -6.030415129707233035, 3.283357778048663800 ) ) ;
#8986=VECTOR ( 'NONE', #494, 1000.000000000000227 ) ;
#9001=DIRECTION ( 'NONE',  ( 0.9928203230275510771, 0.1196152422706609902, 4.006172263299092517E-17 ) ) ;
#9006=AXIS2_PLACEMENT_3D ( 'NONE', #3353, #807, #15965 ) ;
#9010=DIRECTION ( 'NONE',  ( 0.9928203230275512992, 0.1196152422706610180, 4.006172263299093133E-17 ) ) ;
#9012=CARTESIAN_POINT ( 'NONE',  ( -3.538288549924106796, -15.34800872113743431, 16.99955934415556769 ) ) ;
#9016=EDGE_CURVE ( 'NONE', #10739, #8961, #4248, .T. ) ;
#9017=CARTESIAN_POINT ( 'NONE',  ( 33.16732689266149237, -6.221561368663743430, 4.533357778048659803 ) ) ;
#9020=AXIS2_PLACEMENT_3D ( 'NONE', #12423, #4186, #9687 ) ;
#9026=CARTESIAN_POINT ( 'NONE',  ( 25.74134610602432360, -2.427642893298174620, 5.783357778048668685 ) ) ;
#9032=ORIENTED_EDGE ( 'NONE', *, *, #7265, .T. ) ;
#9033=CARTESIAN_POINT ( 'NONE',  ( 33.33308377457396432, -5.274811626130743392, 7.939653947423658487 ) ) ;
#9040=DIRECTION ( 'NONE',  ( -0.1196152422706621143, -0.9928203230275509661, -0.000000000000000000 ) ) ;
#9043=CARTESIAN_POINT ( 'NONE',  ( 31.03132594549780876, -1.780107929003061473, 5.113484796970860558 ) ) ;
#9048=ADVANCED_FACE ( 'NONE', ( #11386 ), #1712, .T. ) ;
#9050=VECTOR ( 'NONE', #9917, 1000.000000000000000 ) ;
#9051=CARTESIAN_POINT ( 'NONE',  ( 30.52163964716380917, -2.178873678870954400, 7.033357778048666020 ) ) ;
#9057=CARTESIAN_POINT ( 'NONE',  ( 32.80318959510331212, -2.203800746085299522, 6.861505862736166250 ) ) ;
#9059=CARTESIAN_POINT ( 'NONE',  ( 45.50000000000000000, -16.03270077640482683, 5.537981825772250843 ) ) ;
#9070=CARTESIAN_POINT ( 'NONE',  ( -18.96667930129623514, 9.308258642545592210, 15.69246997591053017 ) ) ;
#9078=CARTESIAN_POINT ( 'NONE',  ( 25.93714794488954212, -2.393855775999666591, 5.783357778048667797 ) ) ;
#9079=CARTESIAN_POINT ( 'NONE',  ( 25.95846283556873502, -3.455553161483296609, 3.283357778048666464 ) ) ;
#9087=EDGE_LOOP ( 'NONE', ( #16301, #12192, #12592, #11143 ) ) ;
#9092=DIRECTION ( 'NONE',  ( -0.8243186046180107640, 0.5661261679878573094, 0.000000000000000000 ) ) ;
#9103=CARTESIAN_POINT ( 'NONE',  ( 25.90419076669538967, -3.969988049114257400, 3.653240910513405382 ) ) ;
#9104=PRODUCT ( 'MirrorCaliper Body Half', 'MirrorCaliper Body Half', '', ( #1783 ) ) ;
#9108=CARTESIAN_POINT ( 'NONE',  ( 32.89331279191618762, -2.620040694222726785, 3.283357778048666464 ) ) ;
#9112=CARTESIAN_POINT ( 'NONE',  ( -15.92260893619738837, -28.39189527176317540, 12.00000000000000000 ) ) ;
#9118=CARTESIAN_POINT ( 'NONE',  ( 29.47916769939009285, -7.003270332485284300, 5.113484796970857005 ) ) ;
#9119=CARTESIAN_POINT ( 'NONE',  ( 28.49970350196817392, -5.857138497251738407, 3.627061608673662896 ) ) ;
#9124=CARTESIAN_POINT ( 'NONE',  ( 25.71072941247523502, -3.058302133056337357, 6.861505862736165362 ) ) ;
#9125=CARTESIAN_POINT ( 'NONE',  ( 27.27683486999669427, -2.232449958253242883, 5.783357778048667797 ) ) ;
#9129=DIRECTION ( 'NONE',  ( 0.000000000000000000, 0.000000000000000000, -1.000000000000000000 ) ) ;
#9130=DIRECTION ( 'NONE',  ( 0.1196152422706596996, -0.9928203230275514102, 0.000000000000000000 ) ) ;
#9135=CARTESIAN_POINT ( 'NONE',  ( 31.08079519141086067, -2.838413270685653078, 3.283357778048666464 ) ) ;
#9141=CARTESIAN_POINT ( 'NONE',  ( 31.04700706809921940, -2.115577279836057922, 4.533357778048667797 ) ) ;
#9143=VERTEX_POINT ( 'NONE', #446 ) ;
#9146=ORIENTED_EDGE ( 'NONE', *, *, #6355, .F. ) ;
#9147=CARTESIAN_POINT ( 'NONE',  ( 33.27602027394517847, -2.146833986953896822, 6.861505862736165362 ) ) ;
#9148=CARTESIAN_POINT ( 'NONE',  ( 32.32618902979206865, -6.650063623909865385, 5.783357778048657138 ) ) ;
#9154=EDGE_CURVE ( 'NONE', #4193, #10223, #5405, .T. ) ;
#9155=DIRECTION ( 'NONE',  ( 0.000000000000000000, 0.000000000000000000, -1.000000000000000000 ) ) ;
#9156=DIRECTION ( 'NONE',  ( 1.000000000000000000, 0.000000000000000000, 0.000000000000000000 ) ) ;
#9157=CYLINDRICAL_SURFACE ( 'NONE', #16883, 95.00000000000000000 ) ;
#9164=CARTESIAN_POINT ( 'NONE',  ( 26.89670596474818609, -7.703954147932045693, 5.783357778048657138 ) ) ;
#9165=EDGE_CURVE ( 'NONE', #9649, #11134, #619, .T. ) ;
#9170=CARTESIAN_POINT ( 'NONE',  ( -34.91600907648203389, -11.88801210197604341, -0.000000000000000000 ) ) ;
#9171=DIRECTION ( 'NONE',  ( -0.1196152422706610735, 0.9928203230275511881, 0.000000000000000000 ) ) ;
#9183=CARTESIAN_POINT ( 'NONE',  ( 32.96626681528915981, -4.065064760026301016, 5.783357778048663356 ) ) ;
#9184=EDGE_CURVE ( 'NONE', #7076, #12891, #6641, .T. ) ;
#9190=DIRECTION ( 'NONE',  ( 0.000000000000000000, 1.000000000000000000, 0.000000000000000000 ) ) ;
#9195=FACE_OUTER_BOUND ( 'NONE', #9995, .T. ) ;
#9198=CARTESIAN_POINT ( 'NONE',  ( 33.73390066541284682, -2.518766455766908940, 8.283357778048666020 ) ) ;
#9199=CARTESIAN_POINT ( 'NONE',  ( 28.30694982360322953, -3.372479377640031473, 3.627061608673666893 ) ) ;
#9202=CARTESIAN_POINT ( 'NONE',  ( 31.06530721954707985, -6.801974981593605030, 5.783357778048657138 ) ) ;
#9203=CARTESIAN_POINT ( 'NONE',  ( -28.84390385427241199, -13.99246034770667713, 13.48718205731130304 ) ) ;
#9206=DIRECTION ( 'NONE',  ( 0.000000000000000000, 0.000000000000000000, -1.000000000000000000 ) ) ;
#9207=LINE ( 'NONE', #14754, #8389 ) ;
#9209=CARTESIAN_POINT ( 'NONE',  ( 26.01652455409633902, -4.902371455920936150, 5.783357778048662468 ) ) ;
#9212=EDGE_CURVE ( 'NONE', #10101, #15493, #7340, .T. ) ;
#9214=CIRCLE ( 'NONE', #17370, 2.749999999999995559 ) ;
#9219=DIRECTION ( 'NONE',  ( 1.000000000000000000, 0.000000000000000000, 0.000000000000000000 ) ) ;
#9220=CARTESIAN_POINT ( 'NONE',  ( 27.95866967485789090, -6.122194908100387245, 8.283357778048658915 ) ) ;
#9223=AXIS2_PLACEMENT_3D ( 'NONE', #2705, #12389, #11010 ) ;
#9225=CARTESIAN_POINT ( 'NONE',  ( 31.51621784984448738, -6.120678622607529817, 4.705209693361160461 ) ) ;
#9226=CARTESIAN_POINT ( 'NONE',  ( 29.03376756790819613, -4.538853258604016006, 3.627061608673664228 ) ) ;
#9229=DIRECTION ( 'NONE',  ( 1.000000000000000000, 0.000000000000000000, 0.000000000000000000 ) ) ;
#9231=CARTESIAN_POINT ( 'NONE',  ( 29.06119811526816576, -2.017469425591354337, 5.113484796970861446 ) ) ;
#9233=CARTESIAN_POINT ( 'NONE',  ( -27.17934203385504333, -30.00000000000000355, -0.000000000000000000 ) ) ;
#9243=CARTESIAN_POINT ( 'NONE',  ( 5.500000000000000888, -20.49999999999999645, 13.00000000000000178 ) ) ;
#9249=CARTESIAN_POINT ( 'NONE',  ( 26.01595305975170547, -2.384361315936983416, 5.783357778048657138 ) ) ;
#9253=CARTESIAN_POINT ( 'NONE',  ( 25.76524775868382733, -2.816745038626285780, 6.289456735611078209 ) ) ;
#9256=VECTOR ( 'NONE', #12666, 1000.000000000000000 ) ;
#9257=EDGE_CURVE ( 'NONE', #17832, #13537, #4906, .T. ) ;
#9266=EDGE_CURVE ( 'NONE', #8870, #9288, #15487, .T. ) ;
#9267=AXIS2_PLACEMENT_3D ( 'NONE', #17110, #4662, #10190 ) ;
#9271=VERTEX_POINT ( 'NONE', #14597 ) ;
#9272=DIRECTION ( 'NONE',  ( 1.000000000000000000, 0.000000000000000000, 0.000000000000000000 ) ) ;
#9279=CARTESIAN_POINT ( 'NONE',  ( -2.016448651773435938E-27, -20.49999999999999645, 13.00000000000000355 ) ) ;
#9282=CYLINDRICAL_SURFACE ( 'NONE', #15554, 2.000000000000001776 ) ;
#9283=AXIS2_PLACEMENT_3D ( 'NONE', #1736, #17164, #7537 ) ;
#9287=CARTESIAN_POINT ( 'NONE',  ( 31.90644508241650357, -6.373472726347483963, 4.533357778048659803 ) ) ;
#9288=VERTEX_POINT ( 'NONE', #3690 ) ;
#9290=VECTOR ( 'NONE', #8971, 1000.000000000000227 ) ;
#9292=CARTESIAN_POINT ( 'NONE',  ( 28.89355063163679915, -2.047864499088824175, 5.783357778048668685 ) ) ;
#9293=CARTESIAN_POINT ( 'NONE',  ( -29.08686357714922011, -14.78463821260646860, 13.41883458853107669 ) ) ;
#9294=CARTESIAN_POINT ( 'NONE',  ( 20.84394630543432569, -22.08803114836474890, 15.35658910651175013 ) ) ;
#9296=ORIENTED_EDGE ( 'NONE', *, *, #15901, .T. ) ;
#9300=LINE ( 'NONE', #10726, #3538 ) ;
#9306=CARTESIAN_POINT ( 'NONE',  ( -45.50000000000000000, -16.03270077640482683, 8.287981825772241962 ) ) ;
#9310=CARTESIAN_POINT ( 'NONE',  ( 27.41826274939272423, -4.733489685532582314, 3.283357778048664244 ) ) ;
#9313=ORIENTED_EDGE ( 'NONE', *, *, #7444, .T. ) ;
#9315=CARTESIAN_POINT ( 'NONE',  ( 32.01513846370018967, -2.298745344637636912, 6.861505862736165362 ) ) ;
#9316=CARTESIAN_POINT ( 'NONE',  ( 31.24031073583692475, -4.273008382657478954, 7.939653947423662039 ) ) ;
#9317=ORIENTED_EDGE ( 'NONE', *, *, #2827, .T. ) ;
#9318=FACE_OUTER_BOUND ( 'NONE', #15024, .T. ) ;
#9319=CARTESIAN_POINT ( 'NONE',  ( 33.15485366002904755, -6.560422763297783177, 5.783357778048664244 ) ) ;
#9322=CIRCLE ( 'NONE', #1515, 14.00000000000000178 ) ;
#9327=LINE ( 'NONE', #6603, #6635 ) ;
#9328=CARTESIAN_POINT ( 'NONE',  ( 17.15697743806116549, -13.99005979112454767, 15.97644891051836957 ) ) ;
#9337=CARTESIAN_POINT ( 'NONE',  ( 32.54050588463559990, -2.235448945602741766, 4.705209693361167567 ) ) ;
#9339=CARTESIAN_POINT ( 'NONE',  ( -45.00000000000000711, -16.03270077640482683, 5.537981825772250843 ) ) ;
#9340=CARTESIAN_POINT ( 'NONE',  ( 32.61569110240115776, -6.288022587442930522, 4.533357778048659803 ) ) ;
#9350=DIRECTION ( 'NONE',  ( 0.000000000000000000, 0.000000000000000000, -1.000000000000000000 ) ) ;
#9360=CARTESIAN_POINT ( 'NONE',  ( 11.38175538881591287, -22.33742387525453665, 16.67884400577319681 ) ) ;
#9364=CARTESIAN_POINT ( 'NONE',  ( 31.87265695910486230, -5.650636735497883478, 3.283357778048663356 ) ) ;
#9365=DIRECTION ( 'NONE',  ( -0.1196152422706610735, 0.9928203230275511881, 0.000000000000000000 ) ) ;
#9368=CARTESIAN_POINT ( 'NONE',  ( 31.63243098167119172, -2.771952051906466874, 3.283357778048666464 ) ) ;
#9372=CARTESIAN_POINT ( 'NONE',  ( 29.54591158530375239, -2.596238420101622868, 4.705209693361168455 ) ) ;
#9373=CARTESIAN_POINT ( 'NONE',  ( -19.22778933661430756, -11.21824206523807099, 15.64718775662042560 ) ) ;
#9374=CARTESIAN_POINT ( 'NONE',  ( 25.20704250852812933, -22.06899625087205763, 14.42769424659100785 ) ) ;
#9375=EDGE_LOOP ( 'NONE', ( #13688, #9607, #4317, #3867 ) ) ;
#9383=DIRECTION ( 'NONE',  ( -0.9928203230275514102, -0.1196152422706598939, -0.000000000000000000 ) ) ;
#9384=CARTESIAN_POINT ( 'NONE',  ( 29.70732014299206369, -2.276983097582480742, 4.533357778048667797 ) ) ;
#9386=CARTESIAN_POINT ( 'NONE',  ( 26.99805802979993885, -6.665027654307603022, 6.861505862736158257 ) ) ;
#9387=PRODUCT_DEFINITION_SHAPE ( 'NONE', 'NONE',  #5901 ) ;
#9391=CARTESIAN_POINT ( 'NONE',  ( 32.82963640218302004, -5.962437625020304388, 6.861505862736157368 ) ) ;
#9392=CARTESIAN_POINT ( 'NONE',  ( 29.42969845347704450, -5.944964990802679594, 3.283357778048663800 ) ) ;
#9396=ORIENTED_EDGE ( 'NONE', *, *, #6529, .T. ) ;
#9397=CARTESIAN_POINT ( 'NONE',  ( 33.19286683830256379, -2.783822866615540903, 3.627061608673666893 ) ) ;
#9399=CARTESIAN_POINT ( 'NONE',  ( 30.30787278169304244, -6.266260340387784566, 6.861505862736157368 ) ) ;
#9400=VERTEX_POINT ( 'NONE', #5042 ) ;
#9402=DIRECTION ( 'NONE',  ( 0.9928203230275510771, 0.1196152422706609902, 4.006172263299092517E-17 ) ) ;
#9403=CARTESIAN_POINT ( 'NONE',  ( 34.91377932259078420, -11.86950488720510322, 11.57182824616228878 ) ) ;
#9405=CARTESIAN_POINT ( 'NONE',  ( 29.74794773085836397, -1.934729659147405689, 6.453230759126469707 ) ) ;
#9410=CARTESIAN_POINT ( 'NONE',  ( 27.95350797341489368, -12.38528642892598342, 13.73189064827997541 ) ) ;
#9412=EDGE_CURVE ( 'NONE', #1473, #8190, #11666, .T. ) ;
#9415=EDGE_LOOP ( 'NONE', ( #10775, #281 ) ) ;
#9416=CARTESIAN_POINT ( 'NONE',  ( -27.17934203385504333, -30.00000000000000355, 13.93658524716016878 ) ) ;
#9419=CARTESIAN_POINT ( 'NONE',  ( 30.76748005699505129, -4.329975141788874993, 3.627061608673664228 ) ) ;
#9422=CARTESIAN_POINT ( 'NONE',  ( 28.19013153391124860, -7.158573733970061248, 5.783357778048669573 ) ) ;
#9431=CARTESIAN_POINT ( 'NONE',  ( 31.68992120585416217, -1.700760206360153015, 5.783357778048662468 ) ) ;
#9438=CARTESIAN_POINT ( 'NONE',  ( -13.65694651542706595, -25.37101204406941335, 16.45580752066269881 ) ) ;
#9439=( BOUNDED_CURVE ( )  B_SPLINE_CURVE ( 2, ( #6224, #14487, #7683, #13208, #2249, #7763, #3507, #784, #7859 ),
 .UNSPECIFIED., .F., .T. ) 
 B_SPLINE_CURVE_WITH_KNOTS ( ( 3, 2, 2, 2, 3 ),
 ( 0.4038461538461538547, 0.4102564102564102422, 0.4230769230769230727, 0.4358974358974359031, 0.4423076923076923461 ),
 .UNSPECIFIED. ) 
 CURVE ( )  GEOMETRIC_REPRESENTATION_ITEM ( )  RATIONAL_B_SPLINE_CURVE ( ( 0.9330127018922194093, 0.9330127018922196314, 1.000000000000000000, 0.8660254037844387076, 1.000000000000000000, 0.8660254037844387076, 1.000000000000000000, 0.9330127018922190762, 0.9330127018922194093 ) ) 
 REPRESENTATION_ITEM ( '' )  );
#9442=ORIENTED_EDGE ( 'NONE', *, *, #12736, .T. ) ;
#9445=ORIENTED_EDGE ( 'NONE', *, *, #9478, .F. ) ;
#9454=CARTESIAN_POINT ( 'NONE',  ( 33.01342578063301403, -4.059383036018435753, 3.283357778048664244 ) ) ;
#9458=CARTESIAN_POINT ( 'NONE',  ( 31.04338717100262102, -6.177645381738930297, 4.705209693361159573 ) ) ;
#9461=ORIENTED_EDGE ( 'NONE', *, *, #9257, .T. ) ;
#9466=PLANE ( 'NONE',  #547 ) ;
#9467=CARTESIAN_POINT ( 'NONE',  ( 29.98133424373737199, -5.878503772023492502, 3.283357778048663356 ) ) ;
#9469=CARTESIAN_POINT ( 'NONE',  ( 26.66961417369883591, -4.823687054261037055, 7.939653947423662039 ) ) ;
#9470=CARTESIAN_POINT ( 'NONE',  ( 30.25080928106424594, -3.138282701210941994, 7.939653947423664704 ) ) ;
#9471=EDGE_CURVE ( 'NONE', #8870, #10739, #13837, .T. ) ;
#9474=CARTESIAN_POINT ( 'NONE',  ( 32.67619606237177265, -1.592130426037603907, 5.783357778048668685 ) ) ;
#9476=CARTESIAN_POINT ( 'NONE',  ( 28.04870365451522218, -4.657534006690712935, 3.283357778048664244 ) ) ;
#9478=EDGE_CURVE ( 'NONE', #2213, #15493, #4624, .T. ) ;
#9480=VERTEX_POINT ( 'NONE', #15007 ) ;
#9481=CARTESIAN_POINT ( 'NONE',  ( 32.16857880351144416, -6.669052543620333395, 5.783357778048658027 ) ) ;
#9483=VERTEX_POINT ( 'NONE', #8121 ) ;
#9484=CARTESIAN_POINT ( 'NONE',  ( 28.93739072872572393, -3.296523698798161650, 3.627061608673666449 ) ) ;
#9486=AXIS2_PLACEMENT_3D ( 'NONE', #6243, #13413, #11856 ) ;
#9492=CARTESIAN_POINT ( 'NONE',  ( -3.248936832696171617, -20.49508120620799900, -78.00000000000000000 ) ) ;
#9494=CARTESIAN_POINT ( 'NONE',  ( 26.90109536843240789, -7.313877135454839973, 6.453230759126468818 ) ) ;
#9495=ORIENTED_EDGE ( 'NONE', *, *, #16582, .F. ) ;
#9499=DIRECTION ( 'NONE',  ( 0.6000000000000001998, -0.7999999999999999334, 0.000000000000000000 ) ) ;
#9504=CARTESIAN_POINT ( 'NONE',  ( 32.14665875496697822, -6.044722943765660439, 4.705209693361160461 ) ) ;
#9510=FACE_OUTER_BOUND ( 'NONE', #5368, .T. ) ;
#9514=ORIENTED_EDGE ( 'NONE', *, *, #4609, .T. ) ;
#9523=DIRECTION ( 'NONE',  ( 0.1414213562373112243, -0.9899494936611663576, 0.000000000000000000 ) ) ;
#9524=EDGE_CURVE ( 'NONE', #16241, #9967, #9640, .T. ) ;
#9531=VERTEX_POINT ( 'NONE', #10818 ) ;
#9532=FACE_BOUND ( 'NONE', #7663, .T. ) ;
#9534=VECTOR ( 'NONE', #12098, 1000.000000000000000 ) ;
#9542=CARTESIAN_POINT ( 'NONE',  ( 29.14753769709988518, -3.271205139184214516, 7.939653947423664704 ) ) ;
#9544=CARTESIAN_POINT ( 'NONE',  ( 28.75424055680402802, -6.753251120556833520, 4.533357778048659803 ) ) ;
#9545=ORIENTED_EDGE ( 'NONE', *, *, #3902, .F. ) ;
#9548=CARTESIAN_POINT ( 'NONE',  ( 25.93714794488954212, -2.393855775999666591, 5.783357778048667797 ) ) ;
#9553=LINE ( 'NONE', #6845, #6622 ) ;
#9554=CARTESIAN_POINT ( 'NONE',  ( 27.80031630502317341, -2.169380783275094426, 5.113484796970861446 ) ) ;
#9555=CARTESIAN_POINT ( 'NONE',  ( 25.77727942049545717, -5.625018267156629115, 3.627061608673662452 ) ) ;
#9556=CARTESIAN_POINT ( 'NONE',  ( 29.38830135902312080, -2.615227339812091767, 4.705209693361167567 ) ) ;
#9558=CARTESIAN_POINT ( 'NONE',  ( 32.21340264088064487, -1.637691031382005669, 5.113484796970859669 ) ) ;
#9559=CARTESIAN_POINT ( 'NONE',  ( 32.93018312783485158, -2.815471066132994249, 7.939653947423664704 ) ) ;
#9560=( BOUNDED_CURVE ( )  B_SPLINE_CURVE ( 2, ( #8538, #15518, #9968, #11420, #5980, #8446, #3100, #196, #9782 ),
 .UNSPECIFIED., .F., .T. ) 
 B_SPLINE_CURVE_WITH_KNOTS ( ( 3, 2, 2, 2, 3 ),
 ( 0.8653846153846154188, 0.8717948717948718063, 0.8846153846153845812, 0.8974358974358974672, 0.9038461538461538547 ),
 .UNSPECIFIED. ) 
 CURVE ( )  GEOMETRIC_REPRESENTATION_ITEM ( )  RATIONAL_B_SPLINE_CURVE ( ( 0.9330127018922192983, 0.9330127018922198534, 1.000000000000000000, 0.8660254037844387076, 1.000000000000000000, 0.8660254037844387076, 1.000000000000000000, 0.9330127018922194093, 0.9330127018922194093 ) ) 
 REPRESENTATION_ITEM ( '' )  );
#9561=AXIS2_PLACEMENT_3D ( 'NONE', #4197, #15246, #2825 ) ;
#9564=CARTESIAN_POINT ( 'NONE',  ( 30.65370992780335868, -5.597623261208691581, 7.939653947423658487 ) ) ;
#9566=CARTESIAN_POINT ( 'NONE',  ( 30.15443244188179150, -1.895953141405083864, 5.783357778048668685 ) ) ;
#9570=CARTESIAN_POINT ( 'NONE',  ( -20.00000000000000355, 7.999999999999996447, 6.000000000000000000 ) ) ;
#9571=CARTESIAN_POINT ( 'NONE',  ( -50.00000000000000000, -16.03270077640482683, 5.537981825772250843 ) ) ;
#9573=FACE_OUTER_BOUND ( 'NONE', #1677, .T. ) ;
#9574=CARTESIAN_POINT ( 'NONE',  ( 20.00000000000000355, -30.00000000000000355, 17.00000000000000000 ) ) ;
#9575=CARTESIAN_POINT ( 'NONE',  ( 25.76366024945007638, -10.60870341083598056, 14.29366788170017699 ) ) ;
#9580=EDGE_LOOP ( 'NONE', ( #2065, #346, #12822, #11635, #7098 ) ) ;
#9584=ORIENTED_EDGE ( 'NONE', *, *, #16567, .T. ) ;
#9585=CARTESIAN_POINT ( 'NONE',  ( 31.51621784984448738, -6.120678622607529817, 4.705209693361160461 ) ) ;
#9586=CIRCLE ( 'NONE', #2393, 2.749999999999988454 ) ;
#9588=EDGE_CURVE ( 'NONE', #4167, #6841, #7713, .T. ) ;
#9590=CARTESIAN_POINT ( 'NONE',  ( -25.74999999999998934, -16.21813761408365195, 13.00000000000000355 ) ) ;
#9597=ORIENTED_EDGE ( 'NONE', *, *, #12618, .T. ) ;
#9607=ORIENTED_EDGE ( 'NONE', *, *, #7188, .T. ) ;
#9617=CARTESIAN_POINT ( 'NONE',  ( -25.11802603177690330, -16.03270077640482683, 0.5379818257722508434 ) ) ;
#9625=EDGE_CURVE ( 'NONE', #10340, #1236, #8480, .T. ) ;
#9629=CARTESIAN_POINT ( 'NONE',  ( 25.76326615456878244, -3.051972493152843580, 4.705209693361168455 ) ) ;
#9631=CARTESIAN_POINT ( 'NONE',  ( 16.75000000000000355, -16.63579488892710145, 16.03574476417184158 ) ) ;
#9632=EDGE_LOOP ( 'NONE', ( #6023, #9669, #7451, #3185 ) ) ;
#9633=DIRECTION ( 'NONE',  ( 0.000000000000000000, 0.000000000000000000, 1.000000000000000000 ) ) ;
#9634=ORIENTED_EDGE ( 'NONE', *, *, #14529, .T. ) ;
#9635=LINE ( 'NONE', #8022, #6654 ) ;
#9636=VERTEX_POINT ( 'NONE', #7131 ) ;
#9640=LINE ( 'NONE', #10900, #5475 ) ;
#9644=CARTESIAN_POINT ( 'NONE',  ( 29.62489513447700062, -6.348545659133139729, 4.705209693361160461 ) ) ;
#9648=ORIENTED_EDGE ( 'NONE', *, *, #9524, .T. ) ;
#9649=VERTEX_POINT ( 'NONE', #9818 ) ;
#9650=CARTESIAN_POINT ( 'NONE',  ( 26.84461768998868436, -2.294720455324902542, 5.783357778048668685 ) ) ;
#9651=DIRECTION ( 'NONE',  ( -0.000000000000000000, -1.000000000000000000, -0.000000000000000000 ) ) ;
#9653=CARTESIAN_POINT ( 'NONE',  ( 27.65458886993626564, -2.824105456627233224, 4.705209693361168455 ) ) ;
#9655=LINE ( 'NONE', #13673, #4031 ) ;
#9656=CARTESIAN_POINT ( 'NONE',  ( 31.34233605952372415, -6.778795339760710803, 5.783357778048664244 ) ) ;
#9661=FACE_OUTER_BOUND ( 'NONE', #15199, .T. ) ;
#9662=CARTESIAN_POINT ( 'NONE',  ( 27.69360539047986336, -12.07076363665953345, 13.80168160306295810 ) ) ;
#9664=ORIENTED_EDGE ( 'NONE', *, *, #16624, .T. ) ;
#9669=ORIENTED_EDGE ( 'NONE', *, *, #6725, .T. ) ;
#9670=CYLINDRICAL_SURFACE ( 'NONE', #12112, 5.000000000000001776 ) ;
#9674=CARTESIAN_POINT ( 'NONE',  ( 31.49429780130001788, -5.496349022752856861, 3.627061608673662896 ) ) ;
#9687=DIRECTION ( 'NONE',  ( 0.1196152422706605323, -0.9928203230275512992, 0.000000000000000000 ) ) ;
#9688=FACE_OUTER_BOUND ( 'NONE', #13430, .T. ) ;
#9691=EDGE_CURVE ( 'NONE', #5666, #17327, #3191, .T. ) ;
#9693=VERTEX_POINT ( 'NONE', #4570 ) ;
#9694=ADVANCED_FACE ( 'NONE', ( #5742 ), #15544, .F. ) ;
#9698=DIRECTION ( 'NONE',  ( -0.000000000000000000, 1.000000000000000000, -3.469446951953614189E-16 ) ) ;
#9701=FACE_OUTER_BOUND ( 'NONE', #4269, .T. ) ;
#9702=VERTEX_POINT ( 'NONE', #15461 ) ;
#9709=LINE ( 'NONE', #1583, #5408 ) ;
#9711=ORIENTED_EDGE ( 'NONE', *, *, #4119, .F. ) ;
#9714=CARTESIAN_POINT ( 'NONE',  ( 33.09223089549517738, -4.049888575955752579, 3.283357778048664244 ) ) ;
#9721=CARTESIAN_POINT ( 'NONE',  ( 29.69163902039066372, -1.941513746749485847, 5.113484796970859669 ) ) ;
#9724=CIRCLE ( 'NONE', #1949, 6.249999999999998224 ) ;
#9725=CARTESIAN_POINT ( 'NONE',  ( 28.38593337277646711, -7.124786616671554107, 5.783357778048658027 ) ) ;
#9726=CARTESIAN_POINT ( 'NONE',  ( 45.50000000000000000, -16.03270077640482683, 8.287981825772238409 ) ) ;
#9731=CARTESIAN_POINT ( 'NONE',  ( 27.72904566057427189, -3.442105416578422172, 7.939653947423664704 ) ) ;
#9732=CARTESIAN_POINT ( 'NONE',  ( 26.73899421642883567, -2.634607751922174224, 7.033357778048666020 ) ) ;
#9733=ORIENTED_EDGE ( 'NONE', *, *, #3475, .F. ) ;
#9734=CARTESIAN_POINT ( 'NONE',  ( 27.25621498173240198, -3.499072175709823984, 7.939653947423662927 ) ) ;
#9735=VERTEX_POINT ( 'NONE', #1685 ) ;
#9740=CARTESIAN_POINT ( 'NONE',  ( 28.53771668024168662, -2.080538600569502794, 5.783357778048667797 ) ) ;
#9748=CARTESIAN_POINT ( 'NONE',  ( 26.31556265977298992, -7.384422263489805793, 5.783357778048663356 ) ) ;
#9756=ORIENTED_EDGE ( 'NONE', *, *, #528, .T. ) ;
#9757=CARTESIAN_POINT ( 'NONE',  ( 28.14933959732260149, -3.391468297350500372, 3.627061608673666449 ) ) ;
#9758=CARTESIAN_POINT ( 'NONE',  ( 31.80137159822941939, -6.386132006154467078, 7.033357778048657138 ) ) ;
#9773=FACE_OUTER_BOUND ( 'NONE', #4000, .T. ) ;
#9777=CARTESIAN_POINT ( 'NONE',  ( 31.70371634254663817, -2.036456781249897485, 7.033357778048666020 ) ) ;
#9782=CARTESIAN_POINT ( 'NONE',  ( 26.85044460880409645, -7.319979551716484067, 5.783357778048657138 ) ) ;
#9784=ADVANCED_FACE ( 'NONE', ( #7406 ), #6014, .F. ) ;
#9786=ORIENTED_EDGE ( 'NONE', *, *, #2827, .F. ) ;
#9791=VERTEX_POINT ( 'NONE', #3398 ) ;
#9803=CARTESIAN_POINT ( 'NONE',  ( 29.94002636988270538, -4.429666970165102136, 3.283357778048664244 ) ) ;
#9805=DIRECTION ( 'NONE',  ( 1.000000000000000000, 0.000000000000000000, 0.000000000000000000 ) ) ;
#9808=VERTEX_POINT ( 'NONE', #14737 ) ;
#9809=FACE_OUTER_BOUND ( 'NONE', #10517, .T. ) ;
#9812=CARTESIAN_POINT ( 'NONE',  ( 26.64639396487419987, -2.308405637095112706, 5.783357778048667797 ) ) ;
#9813=ADVANCED_FACE ( 'NONE', ( #2051 ), #7746, .T. ) ;
#9814=ORIENTED_EDGE ( 'NONE', *, *, #17303, .F. ) ;
#9818=CARTESIAN_POINT ( 'NONE',  ( 28.45891156537951971, -2.090033060632186412, 5.783357778048657138 ) ) ;
#9824=CARTESIAN_POINT ( 'NONE',  ( 31.54230778485832332, -2.355712103769039611, 6.861505862736166250 ) ) ;
#9830=CARTESIAN_POINT ( 'NONE',  ( 29.36638131047866196, -1.990897739957422807, 5.783357778048668685 ) ) ;
#9833=VECTOR ( 'NONE', #221, 1000.000000000000227 ) ;
#9835=CARTESIAN_POINT ( 'NONE',  ( 30.42903939560917337, -1.852671564043892660, 5.783357778048667797 ) ) ;
#9836=LINE ( 'NONE', #4415, #10078 ) ;
#9843=CARTESIAN_POINT ( 'NONE',  ( -3.248936832696171617, -15.16081378324841111, 17.00000000000000000 ) ) ;
#9850=EDGE_CURVE ( 'NONE', #5034, #16160, #10542, .T. ) ;
#9853=CARTESIAN_POINT ( 'NONE',  ( 30.12381574833269937, -2.526612381163247267, 6.861505862736165362 ) ) ;
#9855=DIRECTION ( 'NONE',  ( 0.000000000000000000, 0.000000000000000000, 1.000000000000000000 ) ) ;
#9857=CYLINDRICAL_SURFACE ( 'NONE', #14818, 2.500000000000001776 ) ;
#9859=VECTOR ( 'NONE', #12149, 1000.000000000000227 ) ;
#9861=CARTESIAN_POINT ( 'NONE',  ( 26.01652455409633902, -4.902371455920926380, 5.783357778048663356 ) ) ;
#9862=CIRCLE ( 'NONE', #3813, 5.000000000000000000 ) ;
#9865=VECTOR ( 'NONE', #12511, 1000.000000000000000 ) ;
#9868=CARTESIAN_POINT ( 'NONE',  ( 25.29083129957448151, -4.989803161779970964, 5.783357778048662468 ) ) ;
#9869=CARTESIAN_POINT ( 'NONE',  ( 32.95080301609915097, -1.548848848676412260, 5.783357778048663356 ) ) ;
#9870=CARTESIAN_POINT ( 'NONE',  ( 28.71361296893772774, -7.095504558991913235, 6.453230759126468818 ) ) ;
#9871=ADVANCED_FACE ( 'NONE', ( #4926 ), #10456, .F. ) ;
#9872=CARTESIAN_POINT ( 'NONE',  ( 30.64556327217151122, -6.525384084031224496, 4.533357778048659803 ) ) ;
#9874=AXIS2_PLACEMENT_3D ( 'NONE', #2227, #10538, #17290 ) ;
#9876=ORIENTED_EDGE ( 'NONE', *, *, #2277, .T. ) ;
#9877=ORIENTED_EDGE ( 'NONE', *, *, #6385, .T. ) ;
#9878=CIRCLE ( 'NONE', #3238, 2.500000000000001776 ) ;
#9883=EDGE_CURVE ( 'NONE', #11770, #5221, #8982, .T. ) ;
#9897=CARTESIAN_POINT ( 'NONE',  ( 26.00347982711925710, -2.723222710571018279, 4.533357778048667797 ) ) ;
#9900=CARTESIAN_POINT ( 'NONE',  ( 26.37178701114681800, -2.351687214456304353, 5.783357778048668685 ) ) ;
#9901=CARTESIAN_POINT ( 'NONE',  ( -28.59532824046058153, -19.01044845393195715, 13.55637998813296186 ) ) ;
#9903=EDGE_LOOP ( 'NONE', ( #5003, #5072 ) ) ;
#9904=VECTOR ( 'NONE', #16465, 1000.000000000000227 ) ;
#9917=DIRECTION ( 'NONE',  ( 0.000000000000000000, 0.000000000000000000, -1.000000000000000000 ) ) ;
#9919=CARTESIAN_POINT ( 'NONE',  ( 29.78250536075762867, -6.329556739422670830, 4.705209693361159573 ) ) ;
#9923=CARTESIAN_POINT ( 'NONE',  ( 26.99805802979993885, -6.665027654307603022, 6.861505862736158257 ) ) ;
#9924=FACE_OUTER_BOUND ( 'NONE', #15881, .T. ) ;
#9926=EDGE_CURVE ( 'NONE', #2813, #2213, #6207, .T. ) ;
#9928=CARTESIAN_POINT ( 'NONE',  ( 27.78610916120306129, -6.570083055755264745, 6.861505862736157368 ) ) ;
#9929=FACE_OUTER_BOUND ( 'NONE', #17380, .T. ) ;
#9931=CARTESIAN_POINT ( 'NONE',  ( 0.000000000000000000, 0.000000000000000000, 12.00000000000000000 ) ) ;
#9945=CARTESIAN_POINT ( 'NONE',  ( 26.84461768998868436, -2.294720455324902542, 5.783357778048668685 ) ) ;
#9949=CARTESIAN_POINT ( 'NONE',  ( 45.00000000000000711, -16.03270077640482683, 5.537981825772250843 ) ) ;
#9950=DIRECTION ( 'NONE',  ( -0.000000000000000000, -0.000000000000000000, 1.000000000000000000 ) ) ;
#9954=CARTESIAN_POINT ( 'NONE',  ( -45.00000000000000711, 0.000000000000000000, 5.537981825772250843 ) ) ;
#9963=CARTESIAN_POINT ( 'NONE',  ( 28.74176732417158320, -7.092112515190875044, 5.783357778048669573 ) ) ;
#9965=CARTESIAN_POINT ( 'NONE',  ( 28.12379965168153362, -6.829206799398704675, 4.533357778048659803 ) ) ;
#9966=DIRECTION ( 'NONE',  ( -0.1196152422706610735, 0.9928203230275511881, 0.000000000000000000 ) ) ;
#9967=VERTEX_POINT ( 'NONE', #7840 ) ;
#9968=CARTESIAN_POINT ( 'NONE',  ( 26.55511561737958814, -2.656761491791831187, 4.533357778048667797 ) ) ;
#9985=EDGE_CURVE ( 'NONE', #5245, #2179, #891, .T. ) ;
#9987=CARTESIAN_POINT ( 'NONE',  ( 32.12473870642251939, -5.420393343910986594, 3.627061608673662896 ) ) ;
#9988=CARTESIAN_POINT ( 'NONE',  ( 27.02867472334902033, -6.034368414549446058, 7.939653947423658487 ) ) ;
#9990=CARTESIAN_POINT ( 'NONE',  ( 29.54600080245929306, -4.477139269648729325, 8.283357778048662468 ) ) ;
#9992=CARTESIAN_POINT ( 'NONE',  ( 28.50956232500783472, -2.083930644370540985, 5.113484796970861446 ) ) ;
#9994=EDGE_CURVE ( 'NONE', #12240, #4518, #17428, .T. ) ;
#9995=EDGE_LOOP ( 'NONE', ( #2695, #6907, #14856, #7398 ) ) ;
#10002=DIRECTION ( 'NONE',  ( 0.000000000000000000, 0.000000000000000000, -1.000000000000000000 ) ) ;
#10007=CARTESIAN_POINT ( 'NONE',  ( 30.28142597461332741, -2.507623461452779701, 6.861505862736166250 ) ) ;
#10009=EDGE_LOOP ( 'NONE', ( #5412, #11608, #812, #13666 ) ) ;
#10012=CARTESIAN_POINT ( 'NONE',  ( 28.86293393808771057, -2.678523738846987357, 6.861505862736165362 ) ) ;
#10024=CARTESIAN_POINT ( 'NONE',  ( -3.347071143357316814, -15.22052928361022950, 17.00000000000000000 ) ) ;
#10035=CARTESIAN_POINT ( 'NONE',  ( 29.50659824675005893, -4.481886499472614638, 3.627061608673664228 ) ) ;
#10036=CARTESIAN_POINT ( 'NONE',  ( 31.21213704492286212, -2.822589171134389563, 8.283357778048666020 ) ) ;
#10037=CARTESIAN_POINT ( 'NONE',  ( 26.31176419598820360, -7.352894575460818594, 5.384699358761103838 ) ) ;
#10039=CARTESIAN_POINT ( 'NONE',  ( 15.92260893619738837, -28.39189527176317540, 12.00000000000000000 ) ) ;
#10046=CARTESIAN_POINT ( 'NONE',  ( -11.16099250167134826, 15.37423824781781079, 16.67067991271537863 ) ) ;
#10047=VERTEX_POINT ( 'NONE', #10144 ) ;
#10051=CYLINDRICAL_SURFACE ( 'NONE', #7772, 6.249999999999998224 ) ;
#10053=ADVANCED_FACE ( 'NONE', ( #5973 ), #11597, .F. ) ;
#10054=CARTESIAN_POINT ( 'NONE',  ( 25.96530230012339757, -2.390463732198628399, 6.453230759126474148 ) ) ;
#10055=CARTESIAN_POINT ( 'NONE',  ( 27.15176839919044482, -1.857969822100365098, 5.783357778048668685 ) ) ;
#10065=VECTOR ( 'NONE', #334, 1000.000000000000227 ) ;
#10067=ORIENTED_EDGE ( 'NONE', *, *, #592, .F. ) ;
#10075=DIRECTION ( 'NONE',  ( 1.000000000000000000, 0.000000000000000000, 0.000000000000000000 ) ) ;
#10077=CARTESIAN_POINT ( 'NONE',  ( 26.03726795043090547, -3.446058701420613879, 3.283357778048666464 ) ) ;
#10078=VECTOR ( 'NONE', #13932, 1000.000000000000000 ) ;
#10080=CARTESIAN_POINT ( 'NONE',  ( -24.62400252878131113, -22.25686381702613659, 14.56428162264008286 ) ) ;
#10081=CARTESIAN_POINT ( 'NONE',  ( 32.92264866086529906, -1.552240892477451784, 5.113484796970859669 ) ) ;
#10099=CARTESIAN_POINT ( 'NONE',  ( 28.71854711534694715, -4.576831098024959132, 7.939653947423662039 ) ) ;
#10101=VERTEX_POINT ( 'NONE', #16888 ) ;
#10102=AXIS2_PLACEMENT_3D ( 'NONE', #5315, #2521, #1528 ) ;
#10105=CARTESIAN_POINT ( 'NONE',  ( 31.55553118839817728, -4.235030543236534939, 3.627061608673664228 ) ) ;
#10106=CARTESIAN_POINT ( 'NONE',  ( 25.71748644841968456, -2.420320648352046078, 5.783357778048663356 ) ) ;
#10110=CARTESIAN_POINT ( 'NONE',  ( 35.74085044863416982, -18.73429073671341172, 11.27079897466147251 ) ) ;
#10116=CARTESIAN_POINT ( 'NONE',  ( 28.77507474356526984, -18.63405514100518801, 13.50648245236009792 ) ) ;
#10117=DIRECTION ( 'NONE',  ( 0.000000000000000000, -1.000000000000000000, 0.000000000000000000 ) ) ;
#10122=CARTESIAN_POINT ( 'NONE',  ( 29.78612525785423060, -2.267488637519798012, 4.533357778048667797 ) ) ;
#10128=ORIENTED_EDGE ( 'NONE', *, *, #15724, .T. ) ;
#10129=CARTESIAN_POINT ( 'NONE',  ( 28.34209327568754944, -5.876127416962207306, 3.627061608673662896 ) ) ;
#10130=CARTESIAN_POINT ( 'NONE',  ( -13.00000000000000178, -1.592040838891559293E-15, 8.700000000000001066 ) ) ;
#10141=CARTESIAN_POINT ( 'NONE',  ( -14.05523583925745257, 13.74128089903392613, 16.39434919531312218 ) ) ;
#10142=CIRCLE ( 'NONE', #2912, 1.000000000000000000 ) ;
#10144=CARTESIAN_POINT ( 'NONE',  ( -29.25000000000000000, -16.21813761408365195, 13.37255996287876947 ) ) ;
#10145=PLANE ( 'NONE',  #11790 ) ;
#10150=CARTESIAN_POINT ( 'NONE',  ( 28.28511899221430070, -4.629050627332469858, 8.283357778048662468 ) ) ;
#10156=EDGE_LOOP ( 'NONE', ( #6325, #4298, #6059, #6544 ) ) ;
#10159=ORIENTED_EDGE ( 'NONE', *, *, #8777, .F. ) ;
#10161=AXIS2_PLACEMENT_3D ( 'NONE', #15231, #6620, #10858 ) ;
#10164=ORIENTED_EDGE ( 'NONE', *, *, #15211, .F. ) ;
#10169=CARTESIAN_POINT ( 'NONE',  ( 36.27615609941022257, -23.17738945083361557, 12.00000000000000000 ) ) ;
#10170=CIRCLE ( 'NONE', #6997, 5.500000000000000888 ) ;
#10174=CARTESIAN_POINT ( 'NONE',  ( 32.79901970863393501, -6.593096864778464017, 5.783357778048658027 ) ) ;
#10176=ADVANCED_FACE ( 'NONE', ( #3092 ), #17261, .F. ) ;
#10179=CARTESIAN_POINT ( 'NONE',  ( 29.08935247050201767, -2.014077381790315702, 5.783357778048667797 ) ) ;
#10190=DIRECTION ( 'NONE',  ( -1.000000000000000000, 0.000000000000000000, 0.000000000000000000 ) ) ;
#10197=CARTESIAN_POINT ( 'NONE',  ( 29.14753769709988518, -3.271205139184214516, 7.939653947423664704 ) ) ;
#10204=CARTESIAN_POINT ( 'NONE',  ( 26.35439372113758694, -4.861664893681965083, 3.627061608673664228 ) ) ;
#10210=CYLINDRICAL_SURFACE ( 'NONE', #12212, 25.00000000000000000 ) ;
#10213=EDGE_CURVE ( 'NONE', #3807, #3702, #11395, .T. ) ;
#10218=CARTESIAN_POINT ( 'NONE',  ( 32.58190297908952004, -5.565186596593329149, 3.283357778048663800 ) ) ;
#10219=ADVANCED_FACE ( 'NONE', ( #14126 ), #358, .T. ) ;
#10221=EDGE_CURVE ( 'NONE', #3677, #1847, #12673, .T. ) ;
#10222=ORIENTED_EDGE ( 'NONE', *, *, #9478, .T. ) ;
#10223=VERTEX_POINT ( 'NONE', #4777 ) ;
#10225=CARTESIAN_POINT ( 'NONE',  ( 33.14902674121363901, -1.535163666906202318, 5.783357778048668685 ) ) ;
#10226=CARTESIAN_POINT ( 'NONE',  ( 32.29974222271236073, -2.891426744974864071, 7.939653947423662927 ) ) ;
#10232=DIRECTION ( 'NONE',  ( 0.000000000000000000, 0.000000000000000000, -1.000000000000000000 ) ) ;
#10237=ORIENTED_EDGE ( 'NONE', *, *, #1673, .F. ) ;
#10242=CARTESIAN_POINT ( 'NONE',  ( 27.33945763453056088, -4.742984145595265488, 3.283357778048664244 ) ) ;
#10243=ORIENTED_EDGE ( 'NONE', *, *, #15614, .F. ) ;
#10244=CARTESIAN_POINT ( 'NONE',  ( 23.02601376483258022, 3.965314980223224151, 6.000000000000000000 ) ) ;
#10254=CARTESIAN_POINT ( 'NONE',  ( -45.50000000000000000, -16.03270077640482683, 2.787981825772262390 ) ) ;
#10261=CARTESIAN_POINT ( 'NONE',  ( 26.24741491880507027, -3.420740141806666745, 8.283357778048664244 ) ) ;
#10263=EDGE_LOOP ( 'NONE', ( #8622, #3925, #11762, #16443 ) ) ;
#10264=CARTESIAN_POINT ( 'NONE',  ( -13.00000000000000178, -1.592040838891559293E-15, 12.00000000000000000 ) ) ;
#10265=DIRECTION ( 'NONE',  ( 0.9928203230275514102, 0.1196152422706598939, 0.000000000000000000 ) ) ;
#10268=( BOUNDED_CURVE ( )  B_SPLINE_CURVE ( 2, ( #9812, #5647, #4301, #14094, #15362, #2944, #8656, #7125, #226 ),
 .UNSPECIFIED., .F., .T. ) 
 B_SPLINE_CURVE_WITH_KNOTS ( ( 3, 2, 2, 2, 3 ),
 ( 0.7884615384615384359, 0.7948717948717948234, 0.8076923076923077094, 0.8205128205128204844, 0.8269230769230769829 ),
 .UNSPECIFIED. ) 
 CURVE ( )  GEOMETRIC_REPRESENTATION_ITEM ( )  RATIONAL_B_SPLINE_CURVE ( ( 0.9330127018922194093, 0.9330127018922194093, 1.000000000000000000, 0.8660254037844387076, 1.000000000000000000, 0.8660254037844387076, 1.000000000000000000, 0.9330127018922187432, 0.9330127018922192983 ) ) 
 REPRESENTATION_ITEM ( '' )  );
#10280=CARTESIAN_POINT ( 'NONE',  ( 32.96459815279162342, -1.884545423566157174, 7.033357778048666020 ) ) ;
#10281=CARTESIAN_POINT ( 'NONE',  ( 27.00222791626931595, -2.275731535614434531, 5.783357778048668685 ) ) ;
#10283=EDGE_LOOP ( 'NONE', ( #11855, #2928, #12924, #1338 ) ) ;
#10286=CARTESIAN_POINT ( 'NONE',  ( 26.46816385032927599, -3.594016774262162706, 7.939653947423664704 ) ) ;
#10287=CARTESIAN_POINT ( 'NONE',  ( 27.50829672905005907, -3.268828784122926212, 8.283357778048666020 ) ) ;
#10291=ORIENTED_EDGE ( 'NONE', *, *, #11694, .F. ) ;
#10292=DIRECTION ( 'NONE',  ( -1.000000000000000000, 0.000000000000000000, 0.000000000000000000 ) ) ;
#10300=CARTESIAN_POINT ( 'NONE',  ( 33.14105852333657509, -6.224726188408045147, 7.033357778048657138 ) ) ;
#10305=CARTESIAN_POINT ( 'NONE',  ( 27.24942365487322959, -6.207645047004940686, 8.283357778048660691 ) ) ;
#10307=FILL_AREA_STYLE ('',( #718 ) ) ;
#10315=EDGE_CURVE ( 'NONE', #11675, #5034, #17528, .T. ) ;
#10320=EDGE_LOOP ( 'NONE', ( #4801, #16544, #17049, #13242 ) ) ;
#10322=DIRECTION ( 'NONE',  ( 0.9928203230275510771, 0.1196152422706609902, 4.006172263299092517E-17 ) ) ;
#10323=CARTESIAN_POINT ( 'NONE',  ( 29.77118727536320719, -5.903822331637461396, 8.283357778048658915 ) ) ;
#10328=EDGE_CURVE ( 'NONE', #10789, #3948, #10142, .T. ) ;
#10335=FACE_OUTER_BOUND ( 'NONE', #10320, .T. ) ;
#10340=VERTEX_POINT ( 'NONE', #14679 ) ;
#10353=CARTESIAN_POINT ( 'NONE',  ( 27.19802975513453092, -2.241944418315925613, 5.783357778048667797 ) ) ;
#10360=( BOUNDED_CURVE ( )  B_SPLINE_CURVE ( 2, ( #9078, #14526, #733, #14703, #8242, #15135, #2721 ),
 .UNSPECIFIED., .F., .F. ) 
 B_SPLINE_CURVE_WITH_KNOTS ( ( 3, 2, 2, 3 ),
 ( 0.9423076923076922906, 0.9487179487179486781, 0.9615384615384615641, 0.9690340935984054216 ),
 .UNSPECIFIED. ) 
 CURVE ( )  GEOMETRIC_REPRESENTATION_ITEM ( )  RATIONAL_B_SPLINE_CURVE ( ( 0.9330127018922194093, 0.9330127018922194093, 1.000000000000000000, 0.8660254037844387076, 1.000000000000000000, 0.9216705062683109295, 0.9349331465915117212 ) ) 
 REPRESENTATION_ITEM ( '' )  );
#10366=CARTESIAN_POINT ( 'NONE',  ( 25.11802603177690330, -19.03270077640482683, 10.53798182577225084 ) ) ;
#10369=CARTESIAN_POINT ( 'NONE',  ( 25.78518620311324838, -3.676302093007511651, 3.627061608673666893 ) ) ;
#10371=B_SPLINE_CURVE_WITH_KNOTS ( 'NONE', 1,
 ( #13334, #2201 ),
 .UNSPECIFIED., .F., .F.,
 ( 2, 2 ),
 ( 0.000000000000000000, 1.000000000000000000 ),
 .UNSPECIFIED. ) ;
#10373=CARTESIAN_POINT ( 'NONE',  ( 26.11428532722776907, -5.713797161519016399, 7.898105917008066079 ) ) ;
#10374=EDGE_CURVE ( 'NONE', #11271, #11309, #9862, .T. ) ;
#10376=CARTESIAN_POINT ( 'NONE',  ( 25.77727992838053339, -5.625024813964539128, 3.627061608673662896 ) ) ;
#10377=CARTESIAN_POINT ( 'NONE',  ( -21.42089235853292806, -10.15736413759261048, 15.24668633003922658 ) ) ;
#10382=CARTESIAN_POINT ( 'NONE',  ( -34.91600907648203389, -11.88801210197604341, -0.000000000000000000 ) ) ;
#10383=VERTEX_POINT ( 'NONE', #5390 ) ;
#10385=CARTESIAN_POINT ( 'NONE',  ( -23.00000000000000000, -16.21813761408365195, 13.00000000000000355 ) ) ;
#10388=DIRECTION ( 'NONE',  ( 0.9928203230275512992, 0.1196152422706610180, 4.006172263299093133E-17 ) ) ;
#10395=CARTESIAN_POINT ( 'NONE',  ( 31.74131510559286085, -5.666460835049168310, 8.283357778048658915 ) ) ;
#10396=VECTOR ( 'NONE', #1726, 1000.000000000000114 ) ;
#10401=CARTESIAN_POINT ( 'NONE',  ( 26.25801688195511474, -3.619335333876111171, 3.627061608673666449 ) ) ;
#10402=VECTOR ( 'NONE', #9001, 1000.000000000000227 ) ;
#10403=CARTESIAN_POINT ( 'NONE',  ( 33.58707084003705745, -6.498152266226124851, 5.783357778048657138 ) ) ;
#10409=LINE ( 'NONE', #14610, #2655 ) ;
#10411=DIRECTION ( 'NONE',  ( -0.7681011886108269904, 0.5760758914581205481, -0.2795659695588259552 ) ) ;
#10413=CARTESIAN_POINT ( 'NONE',  ( -20.00000000000000000, 7.999999999999996447, 15.51150668642334374 ) ) ;
#10415=EDGE_CURVE ( 'NONE', #2179, #5245, #12476, .T. ) ;
#10424=ORIENTED_EDGE ( 'NONE', *, *, #837, .T. ) ;
#10428=LINE ( 'NONE', #4726, #6956 ) ;
#10433=ADVANCED_FACE ( 'NONE', ( #8301 ), #12380, .F. ) ;
#10441=VECTOR ( 'NONE', #14795, 1000.000000000000000 ) ;
#10448=( BOUNDED_CURVE ( )  B_SPLINE_CURVE ( 2, ( #5932, #597, #17023, #4840, #1883, #11456, #10280, #4931, #15647 ),
 .UNSPECIFIED., .F., .T. ) 
 B_SPLINE_CURVE_WITH_KNOTS ( ( 3, 2, 2, 2, 3 ),
 ( 0.05769230769230772327, 0.06410256410256409687, 0.07692307692307692735, 0.08974358974358974395, 0.09615384615384617306 ),
 .UNSPECIFIED. ) 
 CURVE ( )  GEOMETRIC_REPRESENTATION_ITEM ( )  RATIONAL_B_SPLINE_CURVE ( ( 0.9330127018922192983, 0.9330127018922196314, 1.000000000000000000, 0.8660254037844387076, 1.000000000000000000, 0.8660254037844387076, 1.000000000000000000, 0.9330127018922191873, 0.9330127018922194093 ) ) 
 REPRESENTATION_ITEM ( '' )  );
#10454=ADVANCED_FACE ( 'NONE', ( #8127 ), #297, .F. ) ;
#10456=CYLINDRICAL_SURFACE ( 'NONE', #2611, 2.500000000000001776 ) ;
#10465=CARTESIAN_POINT ( 'NONE',  ( 27.25621498173240198, -3.499072175709823984, 7.939653947423664704 ) ) ;
#10466=ORIENTED_EDGE ( 'NONE', *, *, #8612, .F. ) ;
#10469=CARTESIAN_POINT ( 'NONE',  ( 32.72003615946069743, -2.840789625746940938, 3.627061608673666893 ) ) ;
#10470=CARTESIAN_POINT ( 'NONE',  ( 28.16197717867739314, -7.161965777771100328, 6.453230759126468818 ) ) ;
#10484=CARTESIAN_POINT ( 'NONE',  ( 34.91600907648203389, -11.88801210197604341, 11.56671555609732671 ) ) ;
#10489=CARTESIAN_POINT ( 'NONE',  ( 33.09223089549517738, -4.049888575955752579, 3.283357778048664244 ) ) ;
#10494=CARTESIAN_POINT ( 'NONE',  ( 35.62429925076629189, -17.76690233603958546, 10.53798182577225084 ) ) ;
#10495=CARTESIAN_POINT ( 'NONE',  ( 32.28234893270314387, -5.401404424200516807, 3.627061608673662896 ) ) ;
#10497=CARTESIAN_POINT ( 'NONE',  ( 33.06225340847440464, -6.234220648470727433, 7.033357778048657138 ) ) ;
#10501=CARTESIAN_POINT ( 'NONE',  ( -36.27615609941022257, -23.17738945083361557, -0.000000000000000000 ) ) ;
#10503=FACE_BOUND ( 'NONE', #7695, .T. ) ;
#10505=CARTESIAN_POINT ( 'NONE',  ( 20.84129949943806537, -10.34926000617958231, 15.35708546568073984 ) ) ;
#10507=EDGE_CURVE ( 'NONE', #14701, #4898, #10371, .T. ) ;
#10512=CARTESIAN_POINT ( 'NONE',  ( 26.58890374069123652, -3.379597482641427231, 3.283357778048666464 ) ) ;
#10514=VERTEX_POINT ( 'NONE', #13240 ) ;
#10517=EDGE_LOOP ( 'NONE', ( #6568, #3601, #16591, #2311 ) ) ;
#10522=CIRCLE ( 'NONE', #7364, 13.00000000000000178 ) ;
#10527=DIRECTION ( 'NONE',  ( -0.9928203230275512992, -0.1196152422706610180, -4.006172263299093133E-17 ) ) ;
#10533=FACE_OUTER_BOUND ( 'NONE', #6950, .T. ) ;
#10535=DIRECTION ( 'NONE',  ( 1.000000000000000000, 0.000000000000000000, 0.000000000000000000 ) ) ;
#10537=DIRECTION ( 'NONE',  ( 0.1196152422706596996, -0.9928203230275514102, 0.000000000000000000 ) ) ;
#10538=DIRECTION ( 'NONE',  ( 0.000000000000000000, -1.000000000000000000, 3.469446951953614189E-16 ) ) ;
#10542=LINE ( 'NONE', #15823, #16805 ) ;
#10543=CARTESIAN_POINT ( 'NONE',  ( 31.92212620501791775, -6.708942077180482855, 5.113484796970852564 ) ) ;
#10547=CARTESIAN_POINT ( 'NONE',  ( 0.000000000000000000, 0.000000000000000000, 8.700000000000001066 ) ) ;
#10548=CARTESIAN_POINT ( 'NONE',  ( 29.45101334415624095, -7.006662376286321603, 5.783357778048669573 ) ) ;
#10549=CARTESIAN_POINT ( 'NONE',  ( 26.19678349485696955, -4.880653813392439311, 7.939653947423662039 ) ) ;
#10551=ORIENTED_EDGE ( 'NONE', *, *, #4228, .T. ) ;
#10553=CARTESIAN_POINT ( 'NONE',  ( 28.51709679197739078, -3.347160818026084339, 7.939653947423664704 ) ) ;
#10559=CARTESIAN_POINT ( 'NONE',  ( -45.50000000000000000, -16.03270077640482683, 5.537981825772250843 ) ) ;
#10567=DIRECTION ( 'NONE',  ( 0.9928203230275510771, 0.1196152422706621282, 0.000000000000000000 ) ) ;
#10568=DIRECTION ( 'NONE',  ( 0.7999999999999999334, -0.6000000000000001998, 0.000000000000000000 ) ) ;
#10570=CARTESIAN_POINT ( 'NONE',  ( 28.72797218747911074, -6.756415940301135237, 7.033357778048657138 ) ) ;
#10573=CARTESIAN_POINT ( 'NONE',  ( 27.10313151398701947, -6.652368374500619908, 4.705209693361160461 ) ) ;
#10574=CARTESIAN_POINT ( 'NONE',  ( 28.40332666278570173, -4.614808937445885384, 3.627061608673664228 ) ) ;
#10576=EDGE_CURVE ( 'NONE', #17612, #17698, #14874, .T. ) ;
#10577=LINE ( 'NONE', #16144, #5751 ) ;
#10584=CARTESIAN_POINT ( 'NONE',  ( 23.84286890107044954, -10.01213378893004879, 14.74186762137086859 ) ) ;
#10594=EDGE_LOOP ( 'NONE', ( #15821, #2972, #6216, #8652 ) ) ;
#10597=CARTESIAN_POINT ( 'NONE',  ( -19.43845002722867221, 2.988003976273734263, 0.000000000000000000 ) ) ;
#10600=CARTESIAN_POINT ( 'NONE',  ( -3.248936832696171617, 17.78798921770683350, 17.00000000000000000 ) ) ;
#10612=CARTESIAN_POINT ( 'NONE',  ( 35.77680296528374271, -19.03270077640482683, 10.53798182577225084 ) ) ;
#10615=CARTESIAN_POINT ( 'NONE',  ( 27.48088551392658729, -7.244023872874614689, 5.783357778048669573 ) ) ;
#10616=DIRECTION ( 'NONE',  ( 1.000000000000000000, 0.000000000000000000, 0.000000000000000000 ) ) ;
#10625=ADVANCED_FACE ( 'NONE', ( #1442 ), #13776, .T. ) ;
#10628=CARTESIAN_POINT ( 'NONE',  ( 27.63266882139180680, -2.199775856772564708, 5.783357778048668685 ) ) ;
#10631=CARTESIAN_POINT ( 'NONE',  ( 31.69574812466957781, -6.726019302751734763, 5.783357778048657138 ) ) ;
#10633=CARTESIAN_POINT ( 'NONE',  ( 35.74085044863416982, -23.57886868891565513, 11.27079897466147251 ) ) ;
#10637=LINE ( 'NONE', #701, #2893 ) ;
#10639=FACE_BOUND ( 'NONE', #11005, .T. ) ;
#10640=DIRECTION ( 'NONE',  ( 0.000000000000000000, 0.000000000000000000, -1.000000000000000000 ) ) ;
#10646=CARTESIAN_POINT ( 'NONE',  ( 25.81099976294218479, -6.186279776075334524, 4.026415200706355613 ) ) ;
#10649=CARTESIAN_POINT ( 'NONE',  ( 32.22908376348204484, -1.973160382215000785, 4.533357778048667797 ) ) ;
#10651=CARTESIAN_POINT ( 'NONE',  ( 27.29814976067589072, -3.294147343736873346, 3.283357778048666464 ) ) ;
#10654=CARTESIAN_POINT ( 'NONE',  ( 33.28924367748503244, -4.026152426421394814, 3.627061608673664228 ) ) ;
#10655=CARTESIAN_POINT ( 'NONE',  ( 30.43486631442457835, -6.877930660435475296, 5.783357778048657138 ) ) ;
#10658=DIRECTION ( 'NONE',  ( 0.000000000000000000, 0.000000000000000000, -1.000000000000000000 ) ) ;
#10664=DIRECTION ( 'NONE',  ( 0.000000000000000000, 0.000000000000000000, 1.000000000000000000 ) ) ;
#10666=CARTESIAN_POINT ( 'NONE',  ( -19.49912934580633106, 8.667827538924893105, 15.60122950519025409 ) ) ;
#10673=AXIS2_PLACEMENT_3D ( 'NONE', #3024, #5629, #12626 ) ;
#10674=VERTEX_POINT ( 'NONE', #3985 ) ;
#10675=CARTESIAN_POINT ( 'NONE',  ( 32.67202617590239555, -5.981426544730773287, 6.861505862736158257 ) ) ;
#10680=CARTESIAN_POINT ( 'NONE',  ( 25.89388370423996477, -3.884438240559767497, 7.685380675815244089 ) ) ;
#10683=ORIENTED_EDGE ( 'NONE', *, *, #9471, .T. ) ;
#10695=( BOUNDED_CURVE ( )  B_SPLINE_CURVE ( 2, ( #3863, #4123, #10891, #13476, #13556, #12187, #9544, #5552, #17766 ),
 .UNSPECIFIED., .F., .T. ) 
 B_SPLINE_CURVE_WITH_KNOTS ( ( 3, 2, 2, 2, 3 ),
 ( 0.6346153846153846922, 0.6410256410256410797, 0.6538461538461538547, 0.6666666666666666297, 0.6730769230769231282 ),
 .UNSPECIFIED. ) 
 CURVE ( )  GEOMETRIC_REPRESENTATION_ITEM ( )  RATIONAL_B_SPLINE_CURVE ( ( 0.9330127018922192983, 0.9330127018922198534, 1.000000000000000000, 0.8660254037844387076, 1.000000000000000000, 0.8660254037844387076, 1.000000000000000000, 0.9330127018922187432, 0.9330127018922192983 ) ) 
 REPRESENTATION_ITEM ( '' )  );
#10700=CARTESIAN_POINT ( 'NONE',  ( 25.96814307759224505, -4.500799614243313762, 3.446762361689486465 ) ) ;
#10705=ORIENTED_EDGE ( 'NONE', *, *, #7482, .F. ) ;
#10707=DIRECTION ( 'NONE',  ( -1.000000000000000000, 0.000000000000000000, 0.000000000000000000 ) ) ;
#10708=AXIS2_PLACEMENT_3D ( 'NONE', #4459, #9698, #24 ) ;
#10711=AXIS2_PLACEMENT_3D ( 'NONE', #9279, #5189, #10707 ) ;
#10713=EDGE_CURVE ( 'NONE', #2135, #9702, #16270, .T. ) ;
#10715=CARTESIAN_POINT ( 'NONE',  ( 33.20111501597313719, -6.944397359513344803, 5.783357778048657138 ) ) ;
#10717=ORIENTED_EDGE ( 'NONE', *, *, #15334, .T. ) ;
#10719=ADVANCED_FACE ( 'NONE', ( #15218 ), #2631, .T. ) ;
#10720=CARTESIAN_POINT ( 'NONE',  ( 30.41294626588012306, -6.253601060580800564, 4.705209693361159573 ) ) ;
#10721=CARTESIAN_POINT ( 'NONE',  ( -17.07594129529364579, -14.18356557013591868, 15.98851070825981324 ) ) ;
#10726=CARTESIAN_POINT ( 'NONE',  ( 16.75000000000000000, -16.21813761408365195, 13.00000000000000178 ) ) ;
#10732=CARTESIAN_POINT ( 'NONE',  ( 26.21417678486618641, -2.370676134166772808, 5.783357778048668685 ) ) ;
#10736=CARTESIAN_POINT ( 'NONE',  ( 33.46007730730551799, -5.886481946178435010, 6.861505862736157368 ) ) ;
#10738=CARTESIAN_POINT ( 'NONE',  ( 28.49145532429760053, -1.696564004353941613, 5.783357778048668685 ) ) ;
#10739=VERTEX_POINT ( 'NONE', #2722 ) ;
#10742=EDGE_LOOP ( 'NONE', ( #2800, #1776, #13987, #6034 ) ) ;
#10743=CARTESIAN_POINT ( 'NONE',  ( 30.88577694472199298, -6.196634301449400084, 4.705209693361160461 ) ) ;
#10745=CARTESIAN_POINT ( 'NONE',  ( 30.18087924896149588, -5.654590020340094725, 7.939653947423658487 ) ) ;
#10746=EDGE_LOOP ( 'NONE', ( #11137, #3094 ) ) ;
#10756=CARTESIAN_POINT ( 'NONE',  ( -45.50000000000000000, -16.03270077640482683, 8.287981825772238409 ) ) ;
#10763=CARTESIAN_POINT ( 'NONE',  ( 26.61898274975073164, -6.283600725846810953, 8.283357778048658915 ) ) ;
#10766=CARTESIAN_POINT ( 'NONE',  ( 30.88577694472199298, -6.196634301449400084, 4.705209693361160461 ) ) ;
#10769=EDGE_CURVE ( 'NONE', #9967, #15002, #324, .T. ) ;
#10771=CARTESIAN_POINT ( 'NONE',  ( 25.71748644841968456, -2.420320648352046078, 5.783357778048663356 ) ) ;
#10775=ORIENTED_EDGE ( 'NONE', *, *, #7709, .F. ) ;
#10778=AXIS2_PLACEMENT_3D ( 'NONE', #6428, #6051, #3347 ) ;
#10781=CARTESIAN_POINT ( 'NONE',  ( 31.26353094466156080, -6.788289799823394866, 5.783357778048664244 ) ) ;
#10786=ORIENTED_EDGE ( 'NONE', *, *, #13557, .F. ) ;
#10788=AXIS2_PLACEMENT_3D ( 'NONE', #11467, #2497, #6755 ) ;
#10789=VERTEX_POINT ( 'NONE', #4549 ) ;
#10790=DIRECTION ( 'NONE',  ( 0.000000000000000000, 0.000000000000000000, -1.000000000000000000 ) ) ;
#10793=PLANE ( 'NONE',  #8448 ) ;
#10800=CARTESIAN_POINT ( 'NONE',  ( 26.31556265977298992, -7.384422263489805793, 5.783357778048663356 ) ) ;
#10801=CARTESIAN_POINT ( 'NONE',  ( 30.37154917142620292, -2.923863409590206519, 3.283357778048666464 ) ) ;
#10805=CARTESIAN_POINT ( 'NONE',  ( 29.17398450417959310, -7.029842018119214941, 5.783357778048657138 ) ) ;
#10806=CARTESIAN_POINT ( 'NONE',  ( -18.31874363337315970, -12.05639433133630511, 15.79760360980902689 ) ) ;
#10807=CARTESIAN_POINT ( 'NONE',  ( -25.74999999999999645, -16.21813761408365195, 0.000000000000000000 ) ) ;
#10808=ORIENTED_EDGE ( 'NONE', *, *, #17095, .T. ) ;
#10810=VERTEX_POINT ( 'NONE', #10254 ) ;
#10818=CARTESIAN_POINT ( 'NONE',  ( 32.24155699611449677, -1.634298987580965923, 5.783357778048662468 ) ) ;
#10820=CARTESIAN_POINT ( 'NONE',  ( 26.86653773853314320, -2.919050055179571945, 4.705209693361167567 ) ) ;
#10823=CARTESIAN_POINT ( 'NONE',  ( 29.50659824675005893, -4.481886499472614638, 3.627061608673664228 ) ) ;
#10826=CARTESIAN_POINT ( 'NONE',  ( 32.32618902979206865, -6.650063623909865385, 5.783357778048657138 ) ) ;
#10827=CARTESIAN_POINT ( 'NONE',  ( 29.15568435273173264, -2.343444316361667834, 4.533357778048667797 ) ) ;
#10828=( BOUNDED_CURVE ( )  B_SPLINE_CURVE ( 3, ( #2350, #14147, #2777, #8035 ),
 .UNSPECIFIED., .F., .T. ) 
 B_SPLINE_CURVE_WITH_KNOTS ( ( 4, 4 ),
 ( 4.715434792643774742, 4.769085813125753859 ),
 .UNSPECIFIED. ) 
 CURVE ( )  GEOMETRIC_REPRESENTATION_ITEM ( )  RATIONAL_B_SPLINE_CURVE ( ( 1.000000000000000000, 0.9997601450507493936, 0.9997601450507493936, 1.000000000000000000 ) ) 
 REPRESENTATION_ITEM ( '' )  );
#10833=CARTESIAN_POINT ( 'NONE',  ( 29.99682221560115991, -1.914942061115552541, 5.783357778048668685 ) ) ;
#10836=CARTESIAN_POINT ( 'NONE',  ( 31.45915434921569798, -2.992700983430681028, 3.627061608673666449 ) ) ;
#10842=CARTESIAN_POINT ( 'NONE',  ( -9.099998387031005720, -19.29508120620799971, 6.000000000000000000 ) ) ;
#10843=CARTESIAN_POINT ( 'NONE',  ( 0.000000000000000000, 0.000000000000000000, 6.000000000000000000 ) ) ;
#10846=CARTESIAN_POINT ( 'NONE',  ( 26.83664947211162399, -6.984282976826746037, 7.033357778048657138 ) ) ;
#10850=CARTESIAN_POINT ( 'NONE',  ( -32.93004296264518160, -25.68697430340739629, 12.29384923381406658 ) ) ;
#10853=ORIENTED_EDGE ( 'NONE', *, *, #13782, .F. ) ;
#10854=CARTESIAN_POINT ( 'NONE',  ( 33.30246708102489350, -5.905470865888903020, 6.861505862736158257 ) ) ;
#10858=DIRECTION ( 'NONE',  ( 1.000000000000000000, 0.000000000000000000, 0.000000000000000000 ) ) ;
#10859=CARTESIAN_POINT ( 'NONE',  ( 25.94006848055682468, -4.267777217026356595, 7.847536328832044994 ) ) ;
#10865=CARTESIAN_POINT ( 'NONE',  ( 23.00000000000000000, -16.21813761408365195, 13.00000000000000178 ) ) ;
#10880=ORIENTED_EDGE ( 'NONE', *, *, #4996, .F. ) ;
#10889=CARTESIAN_POINT ( 'NONE',  ( 30.78487334700428590, -1.819997462563214263, 5.783357778048668685 ) ) ;
#10890=CARTESIAN_POINT ( 'NONE',  ( -16.95520570318904419, -14.57695177659950581, 16.00609026697356541 ) ) ;
#10891=CARTESIAN_POINT ( 'NONE',  ( 28.44643833274707845, -2.428894455266221275, 4.533357778048667797 ) ) ;
#10899=CARTESIAN_POINT ( 'NONE',  ( 33.95908713831673964, -3.945449517755637014, 5.783357778048663356 ) ) ;
#10900=CARTESIAN_POINT ( 'NONE',  ( 20.00000000000000000, 7.999999999999996447, 0.000000000000000000 ) ) ;
#10903=( BOUNDED_CURVE ( )  B_SPLINE_CURVE ( 3, ( #11536, #1430, #15736, #3394 ),
 .UNSPECIFIED., .F., .T. ) 
 B_SPLINE_CURVE_WITH_KNOTS ( ( 4, 4 ),
 ( 1.230954889131919305, 1.393542617697868691 ),
 .UNSPECIFIED. ) 
 CURVE ( )  GEOMETRIC_REPRESENTATION_ITEM ( )  RATIONAL_B_SPLINE_CURVE ( ( 1.000000000000000000, 0.9977983154653933262, 0.9977983154653933262, 1.000000000000000000 ) ) 
 REPRESENTATION_ITEM ( '' )  );
#10904=CARTESIAN_POINT ( 'NONE',  ( 29.62036837594175154, -3.214238380052812261, 7.939653947423664704 ) ) ;
#10906=FACE_OUTER_BOUND ( 'NONE', #17169, .T. ) ;
#10908=CARTESIAN_POINT ( 'NONE',  ( 33.44685390376565692, -4.007163506710925027, 3.627061608673664228 ) ) ;
#10910=ORIENTED_EDGE ( 'NONE', *, *, #4835, .F. ) ;
#10912=CARTESIAN_POINT ( 'NONE',  ( 31.53813789838894621, -6.745008222462202774, 5.783357778048658027 ) ) ;
#10915=CARTESIAN_POINT ( 'NONE',  ( 28.71854711534694715, -4.576831098024959132, 7.939653947423662039 ) ) ;
#10919=CARTESIAN_POINT ( 'NONE',  ( 28.63031693179632242, -2.406740715396564756, 7.033357778048666020 ) ) ;
#10926=CARTESIAN_POINT ( 'NONE',  ( 28.92482766011098150, -14.18604173879621477, 13.46461621778217577 ) ) ;
#10928=( BOUNDED_CURVE ( )  B_SPLINE_CURVE ( 2, ( #16892, #1742, #12521, #7271, #11413, #16978, #11501, #10054, #15602 ),
 .UNSPECIFIED., .F., .T. ) 
 B_SPLINE_CURVE_WITH_KNOTS ( ( 3, 2, 2, 2, 3 ),
 ( 0.9038461538461538547, 0.9102564102564102422, 0.9230769230769231282, 0.9358974358974359031, 0.9423076923076922906 ),
 .UNSPECIFIED. ) 
 CURVE ( )  GEOMETRIC_REPRESENTATION_ITEM ( )  RATIONAL_B_SPLINE_CURVE ( ( 0.9330127018922194093, 0.9330127018922194093, 1.000000000000000000, 0.8660254037844387076, 1.000000000000000000, 0.8660254037844387076, 1.000000000000000000, 0.9330127018922194093, 0.9330127018922194093 ) ) 
 REPRESENTATION_ITEM ( '' )  );
#10938=CARTESIAN_POINT ( 'NONE',  ( 33.14902674121363901, -1.535163666906202318, 5.783357778048668685 ) ) ;
#10946=DIRECTION ( 'NONE',  ( 0.000000000000000000, 0.000000000000000000, -1.000000000000000000 ) ) ;
#10955=CARTESIAN_POINT ( 'NONE',  ( 31.23537658942770889, -6.791681843624433945, 6.453230759126467042 ) ) ;
#10960=AXIS2_PLACEMENT_3D ( 'NONE', #3082, #12680, #15865 ) ;
#10970=FACE_OUTER_BOUND ( 'NONE', #12624, .T. ) ;
#10971=CIRCLE ( 'NONE', #4628, 13.00000000000000178 ) ;
#10974=CARTESIAN_POINT ( 'NONE',  ( 32.37175601071535169, -5.590505156207296267, 8.283357778048660691 ) ) ;
#10980=CARTESIAN_POINT ( 'NONE',  ( 27.65911562847151117, -5.958412735707574015, 7.939653947423658487 ) ) ;
#10981=DIRECTION ( 'NONE',  ( -0.1196152422706621005, 0.9928203230275509661, 0.000000000000000000 ) ) ;
#10982=CARTESIAN_POINT ( 'NONE',  ( 17.60442140056922611, -19.37930158608179809, 15.90915821310915135 ) ) ;
#10986=ADVANCED_FACE ( 'NONE', ( #5169 ), #17374, .F. ) ;
#10996=CARTESIAN_POINT ( 'NONE',  ( 32.32036211097666012, -1.624804527518282748, 5.783357778048663356 ) ) ;
#10997=CARTESIAN_POINT ( 'NONE',  ( 27.72904566057427189, -3.442105416578422172, 7.939653947423664704 ) ) ;
#11000=CARTESIAN_POINT ( 'NONE',  ( 32.43181250335191379, -6.310176327312596811, 7.033357778048657138 ) ) ;
#11004=EDGE_LOOP ( 'NONE', ( #16094, #5917, #11228, #4978 ) ) ;
#11005=EDGE_LOOP ( 'NONE', ( #4456, #3620 ) ) ;
#11006=CARTESIAN_POINT ( 'NONE',  ( 31.41114436565740320, -6.133337902414513820, 6.861505862736158257 ) ) ;
#11007=CARTESIAN_POINT ( 'NONE',  ( 33.95908713831673964, -3.945449517755648561, 5.783357778048663356 ) ) ;
#11009=CARTESIAN_POINT ( 'NONE',  ( 30.40088504037531791, -1.856063607844930852, 5.113484796970861446 ) ) ;
#11010=DIRECTION ( 'NONE',  ( 0.000000000000000000, 0.000000000000000000, 1.000000000000000000 ) ) ;
#11011=DIRECTION ( 'NONE',  ( -0.1196152422706621143, 0.9928203230275509661, 0.000000000000000000 ) ) ;
#11015=( BOUNDED_CURVE ( )  B_SPLINE_CURVE ( 2, ( #16455, #8277, #15446, #1395, #11069, #15257, #2836, #4381, #12630 ),
 .UNSPECIFIED., .F., .T. ) 
 B_SPLINE_CURVE_WITH_KNOTS ( ( 3, 2, 2, 2, 3 ),
 ( 0.5961538461538461453, 0.6025641025641025328, 0.6153846153846154188, 0.6282051282051281937, 0.6346153846153846922 ),
 .UNSPECIFIED. ) 
 CURVE ( )  GEOMETRIC_REPRESENTATION_ITEM ( )  RATIONAL_B_SPLINE_CURVE ( ( 0.9330127018922194093, 0.9330127018922194093, 1.000000000000000000, 0.8660254037844387076, 1.000000000000000000, 0.8660254037844387076, 1.000000000000000000, 0.9330127018922187432, 0.9330127018922192983 ) ) 
 REPRESENTATION_ITEM ( '' )  );
#11016=VERTEX_POINT ( 'NONE', #9431 ) ;
#11021=FACE_OUTER_BOUND ( 'NONE', #12827, .T. ) ;
#11030=CARTESIAN_POINT ( 'NONE',  ( 31.41114436565740320, -6.133337902414513820, 6.861505862736158257 ) ) ;
#11035=FACE_OUTER_BOUND ( 'NONE', #13200, .T. ) ;
#11045=CIRCLE ( 'NONE', #367, 0.9999999999999995559 ) ;
#11049=DIRECTION ( 'NONE',  ( -0.000000000000000000, -0.000000000000000000, 1.000000000000000000 ) ) ;
#11059=VERTEX_POINT ( 'NONE', #3655 ) ;
#11063=DIRECTION ( 'NONE',  ( 0.000000000000000000, 0.000000000000000000, -1.000000000000000000 ) ) ;
#11067=CARTESIAN_POINT ( 'NONE',  ( 26.01652455409633902, -4.902371455920926380, 5.783357778048663356 ) ) ;
#11069=CARTESIAN_POINT ( 'NONE',  ( 28.91555989733679866, -4.553094948490599592, 8.283357778048662468 ) ) ;
#11070=AXIS2_PLACEMENT_3D ( 'NONE', #639, #15782, #14143 ) ;
#11071=VERTEX_POINT ( 'NONE', #7994 ) ;
#11074=LINE ( 'NONE', #14914, #17718 ) ;
#11075=CARTESIAN_POINT ( 'NONE',  ( 16.95685998530892746, -17.86641812890577796, 16.00584995567978908 ) ) ;
#11077=CARTESIAN_POINT ( 'NONE',  ( 30.96820195323705605, -2.125071739898741097, 4.533357778048667797 ) ) ;
#11078=DIRECTION ( 'NONE',  ( 0.000000000000000000, 1.000000000000000000, -0.000000000000000000 ) ) ;
#11085=CARTESIAN_POINT ( 'NONE',  ( 28.76238721243587193, -5.825490297734302381, 7.939653947423658487 ) ) ;
#11088=CARTESIAN_POINT ( 'NONE',  ( 32.04575515724926760, -1.668086104879473730, 5.783357778048668685 ) ) ;
#11089=EDGE_CURVE ( 'NONE', #2542, #11393, #6467, .T. ) ;
#11092=ORIENTED_EDGE ( 'NONE', *, *, #17947, .T. ) ;
#11093=CARTESIAN_POINT ( 'NONE',  ( 27.08121146544255353, -6.028038774645947839, 3.627061608673662896 ) ) ;
#11094=CARTESIAN_POINT ( 'NONE',  ( -45.00000000000000711, -19.03270077640482683, 10.53798182577225084 ) ) ;
#11096=CARTESIAN_POINT ( 'NONE',  ( 27.75966235412334981, -2.811446176820259879, 6.861505862736166250 ) ) ;
#11098=DIRECTION ( 'NONE',  ( -0.1196152422706610735, 0.9928203230275511881, 0.000000000000000000 ) ) ;
#11099=CARTESIAN_POINT ( 'NONE',  ( -45.50000000000000000, -19.03270077640483038, 8.287981825772241962 ) ) ;
#11106=CARTESIAN_POINT ( 'NONE',  ( 28.29479612530171551, -12.89112598890823946, 13.63906826012424922 ) ) ;
#11112=ADVANCED_FACE ( 'NONE', ( #5698 ), #11215, .F. ) ;
#11114=CARTESIAN_POINT ( 'NONE',  ( 27.62849893492243325, -6.589071975465733644, 6.861505862736158257 ) ) ;
#11116=DIRECTION ( 'NONE',  ( 0.9928203230275514102, 0.1196152422706598939, 0.000000000000000000 ) ) ;
#11131=CARTESIAN_POINT ( 'NONE',  ( 32.82573654529290508, -1.174368712523534475, 5.783357778048668685 ) ) ;
#11134=VERTEX_POINT ( 'NONE', #1200 ) ;
#11137=ORIENTED_EDGE ( 'NONE', *, *, #17392, .T. ) ;
#11139=ORIENTED_EDGE ( 'NONE', *, *, #5413, .T. ) ;
#11143=ORIENTED_EDGE ( 'NONE', *, *, #335, .T. ) ;
#11151=CARTESIAN_POINT ( 'NONE',  ( 30.06013935859953534, -5.869009311960810216, 3.283357778048663800 ) ) ;
#11152=CARTESIAN_POINT ( 'NONE',  ( 26.52522735095806894, -6.721994413439005278, 6.861505862736157368 ) ) ;
#11154=CARTESIAN_POINT ( 'NONE',  ( -35.74085044863416272, -18.73429073671335132, 11.27079897466147607 ) ) ;
#11155=ORIENTED_EDGE ( 'NONE', *, *, #6483, .T. ) ;
#11159=ORIENTED_EDGE ( 'NONE', *, *, #16525, .T. ) ;
#11167=CARTESIAN_POINT ( 'NONE',  ( 28.98992747081925359, -3.290194058894681639, 7.939653947423664704 ) ) ;
#11168=DIRECTION ( 'NONE',  ( 0.9928203230275512992, 0.1196152422706610180, 4.006172263299093133E-17 ) ) ;
#11169=CARTESIAN_POINT ( 'NONE',  ( -36.95907006869318678, -17.52584492564777818, 5.783357778048664244 ) ) ;
#11170=CARTESIAN_POINT ( 'NONE',  ( 31.02146712245815507, -5.553315781884258229, 3.627061608673662896 ) ) ;
#11173=CARTESIAN_POINT ( 'NONE',  ( 30.15026255541241440, -6.285249260098253465, 6.861505862736158257 ) ) ;
#11177=CARTESIAN_POINT ( 'NONE',  ( 27.86926259684567597, -5.933094176093607786, 3.627061608673662896 ) ) ;
#11180=CARTESIAN_POINT ( 'NONE',  ( -23.00000000000000000, -16.21813761408365195, 13.00000000000000178 ) ) ;
#11181=DIRECTION ( 'NONE',  ( 0.9928203230275512992, 0.1196152422706610180, 4.006172263299093133E-17 ) ) ;
#11190=SURFACE_SIDE_STYLE ('',( #11570 ) ) ;
#11193=DIRECTION ( 'NONE',  ( 0.000000000000000000, 1.000000000000000000, 0.000000000000000000 ) ) ;
#11194=DIRECTION ( 'NONE',  ( -0.1196152422706611151, 0.9928203230275511881, 0.000000000000000000 ) ) ;
#11195=ADVANCED_FACE ( 'NONE', ( #9773 ), #1793, .T. ) ;
#11199=ORIENTED_EDGE ( 'NONE', *, *, #9926, .T. ) ;
#11200=CARTESIAN_POINT ( 'NONE',  ( 28.35948656569676629, -3.366149737736551906, 7.939653947423662927 ) ) ;
#11203=CARTESIAN_POINT ( 'NONE',  ( 13.00000000000000178, 0.000000000000000000, 12.00000000000000000 ) ) ;
#11204=CARTESIAN_POINT ( 'NONE',  ( 26.01652455409633902, -4.902371455920926380, 5.783357778048663356 ) ) ;
#11211=AXIS2_PLACEMENT_3D ( 'NONE', #10899, #9383, #4221 ) ;
#11212=ORIENTED_EDGE ( 'NONE', *, *, #201, .T. ) ;
#11215=CYLINDRICAL_SURFACE ( 'NONE', #16864, 6.249999999999998224 ) ;
#11219=CARTESIAN_POINT ( 'NONE',  ( 32.22908376348204484, -1.973160382215000785, 4.533357778048667797 ) ) ;
#11228=ORIENTED_EDGE ( 'NONE', *, *, #9165, .T. ) ;
#11229=CARTESIAN_POINT ( 'NONE',  ( 29.25000000000000000, -16.21813761408365195, 13.00000000000000178 ) ) ;
#11241=CARTESIAN_POINT ( 'NONE',  ( 33.60446413004628141, -3.988174587000466342, 7.939653947423662039 ) ) ;
#11243=CARTESIAN_POINT ( 'NONE',  ( 27.65458886993626564, -2.824105456627233224, 4.705209693361168455 ) ) ;
#11244=CARTESIAN_POINT ( 'NONE',  ( 33.21234388421201800, -5.489230917751459771, 3.283357778048663356 ) ) ;
#11255=DIRECTION ( 'NONE',  ( 0.9928203230275512992, 0.1196152422706610180, 4.006172263299093133E-17 ) ) ;
#11260=CARTESIAN_POINT ( 'NONE',  ( 31.61111609099199171, -1.710254666422835745, 5.783357778048665132 ) ) ;
#11262=CARTESIAN_POINT ( 'NONE',  ( 31.44176105920648823, -5.502678662656354192, 7.939653947423658487 ) ) ;
#11266=EDGE_CURVE ( 'NONE', #14073, #6202, #4320, .T. ) ;
#11267=CARTESIAN_POINT ( 'NONE',  ( 29.82181869931131146, -4.443908660051686610, 7.939653947423662039 ) ) ;
#11270=VECTOR ( 'NONE', #3747, 1000.000000000000000 ) ;
#11271=VERTEX_POINT ( 'NONE', #7416 ) ;
#11272=CARTESIAN_POINT ( 'NONE',  ( 26.49878054387835746, -2.963357534503999968, 6.861505862736166250 ) ) ;
#11274=CYLINDRICAL_SURFACE ( 'NONE', #15890, 2.500000000000001776 ) ;
#11283=DIRECTION ( 'NONE',  ( -1.000000000000000000, 0.000000000000000000, 0.000000000000000000 ) ) ;
#11284=FILL_AREA_STYLE_COLOUR ( '', #617 ) ;
#11293=EDGE_CURVE ( 'NONE', #13537, #8906, #10170, .T. ) ;
#11294=CARTESIAN_POINT ( 'NONE',  ( 28.56093688906631911, -4.595820017735426255, 7.939653947423662039 ) ) ;
#11298=PLANE ( 'NONE',  #3755 ) ;
#11303=LINE ( 'NONE', #3533, #13917 ) ;
#11308=VECTOR ( 'NONE', #7988, 1000.000000000000227 ) ;
#11309=VERTEX_POINT ( 'NONE', #14112 ) ;
#11315=CARTESIAN_POINT ( 'NONE',  ( 29.32081432955537892, -3.050456207659999475, 8.283357778048664244 ) ) ;
#11318=AXIS2_PLACEMENT_3D ( 'NONE', #9183, #10265, #16097 ) ;
#11323=LINE ( 'NONE', #3186, #17214 ) ;
#11330=ORIENTED_EDGE ( 'NONE', *, *, #3486, .T. ) ;
#11334=CARTESIAN_POINT ( 'NONE',  ( 27.18555652250208610, -2.580805812949960920, 4.533357778048667797 ) ) ;
#11339=DIRECTION ( 'NONE',  ( 0.1113444980252557837, -0.9937818688019538493, 0.000000000000000000 ) ) ;
#11341=CARTESIAN_POINT ( 'NONE',  ( 26.20620856698912604, -7.060238655668615415, 7.033357778048657138 ) ) ;
#11343=ADVANCED_FACE ( 'NONE', ( #9924 ), #7231, .F. ) ;
#11346=CARTESIAN_POINT ( 'NONE',  ( 27.00222791626931595, -2.275731535614434531, 5.783357778048668685 ) ) ;
#11347=CARTESIAN_POINT ( 'NONE',  ( -18.05624385570398260, -20.06430210183123464, 15.83921756800030245 ) ) ;
#11351=LINE ( 'NONE', #13815, #3565 ) ;
#11353=CARTESIAN_POINT ( 'NONE',  ( 25.71748644841968456, -2.420320648352046078, 5.783357778048663356 ) ) ;
#11358=VECTOR ( 'NONE', #2882, 1000.000000000000227 ) ;
#11360=SHAPE_DEFINITION_REPRESENTATION ( #9387, #691 ) ;
#11366=CARTESIAN_POINT ( 'NONE',  ( 30.80679339554874119, -2.444327062417882779, 4.705209693361168455 ) ) ;
#11367=ORIENTED_EDGE ( 'NONE', *, *, #4209, .T. ) ;
#11371=CARTESIAN_POINT ( 'NONE',  ( 27.62849893492243325, -6.589071975465733644, 6.861505862736158257 ) ) ;
#11377=CYLINDRICAL_SURFACE ( 'NONE', #6370, 13.00000000000000178 ) ;
#11380=DIRECTION ( 'NONE',  ( 0.8243186046180107640, 0.5661261679878571984, 0.000000000000000000 ) ) ;
#11382=EDGE_CURVE ( 'NONE', #8560, #11271, #17426, .T. ) ;
#11386=FACE_OUTER_BOUND ( 'NONE', #16248, .T. ) ;
#11389=VERTEX_POINT ( 'NONE', #14664 ) ;
#11393=VERTEX_POINT ( 'NONE', #17222 ) ;
#11395=( BOUNDED_CURVE ( )  B_SPLINE_CURVE ( 3, ( #4430, #8788, #14321, #17142 ),
 .UNSPECIFIED., .F., .T. ) 
 B_SPLINE_CURVE_WITH_KNOTS ( ( 4, 4 ),
 ( 4.846194975958193929, 4.967031014587541371 ),
 .UNSPECIFIED. ) 
 CURVE ( )  GEOMETRIC_REPRESENTATION_ITEM ( )  RATIONAL_B_SPLINE_CURVE ( ( 1.000000000000000000, 0.9987835910734579326, 0.9987835910734579326, 1.000000000000000000 ) ) 
 REPRESENTATION_ITEM ( '' )  );
#11396=EDGE_LOOP ( 'NONE', ( #16155, #14957 ) ) ;
#11397=CARTESIAN_POINT ( 'NONE',  ( 29.82181869931131146, -4.443908660051686610, 7.939653947423662039 ) ) ;
#11405=DIRECTION ( 'NONE',  ( 0.000000000000000000, 0.000000000000000000, -1.000000000000000000 ) ) ;
#11407=CARTESIAN_POINT ( 'NONE',  ( -3.248936832696171617, 17.78798921770683350, 17.00000000000000000 ) ) ;
#11410=DIRECTION ( 'NONE',  ( -0.000000000000000000, -0.000000000000000000, 1.000000000000000000 ) ) ;
#11413=CARTESIAN_POINT ( 'NONE',  ( 26.39379627684682106, -4.856917663858078882, 8.283357778048662468 ) ) ;
#11414=CARTESIAN_POINT ( 'NONE',  ( 28.44643833274707845, -2.428894455266221275, 4.533357778048667797 ) ) ;
#11417=EDGE_CURVE ( 'NONE', #9483, #6202, #3900, .T. ) ;
#11420=CARTESIAN_POINT ( 'NONE',  ( 26.58890374069123652, -3.379597482641427231, 3.283357778048666464 ) ) ;
#11427=EDGE_CURVE ( 'NONE', #10047, #10383, #17410, .T. ) ;
#11432=LINE ( 'NONE', #3025, #15864 ) ;
#11436=CARTESIAN_POINT ( 'NONE',  ( 31.91459173804834748, -5.445711903524953712, 7.939653947423658487 ) ) ;
#11450=CARTESIAN_POINT ( 'NONE',  ( 28.12379965168153362, -6.829206799398704675, 4.533357778048659803 ) ) ;
#11456=CARTESIAN_POINT ( 'NONE',  ( 33.10345976029034887, -2.594722134608779207, 8.283357778048666020 ) ) ;
#11457=CARTESIAN_POINT ( 'NONE',  ( 29.34898802046944155, -4.500875419183088866, 7.939653947423662039 ) ) ;
#11458=ORIENTED_EDGE ( 'NONE', *, *, #8133, .T. ) ;
#11459=ORIENTED_EDGE ( 'NONE', *, *, #2930, .F. ) ;
#11460=EDGE_CURVE ( 'NONE', #12849, #16241, #2673, .T. ) ;
#11463=CARTESIAN_POINT ( 'NONE',  ( 32.17274868998081416, -2.279756424927169345, 6.861505862736166250 ) ) ;
#11464=DIRECTION ( 'NONE',  ( 0.000000000000000000, 0.000000000000000000, 1.000000000000000000 ) ) ;
#11466=VERTEX_POINT ( 'NONE', #4212 ) ;
#11467=CARTESIAN_POINT ( 'NONE',  ( -2.016448651773435938E-27, -20.49999999999999645, 13.00000000000000178 ) ) ;
#11468=CARTESIAN_POINT ( 'NONE',  ( 0.000000000000000000, 0.000000000000000000, 12.00000000000000000 ) ) ;
#11477=CARTESIAN_POINT ( 'NONE',  ( 28.58911057998038885, -6.046239229258517867, 8.283357778048660691 ) ) ;
#11478=CARTESIAN_POINT ( 'NONE',  ( 29.75233713454258933, -1.544652646670201523, 5.783357778048668685 ) ) ;
#11482=VERTEX_POINT ( 'NONE', #13641 ) ;
#11484=CARTESIAN_POINT ( 'NONE',  ( 30.25533603959949502, -6.272589980291270351, 4.705209693361160461 ) ) ;
#11494=DIRECTION ( 'NONE',  ( -0.000000000000000000, -0.000000000000000000, 1.000000000000000000 ) ) ;
#11495=EDGE_CURVE ( 'NONE', #4518, #60, #11074, .T. ) ;
#11501=CARTESIAN_POINT ( 'NONE',  ( 26.02974819644417792, -2.720057890826728109, 7.033357778048666020 ) ) ;
#11502=CARTESIAN_POINT ( 'NONE',  ( 28.09001152836989235, -6.106370808549102414, 3.283357778048663800 ) ) ;
#11505=ORIENTED_EDGE ( 'NONE', *, *, #15334, .F. ) ;
#11507=ORIENTED_EDGE ( 'NONE', *, *, #9926, .F. ) ;
#11508=EDGE_CURVE ( 'NONE', #12121, #13857, #12461, .T. ) ;
#11510=ORIENTED_EDGE ( 'NONE', *, *, #14304, .T. ) ;
#11520=DIRECTION ( 'NONE',  ( 1.000000000000000000, 0.000000000000000000, 0.000000000000000000 ) ) ;
#11526=CARTESIAN_POINT ( 'NONE',  ( 32.54503264317084188, -5.369756224683081669, 7.939653947423658487 ) ) ;
#11527=VECTOR ( 'NONE', #13838, 1000.000000000000227 ) ;
#11528=ADVANCED_FACE ( 'NONE', ( #6657 ), #16635, .F. ) ;
#11530=CARTESIAN_POINT ( 'NONE',  ( -26.11936545685874833, -21.64910423302892895, 14.20663795870742696 ) ) ;
#11531=FACE_OUTER_BOUND ( 'NONE', #2589, .T. ) ;
#11536=CARTESIAN_POINT ( 'NONE',  ( 34.91600907648203389, -11.88801210197604341, 11.56671555609732671 ) ) ;
#11537=ORIENTED_EDGE ( 'NONE', *, *, #14065, .F. ) ;
#11541=EDGE_CURVE ( 'NONE', #8190, #15383, #7394, .T. ) ;
#11547=CARTESIAN_POINT ( 'NONE',  ( 31.56875459193803124, -6.114348982704044921, 6.861505862736157368 ) ) ;
#11555=EDGE_CURVE ( 'NONE', #10383, #10047, #11740, .T. ) ;
#11556=CARTESIAN_POINT ( 'NONE',  ( 33.46007730730551799, -5.886481946178435010, 6.861505862736157368 ) ) ;
#11564=LINE ( 'NONE', #5857, #8743 ) ;
#11568=CARTESIAN_POINT ( 'NONE',  ( 28.29630561643014275, -19.54286113573893502, 13.63865706309495884 ) ) ;
#11570=SURFACE_STYLE_FILL_AREA ( #6041 ) ;
#11574=CARTESIAN_POINT ( 'NONE',  ( 31.35480929215617252, -6.439933945126671055, 4.533357778048659803 ) ) ;
#11578=CARTESIAN_POINT ( 'NONE',  ( 26.34117031759772942, -2.982346454214467535, 6.861505862736165362 ) ) ;
#11588=EDGE_LOOP ( 'NONE', ( #4237, #8067, #12161, #9317 ) ) ;
#11592=EDGE_CURVE ( 'NONE', #17243, #17459, #14459, .T. ) ;
#11595=ORIENTED_EDGE ( 'NONE', *, *, #12502, .F. ) ;
#11597=CYLINDRICAL_SURFACE ( 'NONE', #9283, 2.500000000000001776 ) ;
#11598=CARTESIAN_POINT ( 'NONE',  ( 35.46635924378174565, -16.45598204045931823, 11.37070560279563480 ) ) ;
#11603=CARTESIAN_POINT ( 'NONE',  ( 30.04891049036066164, -7.324175753722694360, 5.783357778048657138 ) ) ;
#11608=ORIENTED_EDGE ( 'NONE', *, *, #15671, .T. ) ;
#11610=ORIENTED_EDGE ( 'NONE', *, *, #7546, .F. ) ;
#11611=ADVANCED_FACE ( 'NONE', ( #6193 ), #6101, .F. ) ;
#11620=FACE_BOUND ( 'NONE', #9903, .T. ) ;
#11624=VERTEX_POINT ( 'NONE', #4822 ) ;
#11625=CARTESIAN_POINT ( 'NONE',  ( 25.40682704530840397, -3.522014380262483702, 3.283357778048666464 ) ) ;
#11626=AXIS2_PLACEMENT_3D ( 'NONE', #14515, #725, #13051 ) ;
#11628=ORIENTED_EDGE ( 'NONE', *, *, #13467, .T. ) ;
#11635=ORIENTED_EDGE ( 'NONE', *, *, #1673, .T. ) ;
#11639=AXIS2_PLACEMENT_3D ( 'NONE', #12300, #15011, #12205 ) ;
#11640=( BOUNDED_CURVE ( )  B_SPLINE_CURVE ( 3, ( #12506, #8516, #4342, #5780 ),
 .UNSPECIFIED., .F., .T. ) 
 B_SPLINE_CURVE_WITH_KNOTS ( ( 4, 4 ),
 ( 3.141592653589793116, 6.283185307179586232 ),
 .UNSPECIFIED. ) 
 CURVE ( )  GEOMETRIC_REPRESENTATION_ITEM ( )  RATIONAL_B_SPLINE_CURVE ( ( 1.000000000000000000, 0.3333333333333333703, 0.3333333333333333703, 1.000000000000000000 ) ) 
 REPRESENTATION_ITEM ( '' )  );
#11642=DIRECTION ( 'NONE',  ( -0.1196152422706620172, 0.9928203230275510771, 0.000000000000000000 ) ) ;
#11645=EDGE_CURVE ( 'NONE', #4376, #9400, #15657, .T. ) ;
#11648=CARTESIAN_POINT ( 'NONE',  ( 27.45766530510195835, -4.728742455708699666, 7.939653947423662039 ) ) ;
#11651=ORIENTED_EDGE ( 'NONE', *, *, #4462, .T. ) ;
#11654=CARTESIAN_POINT ( 'NONE',  ( 33.76207435632690590, -3.969185667289998332, 7.939653947423662039 ) ) ;
#11659=CARTESIAN_POINT ( 'NONE',  ( 45.50000000000000000, -16.03270077640482683, 2.787981825772258837 ) ) ;
#11666=LINE ( 'NONE', #7951, #13601 ) ;
#11672=CARTESIAN_POINT ( 'NONE',  ( 29.81991338116587542, -2.990324628369393611, 3.283357778048666464 ) ) ;
#11673=ORIENTED_EDGE ( 'NONE', *, *, #4632, .F. ) ;
#11674=ORIENTED_EDGE ( 'NONE', *, *, #5451, .F. ) ;
#11675=VERTEX_POINT ( 'NONE', #8832 ) ;
#11677=CARTESIAN_POINT ( 'NONE',  ( 32.82963640218302004, -5.962437625020304388, 6.861505862736157368 ) ) ;
#11678=DIRECTION ( 'NONE',  ( 0.000000000000000000, 0.000000000000000000, -1.000000000000000000 ) ) ;
#11687=VERTEX_POINT ( 'NONE', #14368 ) ;
#11692=ORIENTED_EDGE ( 'NONE', *, *, #3515, .T. ) ;
#11693=LINE ( 'NONE', #17263, #8336 ) ;
#11694=EDGE_CURVE ( 'NONE', #9271, #8079, #671, .T. ) ;
#11695=CARTESIAN_POINT ( 'NONE',  ( 29.86122125502053848, -4.439161430227785310, 3.283357778048664244 ) ) ;
#11696=ORIENTED_EDGE ( 'NONE', *, *, #6840, .F. ) ;
#11700=VERTEX_POINT ( 'NONE', #2565 ) ;
#11706=CARTESIAN_POINT ( 'NONE',  ( 21.42601376483257880, 2.765314980223224417, 0.000000000000000000 ) ) ;
#11708=CARTESIAN_POINT ( 'NONE',  ( 27.49335874655903567, -6.905162478240574053, 4.533357778048659803 ) ) ;
#11711=DIRECTION ( 'NONE',  ( -0.000000000000000000, -0.000000000000000000, 1.000000000000000000 ) ) ;
#11712=CARTESIAN_POINT ( 'NONE',  ( 31.30154412293507349, -3.011689903141150815, 3.627061608673666893 ) ) ;
#11714=ORIENTED_EDGE ( 'NONE', *, *, #2046, .T. ) ;
#11716=CARTESIAN_POINT ( 'NONE',  ( 8.632250723006720250, -18.84644399697197770, 13.00000000000000178 ) ) ;
#11717=DIRECTION ( 'NONE',  ( -0.1196152422706610735, 0.9928203230275511881, 0.000000000000000000 ) ) ;
#11719=CARTESIAN_POINT ( 'NONE',  ( 26.31065902414478330, -7.328232685206446106, 5.254681170202263552 ) ) ;
#11723=CARTESIAN_POINT ( 'NONE',  ( 33.40745134805642635, -4.011910736534825439, 8.283357778048662468 ) ) ;
#11724=ORIENTED_EDGE ( 'NONE', *, *, #7020, .F. ) ;
#11732=CARTESIAN_POINT ( 'NONE',  ( 27.91310269393460430, -7.181753375802955475, 5.783357778048657138 ) ) ;
#11737=CARTESIAN_POINT ( 'NONE',  ( 32.95662993491455950, -6.574107945067995118, 5.783357778048657138 ) ) ;
#11738=CARTESIAN_POINT ( 'NONE',  ( 28.19013153391124860, -7.158573733970061248, 5.783357778048669573 ) ) ;
#11740=B_SPLINE_CURVE_WITH_KNOTS ( 'NONE', 3,
 ( #410, #14178, #8650, #3117, #1769, #7029, #17099, #16820, #1865, #7298, #11347, #14088, #4475, #6001, #12721, #14004, #12817, #4652, #4387, #13903, #5914, #8748, #17004, #4558, #2842, #10080, #315, #2937, #8371, #11530, #15630, #12547, #1587, #7120, #3207, #14279, #9901, #15450, #3033, #8556, #1675, #16919, #5821 ),
 .UNSPECIFIED., .F., .F.,
 ( 4, 2, 2, 1, 2, 2, 2, 2, 2, 2, 2, 2, 2, 2, 2, 2, 2, 2, 2, 2, 2, 4 ),
 ( 0.01976914256504654077, 0.02100445419277401429, 0.02162211000663775626, 0.02223976582050150169, 0.02285742163436524366, 0.02347507744822898562, 0.02471038907595646955, 0.02594570070368395695, 0.02718101233141144435, 0.02779866814527519325, 0.02841632395913894216, 0.02965163558686643996, 0.03088694721459393777, 0.03150460302845767974, 0.03212225884232142170, 0.03335757047004890563, 0.03459288209777638956, 0.03582819372550387349, 0.03644584953936762239, 0.03706350535323135742, 0.03829881698095885523, 0.03953412860868634610 ),
 .UNSPECIFIED. ) ;
#11749=DIRECTION ( 'NONE',  ( -0.1196152422706610735, 0.9928203230275511881, 0.000000000000000000 ) ) ;
#11755=CARTESIAN_POINT ( 'NONE',  ( 30.25524682244395436, -4.391689130744175884, 8.283357778048662468 ) ) ;
#11761=CARTESIAN_POINT ( 'NONE',  ( 33.33308377457396432, -5.274811626130743392, 7.939653947423658487 ) ) ;
#11762=ORIENTED_EDGE ( 'NONE', *, *, #10374, .F. ) ;
#11769=CYLINDRICAL_SURFACE ( 'NONE', #9006, 2.000000000000001776 ) ;
#11770=VERTEX_POINT ( 'NONE', #16183 ) ;
#11771=CARTESIAN_POINT ( 'NONE',  ( 15.39462056267347734, 12.71537873815137232, 16.22282132715419678 ) ) ;
#11774=EDGE_LOOP ( 'NONE', ( #13245, #8151, #13922, #1254 ) ) ;
#11790=AXIS2_PLACEMENT_3D ( 'NONE', #16976, #10567, #1927 ) ;
#11801=AXIS2_PLACEMENT_3D ( 'NONE', #9949, #16964, #3081 ) ;
#11811=EDGE_CURVE ( 'NONE', #11466, #7755, #12072, .T. ) ;
#11813=CARTESIAN_POINT ( 'NONE',  ( 30.10960860451258370, -6.927314653643411368, 5.113484796970852564 ) ) ;
#11814=VECTOR ( 'NONE', #9499, 999.9999999999998863 ) ;
#11824=CARTESIAN_POINT ( 'NONE',  ( 33.45617745041539592, -1.098413033681664430, 5.783357778048668685 ) ) ;
#11826=CARTESIAN_POINT ( 'NONE',  ( 26.30654288775393113, -7.309557114202775985, 6.143482903293868702 ) ) ;
#11828=CARTESIAN_POINT ( 'NONE',  ( 32.69811611091622439, -2.216460025892273311, 4.705209693361168455 ) ) ;
#11829=CARTESIAN_POINT ( 'NONE',  ( -19.73861724507318627, -10.88265359452670644, 15.55811197012310743 ) ) ;
#11833=AXIS2_PLACEMENT_3D ( 'NONE', #1953, #9010, #11717 ) ;
#11836=VERTEX_POINT ( 'NONE', #114 ) ;
#11837=CARTESIAN_POINT ( 'NONE',  ( -34.91600907648203389, -11.88801210197604341, 12.00000000000000000 ) ) ;
#11840=FACE_OUTER_BOUND ( 'NONE', #12762, .T. ) ;
#11846=CARTESIAN_POINT ( 'NONE',  ( 32.37175601071535880, -5.590505156207296267, 8.283357778048658915 ) ) ;
#11847=AXIS2_PLACEMENT_3D ( 'NONE', #2787, #12484, #4239 ) ;
#11849=ORIENTED_EDGE ( 'NONE', *, *, #2277, .F. ) ;
#11851=CARTESIAN_POINT ( 'NONE',  ( 26.47269060886452507, -6.728324053342490174, 4.705209693361160461 ) ) ;
#11853=VECTOR ( 'NONE', #15805, 1000.000000000000114 ) ;
#11854=CARTESIAN_POINT ( 'NONE',  ( 32.69811611091622439, -2.216460025892273311, 4.705209693361168455 ) ) ;
#11855=ORIENTED_EDGE ( 'NONE', *, *, #10713, .F. ) ;
#11856=DIRECTION ( 'NONE',  ( 1.000000000000000000, 0.000000000000000000, 0.000000000000000000 ) ) ;
#11874=CARTESIAN_POINT ( 'NONE',  ( 26.70901672940806648, -4.818939824437135755, 3.283357778048664244 ) ) ;
#11875=AXIS2_PLACEMENT_3D ( 'NONE', #6083, #10946, #1097 ) ;
#11880=DIRECTION ( 'NONE',  ( -1.000000000000000000, 0.000000000000000000, 0.000000000000000000 ) ) ;
#11883=ORIENTED_EDGE ( 'NONE', *, *, #1104, .T. ) ;
#11895=EDGE_CURVE ( 'NONE', #14407, #9693, #14221, .T. ) ;
#11898=DIRECTION ( 'NONE',  ( 0.000000000000000000, 0.000000000000000000, -1.000000000000000000 ) ) ;
#11900=CARTESIAN_POINT ( 'NONE',  ( 0.000000000000000000, 0.000000000000000000, 10.50000000000000000 ) ) ;
#11902=CARTESIAN_POINT ( 'NONE',  ( 26.10492286888474922, -5.636087676172644834, 3.446205193745024431 ) ) ;
#11907=DIRECTION ( 'NONE',  ( -0.1196152422706610735, 0.9928203230275511881, 0.000000000000000000 ) ) ;
#11909=CARTESIAN_POINT ( 'NONE',  ( 36.27615609941022257, -23.17738945083361557, 12.00000000000000000 ) ) ;
#11913=CARTESIAN_POINT ( 'NONE',  ( 26.37178701114681800, -2.351687214456304353, 5.783357778048668685 ) ) ;
#11918=ORIENTED_EDGE ( 'NONE', *, *, #16812, .F. ) ;
#11919=CARTESIAN_POINT ( 'NONE',  ( 30.18087924896149588, -5.654590020340094725, 7.939653947423658487 ) ) ;
#11920=CARTESIAN_POINT ( 'NONE',  ( -29.20850947011023280, -15.38975055298431549, 13.38439523458337099 ) ) ;
#11922=EDGE_CURVE ( 'NONE', #7124, #8890, #2911, .T. ) ;
#11923=ORIENTED_EDGE ( 'NONE', *, *, #5296, .F. ) ;
#11926=AXIS2_PLACEMENT_3D ( 'NONE', #8233, #13766, #17964 ) ;
#11927=LINE ( 'NONE', #10382, #5197 ) ;
#11928=FACE_BOUND ( 'NONE', #10009, .T. ) ;
#11939=CARTESIAN_POINT ( 'NONE',  ( 26.94172295629870462, -6.971623697019761146, 4.533357778048659803 ) ) ;
#11946=ORIENTED_EDGE ( 'NONE', *, *, #4448, .T. ) ;
#11947=CARTESIAN_POINT ( 'NONE',  ( 26.24062359194589433, -6.129313013101782559, 7.939653947423658487 ) ) ;
#11949=DIRECTION ( 'NONE',  ( -1.000000000000000000, 0.000000000000000000, 0.000000000000000000 ) ) ;
#11952=PRESENTATION_STYLE_ASSIGNMENT (( #17150 ) ) ;
#11955=LINE ( 'NONE', #1263, #15983 ) ;
#11965=EDGE_LOOP ( 'NONE', ( #11505, #4562, #2675, #10910 ) ) ;
#11975=CARTESIAN_POINT ( 'NONE',  ( 25.85239768453567777, -3.540099486550930763, 7.452613241158525526 ) ) ;
#11978=CIRCLE ( 'NONE', #12267, 2.749999999999992895 ) ;
#11980=VERTEX_POINT ( 'NONE', #4992 ) ;
#11990=CARTESIAN_POINT ( 'NONE',  ( 30.66050125466253107, -2.889050389913576655, 8.283357778048666020 ) ) ;
#11992=VERTEX_POINT ( 'NONE', #15987 ) ;
#11994=DIRECTION ( 'NONE',  ( -0.000000000000000000, -0.000000000000000000, 1.000000000000000000 ) ) ;
#11995=CARTESIAN_POINT ( 'NONE',  ( -3.538288549924106796, -15.34800872113743431, 13.00000000000000178 ) ) ;
#11997=CARTESIAN_POINT ( 'NONE',  ( 32.84384354600314282, -1.561735352540135180, 5.113484796970859669 ) ) ;
#12002=FACE_BOUND ( 'NONE', #8324, .T. ) ;
#12006=CARTESIAN_POINT ( 'NONE',  ( 27.12922144900085186, -2.887401855662130146, 6.861505862736166250 ) ) ;
#12010=CARTESIAN_POINT ( 'NONE',  ( 30.30787278169304244, -6.266260340387784566, 6.861505862736157368 ) ) ;
#12012=ORIENTED_EDGE ( 'NONE', *, *, #7118, .F. ) ;
#12014=PLANE ( 'NONE',  #7246 ) ;
#12023=LINE ( 'NONE', #17527, #16184 ) ;
#12025=CARTESIAN_POINT ( 'NONE',  ( 28.58911057998038530, -6.046239229258517867, 8.283357778048658915 ) ) ;
#12027=EDGE_LOOP ( 'NONE', ( #1990, #68 ) ) ;
#12029=CARTESIAN_POINT ( 'NONE',  ( 32.02836186724004364, -4.178063784105134459, 3.627061608673664228 ) ) ;
#12030=CARTESIAN_POINT ( 'NONE',  ( 30.19827253897071273, -3.144612341114421561, 3.627061608673666449 ) ) ;
#12031=ORIENTED_EDGE ( 'NONE', *, *, #2994, .F. ) ;
#12034=CARTESIAN_POINT ( 'NONE',  ( -45.50000000000000000, -16.03270077640482683, 5.537981825772250843 ) ) ;
#12036=CARTESIAN_POINT ( 'NONE',  ( 29.81239362717914787, -2.264323817775507397, 7.033357778048666020 ) ) ;
#12038=DIRECTION ( 'NONE',  ( 0.000000000000000000, 0.000000000000000000, -1.000000000000000000 ) ) ;
#12042=CARTESIAN_POINT ( 'NONE',  ( 18.06432791129289939, -12.37828432491873443, 15.83774382844986484 ) ) ;
#12050=EDGE_LOOP ( 'NONE', ( #7899, #7963, #16786, #13412 ) ) ;
#12051=CARTESIAN_POINT ( 'NONE',  ( 32.51858583609114106, -1.611119345748072362, 5.783357778048668685 ) ) ;
#12056=EDGE_CURVE ( 'NONE', #14281, #6423, #7641, .T. ) ;
#12070=ORIENTED_EDGE ( 'NONE', *, *, #11495, .F. ) ;
#12071=CARTESIAN_POINT ( 'NONE',  ( -45.50000000000000000, -16.03270077640482683, 5.537981825772250843 ) ) ;
#12072=LINE ( 'NONE', #1384, #11270 ) ;
#12073=ORIENTED_EDGE ( 'NONE', *, *, #8160, .F. ) ;
#12074=CARTESIAN_POINT ( 'NONE',  ( 25.76775864925887660, -2.837585720338236861, 5.127143661396867280 ) ) ;
#12076=EDGE_CURVE ( 'NONE', #8906, #8079, #15672, .T. ) ;
#12082=CARTESIAN_POINT ( 'NONE',  ( 31.61111609099199171, -1.710254666422835745, 5.783357778048665132 ) ) ;
#12086=CARTESIAN_POINT ( 'NONE',  ( 32.26287188679368967, -2.695996373064596607, 3.283357778048666464 ) ) ;
#12087=VERTEX_POINT ( 'NONE', #563 ) ;
#12089=AXIS2_PLACEMENT_3D ( 'NONE', #4551, #3109, #11520 ) ;
#12092=CARTESIAN_POINT ( 'NONE',  ( 28.39010325924584421, -2.735490497978389612, 6.861505862736166250 ) ) ;
#12094=CARTESIAN_POINT ( 'NONE',  ( -2.016448651773435938E-27, -20.49999999999999645, 17.00000000000000000 ) ) ;
#12096=DIRECTION ( 'NONE',  ( -1.000000000000000000, 0.000000000000000000, 0.000000000000000000 ) ) ;
#12098=DIRECTION ( 'NONE',  ( 0.000000000000000000, 1.000000000000000000, 0.000000000000000000 ) ) ;
#12104=AXIS2_PLACEMENT_3D ( 'NONE', #6882, #11116, #5514 ) ;
#12106=CIRCLE ( 'NONE', #5436, 14.00000000000000178 ) ;
#12108=CARTESIAN_POINT ( 'NONE',  ( 27.12505156253147476, -7.276697974355294640, 5.783357778048658027 ) ) ;
#12111=CARTESIAN_POINT ( 'NONE',  ( 33.32855701603872234, -2.140504347050403045, 4.705209693361168455 ) ) ;
#12112=AXIS2_PLACEMENT_3D ( 'NONE', #3156, #7248, #11194 ) ;
#12113=CARTESIAN_POINT ( 'NONE',  ( 27.46709037723411839, -6.908327297984874882, 7.033357778048657138 ) ) ;
#12114=( BOUNDED_CURVE ( )  B_SPLINE_CURVE ( 2, ( #2876, #16854, #12391, #14032, #12660, #5401, #10919, #4058, #9740 ),
 .UNSPECIFIED., .F., .T. ) 
 B_SPLINE_CURVE_WITH_KNOTS ( ( 3, 2, 2, 2, 3 ),
 ( 0.5192307692307692735, 0.5256410256410256610, 0.5384615384615384359, 0.5512820512820513219, 0.5576923076923077094 ),
 .UNSPECIFIED. ) 
 CURVE ( )  GEOMETRIC_REPRESENTATION_ITEM ( )  RATIONAL_B_SPLINE_CURVE ( ( 0.9330127018922192983, 0.9330127018922198534, 1.000000000000000000, 0.8660254037844387076, 1.000000000000000000, 0.8660254037844387076, 1.000000000000000000, 0.9330127018922194093, 0.9330127018922194093 ) ) 
 REPRESENTATION_ITEM ( '' )  );
#12121=VERTEX_POINT ( 'NONE', #9590 ) ;
#12122=B_SPLINE_CURVE_WITH_KNOTS ( 'NONE', 3,
 ( #11407, #5793, #17064, #12781, #4446, #5884, #10046, #4617, #14242, #10141, #2373, #13508, #5147, #9070, #10666, #10413 ),
 .UNSPECIFIED., .F., .F.,
 ( 4, 2, 2, 2, 2, 2, 2, 4 ),
 ( 0.000000000000000000, 0.004966453901722449327, 0.007449680852583671388, 0.008691294328014282852, 0.009932907803444893449, 0.01489936170516735839, 0.01738258865602858652, 0.01986581560688981465 ),
 .UNSPECIFIED. ) ;
#12123=CARTESIAN_POINT ( 'NONE',  ( 33.40754056521197413, -5.892811586081919906, 4.705209693361160461 ) ) ;
#12124=CARTESIAN_POINT ( 'NONE',  ( 29.77797860222238313, -3.195249460342344250, 7.939653947423662927 ) ) ;
#12126=DIRECTION ( 'NONE',  ( 0.000000000000000000, 0.000000000000000000, -1.000000000000000000 ) ) ;
#12127=CARTESIAN_POINT ( 'NONE',  ( 32.33415724766913257, -1.960501102408027219, 7.033357778048666020 ) ) ;
#12128=FACE_OUTER_BOUND ( 'NONE', #928, .T. ) ;
#12131=EDGE_LOOP ( 'NONE', ( #8552, #3408 ) ) ;
#12137=AXIS2_PLACEMENT_3D ( 'NONE', #8372, #490, #7121 ) ;
#12144=EDGE_CURVE ( 'NONE', #15022, #4229, #5334, .T. ) ;
#12146=CARTESIAN_POINT ( 'NONE',  ( 31.08270050955629671, -4.291997302367946077, 7.939653947423662039 ) ) ;
#12149=DIRECTION ( 'NONE',  ( 0.1196152422706621143, 0.9928203230275509661, 0.000000000000000000 ) ) ;
#12160=EDGE_CURVE ( 'NONE', #1847, #9483, #8876, .T. ) ;
#12161=ORIENTED_EDGE ( 'NONE', *, *, #12144, .T. ) ;
#12163=VECTOR ( 'NONE', #17297, 1000.000000000000000 ) ;
#12164=PLANE ( 'NONE',  #102 ) ;
#12177=CARTESIAN_POINT ( 'NONE',  ( 31.63243098167119172, -2.771952051906466430, 3.283357778048666464 ) ) ;
#12181=CARTESIAN_POINT ( 'NONE',  ( 33.50243880635947846, -1.482387629897225390, 5.783357778048663356 ) ) ;
#12182=CARTESIAN_POINT ( 'NONE',  ( 32.69820532807177216, -4.097360875439379768, 8.283357778048662468 ) ) ;
#12185=CARTESIAN_POINT ( 'NONE',  ( 30.60986983071443390, -4.348964061499348333, 7.939653947423662039 ) ) ;
#12186=DIRECTION ( 'NONE',  ( 1.000000000000000000, 0.000000000000000000, 0.000000000000000000 ) ) ;
#12187=CARTESIAN_POINT ( 'NONE',  ( 28.72045243349238675, -6.030415129707233035, 3.283357778048663356 ) ) ;
#12192=ORIENTED_EDGE ( 'NONE', *, *, #15299, .T. ) ;
#12202=CARTESIAN_POINT ( 'NONE',  ( 26.87106449706838873, -6.053357334259913181, 7.939653947423658487 ) ) ;
#12203=( BOUNDED_CURVE ( )  B_SPLINE_CURVE ( 2, ( #3206, #14278, #1864, #5178, #6978, #11990, #2402, #13862, #6477 ),
 .UNSPECIFIED., .F., .T. ) 
 B_SPLINE_CURVE_WITH_KNOTS ( ( 3, 2, 2, 2, 3 ),
 ( 0.2884615384615384914, 0.2948717948717948789, 0.3076923076923077094, 0.3205128205128205399, 0.3269230769230769273 ),
 .UNSPECIFIED. ) 
 CURVE ( )  GEOMETRIC_REPRESENTATION_ITEM ( )  RATIONAL_B_SPLINE_CURVE ( ( 0.9330127018922194093, 0.9330127018922196314, 1.000000000000000000, 0.8660254037844387076, 1.000000000000000000, 0.8660254037844387076, 1.000000000000000000, 0.9330127018922194093, 0.9330127018922194093 ) ) 
 REPRESENTATION_ITEM ( '' )  );
#12204=CARTESIAN_POINT ( 'NONE',  ( 29.64681518302145591, -6.972875258987813574, 5.783357778048658027 ) ) ;
#12205=DIRECTION ( 'NONE',  ( -0.1196152422706610735, 0.9928203230275511881, 0.000000000000000000 ) ) ;
#12206=CARTESIAN_POINT ( 'NONE',  ( 32.52441275490655670, -6.636378442139655220, 5.783357778048664244 ) ) ;
#12207=CARTESIAN_POINT ( 'NONE',  ( 32.28234893270314387, -5.401404424200516807, 3.627061608673662896 ) ) ;
#12208=VECTOR ( 'NONE', #15422, 1000.000000000000000 ) ;
#12209=CARTESIAN_POINT ( 'NONE',  ( 27.86101441917510257, -1.772519683195811657, 5.783357778048668685 ) ) ;
#12211=ORIENTED_EDGE ( 'NONE', *, *, #14243, .F. ) ;
#12212=AXIS2_PLACEMENT_3D ( 'NONE', #14119, #15759, #1622 ) ;
#12213=AXIS2_PLACEMENT_3D ( 'NONE', #8006, #11063, #4109 ) ;
#12215=ORIENTED_EDGE ( 'NONE', *, *, #6529, .F. ) ;
#12216=CARTESIAN_POINT ( 'NONE',  ( 31.08270050955629671, -4.291997302367946077, 7.939653947423662039 ) ) ;
#12217=CARTESIAN_POINT ( 'NONE',  ( -5.499998387031001634, -20.49508120620799900, 12.00000000000000000 ) ) ;
#12218=CARTESIAN_POINT ( 'NONE',  ( 29.34898802046944155, -4.500875419183088866, 7.939653947423662039 ) ) ;
#12219=CARTESIAN_POINT ( 'NONE',  ( 29.79859849048667897, -1.928627242885762705, 5.783357778048662468 ) ) ;
#12220=DIRECTION ( 'NONE',  ( 0.000000000000000000, 0.000000000000000000, -1.000000000000000000 ) ) ;
#12223=VECTOR ( 'NONE', #1335, 1000.000000000000000 ) ;
#12224=CARTESIAN_POINT ( 'NONE',  ( 30.63309003953906995, -6.864245478665264244, 5.783357778048664244 ) ) ;
#12229=CARTESIAN_POINT ( 'NONE',  ( 29.24999999999999645, -15.80522841342829921, 13.37255996287877480 ) ) ;
#12236=B_SPLINE_CURVE_WITH_KNOTS ( 'NONE', 3,
 ( #2680, #8208, #3947, #15000 ),
 .UNSPECIFIED., .F., .F.,
 ( 4, 4 ),
 ( 0.004328141481285538092, 0.004974662558709086295 ),
 .UNSPECIFIED. ) ;
#12238=DIRECTION ( 'NONE',  ( -0.7999999999999999334, 0.6000000000000000888, 0.000000000000000000 ) ) ;
#12240=VERTEX_POINT ( 'NONE', #10597 ) ;
#12241=ORIENTED_EDGE ( 'NONE', *, *, #6303, .F. ) ;
#12242=CARTESIAN_POINT ( 'NONE',  ( 33.60446413004628141, -3.988174587000466342, 7.939653947423662039 ) ) ;
#12246=CIRCLE ( 'NONE', #4428, 2.749999999999991118 ) ;
#12250=CARTESIAN_POINT ( 'NONE',  ( 25.80685721358263152, -3.162108319002908896, 7.047028914770492314 ) ) ;
#12252=EDGE_CURVE ( 'NONE', #1184, #5157, #17154, .T. ) ;
#12253=CIRCLE ( 'NONE', #4152, 2.749999999999988454 ) ;
#12259=CARTESIAN_POINT ( 'NONE',  ( 30.37838863598085837, -1.858773980305536089, 6.453230759126469707 ) ) ;
#12264=CARTESIAN_POINT ( 'NONE',  ( 45.00000000000000711, -19.03270077640482683, 10.53798182577225084 ) ) ;
#12265=AXIS2_PLACEMENT_3D ( 'NONE', #903, #6525, #5144 ) ;
#12267=AXIS2_PLACEMENT_3D ( 'NONE', #4944, #7682, #4850 ) ;
#12271=DIRECTION ( 'NONE',  ( 0.9937818688019538493, -0.1113444980252557837, 0.000000000000000000 ) ) ;
#12281=EDGE_CURVE ( 'NONE', #118, #11675, #17558, .T. ) ;
#12282=CARTESIAN_POINT ( 'NONE',  ( 29.02054416436834217, -2.659534819136519790, 6.861505862736166250 ) ) ;
#12284=CARTESIAN_POINT ( 'NONE',  ( 18.32374253600956493, -20.38504502893476200, 15.79679025666372283 ) ) ;
#12297=CARTESIAN_POINT ( 'NONE',  ( 32.34851646621051202, -1.621412483717243447, 6.453230759126471483 ) ) ;
#12299=CARTESIAN_POINT ( 'NONE',  ( 27.60205212784272177, -2.830435096530727446, 6.861505862736165362 ) ) ;
#12300=CARTESIAN_POINT ( 'NONE',  ( 26.01652455409633902, -4.902371455920926380, 5.783357778048663356 ) ) ;
#12305=ADVANCED_FACE ( 'NONE', ( #8250 ), #2729, .F. ) ;
#12306=CARTESIAN_POINT ( 'NONE',  ( 30.13703915187255689, -4.405930820630744371, 3.627061608673664228 ) ) ;
#12309=CARTESIAN_POINT ( 'NONE',  ( 30.60986983071443390, -4.348964061499348333, 7.939653947423662039 ) ) ;
#12310=DIRECTION ( 'NONE',  ( 1.000000000000000000, 0.000000000000000000, 0.000000000000000000 ) ) ;
#12311=DIRECTION ( 'NONE',  ( -0.000000000000000000, -0.000000000000000000, 1.000000000000000000 ) ) ;
#12312=PLANE ( 'NONE',  #14230 ) ;
#12318=DIRECTION ( 'NONE',  ( -0.1196152422706610735, 0.9928203230275511881, 0.000000000000000000 ) ) ;
#12327=CARTESIAN_POINT ( 'NONE',  ( 31.91459173804835103, -5.445711903524953712, 7.939653947423658487 ) ) ;
#12340=CARTESIAN_POINT ( 'NONE',  ( 27.17934203385504333, -30.00000000000000355, 12.00000000000000000 ) ) ;
#12341=CARTESIAN_POINT ( 'NONE',  ( 0.000000000000000000, 0.000000000000000000, 10.50000000000000000 ) ) ;
#12342=CARTESIAN_POINT ( 'NONE',  ( -45.00000000000000711, -16.03270077640482683, 0.5379818257722508434 ) ) ;
#12344=ORIENTED_EDGE ( 'NONE', *, *, #8818, .T. ) ;
#12345=ADVANCED_FACE ( 'NONE', ( #11035 ), #9857, .F. ) ;
#12346=EDGE_LOOP ( 'NONE', ( #9514, #11510 ) ) ;
#12354=CYLINDRICAL_SURFACE ( 'NONE', #1149, 2.000000000000001776 ) ;
#12362=AXIS2_PLACEMENT_3D ( 'NONE', #17281, #12990, #10075 ) ;
#12364=CARTESIAN_POINT ( 'NONE',  ( 26.62577407660990758, -3.575027854551694695, 7.939653947423664704 ) ) ;
#12365=CARTESIAN_POINT ( 'NONE',  ( 25.71748644841968456, -2.420320648352046078, 5.783357778048663356 ) ) ;
#12373=CARTESIAN_POINT ( 'NONE',  ( 28.09001152836988524, -6.106370808549102414, 3.283357778048663356 ) ) ;
#12375=CARTESIAN_POINT ( 'NONE',  ( 26.88845778707760914, -3.543379655034240905, 3.627061608673666893 ) ) ;
#12376=CARTESIAN_POINT ( 'NONE',  ( 30.23341599105502908, -5.648260380436597394, 3.627061608673662896 ) ) ;
#12377=VECTOR ( 'NONE', #16594, 1000.000000000000227 ) ;
#12380=CYLINDRICAL_SURFACE ( 'NONE', #1487, 2.749999999999992006 ) ;
#12381=ORIENTED_EDGE ( 'NONE', *, *, #16624, .F. ) ;
#12384=CARTESIAN_POINT ( 'NONE',  ( 32.79901970863393501, -6.593096864778464017, 5.783357778048658027 ) ) ;
#12385=CARTESIAN_POINT ( 'NONE',  ( 36.07773319708005744, -23.32620662758124297, 11.14818368178938357 ) ) ;
#12387=CARTESIAN_POINT ( 'NONE',  ( 30.29464937815318493, -4.386941900920275472, 3.627061608673664228 ) ) ;
#12389=DIRECTION ( 'NONE',  ( -0.000000000000000000, 1.000000000000000000, -3.469446951953614189E-16 ) ) ;
#12390=CARTESIAN_POINT ( 'NONE',  ( 27.27683486999669427, -2.232449958253242883, 5.783357778048667797 ) ) ;
#12391=CARTESIAN_POINT ( 'NONE',  ( 29.35841309260160159, -6.680460261459264970, 7.033357778048657138 ) ) ;
#12392=CIRCLE ( 'NONE', #15583, 13.00000000000000178 ) ;
#12399=CARTESIAN_POINT ( 'NONE',  ( 26.24741491880506672, -3.420740141806666301, 8.283357778048666020 ) ) ;
#12407=ORIENTED_EDGE ( 'NONE', *, *, #11382, .T. ) ;
#12409=CARTESIAN_POINT ( 'NONE',  ( 33.19286683830256379, -2.783822866615540459, 3.627061608673666449 ) ) ;
#12413=DIRECTION ( 'NONE',  ( -0.000000000000000000, -0.000000000000000000, 1.000000000000000000 ) ) ;
#12417=DIRECTION ( 'NONE',  ( -0.000000000000000000, -0.000000000000000000, -1.000000000000000000 ) ) ;
#12423=CARTESIAN_POINT ( 'NONE',  ( 33.95908713831673964, -3.945449517755637014, 5.783357778048663356 ) ) ;
#12425=CARTESIAN_POINT ( 'NONE',  ( 19.43845002722867221, 2.988003976273734263, 6.000000000000000000 ) ) ;
#12429=AXIS2_PLACEMENT_3D ( 'NONE', #13840, #11181, #1262 ) ;
#12430=EDGE_CURVE ( 'NONE', #9791, #2920, #2292, .T. ) ;
#12446=CARTESIAN_POINT ( 'NONE',  ( 29.62480591732145996, -4.467644809586046151, 8.283357778048662468 ) ) ;
#12451=AXIS2_PLACEMENT_3D ( 'NONE', #3128, #11255, #16833 ) ;
#12452=CIRCLE ( 'NONE', #15065, 13.00000000000000178 ) ;
#12454=CARTESIAN_POINT ( 'NONE',  ( 25.78518620311324838, -3.676302093007511651, 3.627061608673666893 ) ) ;
#12458=CARTESIAN_POINT ( 'NONE',  ( -45.00000000000000711, -16.03270077640482683, 5.537981825772250843 ) ) ;
#12461=CIRCLE ( 'NONE', #8395, 2.749999999999988454 ) ;
#12465=CARTESIAN_POINT ( 'NONE',  ( 27.84978555093622177, -3.227686124957687586, 3.283357778048666464 ) ) ;
#12467=CARTESIAN_POINT ( 'NONE',  ( 30.78070346053490880, -6.209293581256383199, 6.861505862736158257 ) ) ;
#12476=CIRCLE ( 'NONE', #1779, 2.749999999999988454 ) ;
#12478=CARTESIAN_POINT ( 'NONE',  ( 28.10549950023366961, -2.142809097641162897, 5.783357778048668685 ) ) ;
#12480=ORIENTED_EDGE ( 'NONE', *, *, #16289, .F. ) ;
#12481=CARTESIAN_POINT ( 'NONE',  ( 27.15566825608056689, -6.646038734597135011, 6.861505862736157368 ) ) ;
#12484=DIRECTION ( 'NONE',  ( 0.000000000000000000, 0.000000000000000000, -1.000000000000000000 ) ) ;
#12488=ORIENTED_EDGE ( 'NONE', *, *, #3587, .F. ) ;
#12497=ADVANCED_FACE ( 'NONE', ( #3438, #15776 ), #3350, .F. ) ;
#12502=EDGE_CURVE ( 'NONE', #8079, #15284, #11955, .T. ) ;
#12505=CARTESIAN_POINT ( 'NONE',  ( 27.71165237056504793, -5.952083095804076684, 3.627061608673662896 ) ) ;
#12506=CARTESIAN_POINT ( 'NONE',  ( 25.90934487712385348, 0.1208734971681838660, 5.783357778048663356 ) ) ;
#12511=DIRECTION ( 'NONE',  ( -1.000000000000000000, 0.000000000000000000, 0.000000000000000000 ) ) ;
#12515=LINE ( 'NONE', #16430, #642 ) ;
#12517=ADVANCED_FACE ( 'NONE', ( #12128 ), #15027, .F. ) ;
#12521=CARTESIAN_POINT ( 'NONE',  ( 26.75784435724945709, -6.993777436889428323, 7.033357778048657138 ) ) ;
#12522=CARTESIAN_POINT ( 'NONE',  ( 30.30397292480292037, -1.478191427891014431, 5.783357778048668685 ) ) ;
#12528=ORIENTED_EDGE ( 'NONE', *, *, #3564, .F. ) ;
#12541=CARTESIAN_POINT ( 'NONE',  ( -13.00000000000000178, -1.592040838891559293E-15, 12.00000000000000000 ) ) ;
#12544=CARTESIAN_POINT ( 'NONE',  ( 27.92859066579839222, -3.218191664895003967, 3.283357778048666464 ) ) ;
#12546=CARTESIAN_POINT ( 'NONE',  ( 25.99533317148741318, -3.650983533393564517, 7.939653947423664704 ) ) ;
#12547=CARTESIAN_POINT ( 'NONE',  ( -27.11285657029384666, -20.94160726625447211, 13.95434672273383114 ) ) ;
#12560=DIRECTION ( 'NONE',  ( 0.000000000000000000, 1.000000000000000000, 0.000000000000000000 ) ) ;
#12561=CARTESIAN_POINT ( 'NONE',  ( 30.13703915187255689, -4.405930820630744371, 3.627061608673664228 ) ) ;
#12562=LINE ( 'NONE', #57, #8183 ) ;
#12563=CARTESIAN_POINT ( 'NONE',  ( 32.52441275490655670, -6.636378442139655220, 5.783357778048664244 ) ) ;
#12564=CARTESIAN_POINT ( 'NONE',  ( 29.67743187657054449, -6.342216019229654833, 6.861505862736157368 ) ) ;
#12567=CARTESIAN_POINT ( 'NONE',  ( 28.14933959732260149, -3.391468297350501260, 3.627061608673666893 ) ) ;
#12568=DIRECTION ( 'NONE',  ( 0.9928203230275512992, 0.1196152422706610180, 4.006172263299093133E-17 ) ) ;
#12571=CARTESIAN_POINT ( 'NONE',  ( 27.65911562847151117, -5.958412735707574015, 7.939653947423658487 ) ) ;
#12575=( BOUNDED_CURVE ( )  B_SPLINE_CURVE ( 2, ( #12390, #17958, #5490, #17033, #3332, #3147, #12659, #14117, #5944 ),
 .UNSPECIFIED., .F., .T. ) 
 B_SPLINE_CURVE_WITH_KNOTS ( ( 3, 2, 2, 2, 3 ),
 ( 0.7115384615384615641, 0.7179487179487179516, 0.7307692307692307265, 0.7435897435897436125, 0.7500000000000000000 ),
 .UNSPECIFIED. ) 
 CURVE ( )  GEOMETRIC_REPRESENTATION_ITEM ( )  RATIONAL_B_SPLINE_CURVE ( ( 0.9330127018922194093, 0.9330127018922194093, 1.000000000000000000, 0.8660254037844387076, 1.000000000000000000, 0.8660254037844387076, 1.000000000000000000, 0.9330127018922194093, 0.9330127018922194093 ) ) 
 REPRESENTATION_ITEM ( '' )  );
#12577=LINE ( 'NONE', #16753, #276 ) ;
#12585=CARTESIAN_POINT ( 'NONE',  ( 26.92924972366625980, -7.310485091653801781, 5.783357778048669573 ) ) ;
#12592=ORIENTED_EDGE ( 'NONE', *, *, #6791, .T. ) ;
#12594=CARTESIAN_POINT ( 'NONE',  ( 27.09860475545177039, -3.518061095420291995, 7.939653947423662927 ) ) ;
#12600=DIRECTION ( 'NONE',  ( -1.000000000000000000, 0.000000000000000000, 0.000000000000000000 ) ) ;
#12607=ORIENTED_EDGE ( 'NONE', *, *, #12629, .F. ) ;
#12613=CARTESIAN_POINT ( 'NONE',  ( 33.10345976029034176, -2.594722134608779207, 8.283357778048664244 ) ) ;
#12618=EDGE_CURVE ( 'NONE', #7363, #8657, #2272, .T. ) ;
#12622=CARTESIAN_POINT ( 'NONE',  ( 6.540214080563054644, 17.14393242671841477, 16.94648454462088694 ) ) ;
#12624=EDGE_LOOP ( 'NONE', ( #344, #2579, #2428, #1405, #16295 ) ) ;
#12626=DIRECTION ( 'NONE',  ( 1.000000000000000000, 0.000000000000000000, 0.000000000000000000 ) ) ;
#12629=EDGE_CURVE ( 'NONE', #10810, #8875, #9586, .T. ) ;
#12630=CARTESIAN_POINT ( 'NONE',  ( 28.45891156537951971, -2.090033060632186412, 5.783357778048657138 ) ) ;
#12631=CARTESIAN_POINT ( 'NONE',  ( 31.91006497951310550, -2.311404624444611589, 4.705209693361167567 ) ) ;
#12634=CARTESIAN_POINT ( 'NONE',  ( 32.93832978346670615, -1.887710243310447567, 4.533357778048667797 ) ) ;
#12638=ORIENTED_EDGE ( 'NONE', *, *, #10213, .F. ) ;
#12639=CYLINDRICAL_SURFACE ( 'NONE', #14282, 2.749999999999992006 ) ;
#12644=CARTESIAN_POINT ( 'NONE',  ( 33.64386668575551198, -3.983427357176565486, 3.283357778048664244 ) ) ;
#12649=CARTESIAN_POINT ( 'NONE',  ( 31.65190802758064592, -5.477360103042387074, 3.627061608673662896 ) ) ;
#12650=VERTEX_POINT ( 'NONE', #9656 ) ;
#12653=CARTESIAN_POINT ( 'NONE',  ( 28.76238721243587193, -5.825490297734302381, 7.939653947423658487 ) ) ;
#12655=ADVANCED_FACE ( 'NONE', ( #15207 ), #2975, .F. ) ;
#12657=CARTESIAN_POINT ( 'NONE',  ( 27.02867472334902033, -6.034368414549445170, 7.939653947423658487 ) ) ;
#12659=CARTESIAN_POINT ( 'NONE',  ( 27.57216386142120257, -6.895668018177890879, 4.533357778048659803 ) ) ;
#12660=CARTESIAN_POINT ( 'NONE',  ( 28.99436501219896201, -4.543600488427916417, 8.283357778048662468 ) ) ;
#12666=DIRECTION ( 'NONE',  ( 0.000000000000000000, 0.000000000000000000, -1.000000000000000000 ) ) ;
#12673=( BOUNDED_CURVE ( )  B_SPLINE_CURVE ( 2, ( #4513, #7345, #5951, #11477, #1903, #7427, #14600, #17237, #3695 ),
 .UNSPECIFIED., .F., .T. ) 
 B_SPLINE_CURVE_WITH_KNOTS ( ( 3, 2, 2, 2, 3 ),
 ( 0.5961538461538461453, 0.6025641025641025328, 0.6153846153846154188, 0.6282051282051281937, 0.6346153846153846922 ),
 .UNSPECIFIED. ) 
 CURVE ( )  GEOMETRIC_REPRESENTATION_ITEM ( )  RATIONAL_B_SPLINE_CURVE ( ( 0.9330127018922194093, 0.9330127018922194093, 1.000000000000000000, 0.8660254037844387076, 1.000000000000000000, 0.8660254037844387076, 1.000000000000000000, 0.9330127018922187432, 0.9330127018922192983 ) ) 
 REPRESENTATION_ITEM ( '' )  );
#12675=ORIENTED_EDGE ( 'NONE', *, *, #8861, .F. ) ;
#12676=CARTESIAN_POINT ( 'NONE',  ( 29.60297508593253468, -5.724216059278466773, 3.627061608673662896 ) ) ;
#12678=CARTESIAN_POINT ( 'NONE',  ( 31.86581749455020329, -6.715726164782562790, 6.453230759126467042 ) ) ;
#12680=DIRECTION ( 'NONE',  ( -0.000000000000000000, -0.000000000000000000, -1.000000000000000000 ) ) ;
#12687=CARTESIAN_POINT ( 'NONE',  ( 2.749999999999992895, -20.49999999999999645, 13.00000000000000178 ) ) ;
#12688=VECTOR ( 'NONE', #3612, 1000.000000000000000 ) ;
#12692=FACE_OUTER_BOUND ( 'NONE', #449, .T. ) ;
#12693=CARTESIAN_POINT ( 'NONE',  ( -23.00000000000000000, -16.21813761408365195, 13.00000000000000178 ) ) ;
#12696=CARTESIAN_POINT ( 'NONE',  ( 32.06776442294927421, -4.173316554281249147, 8.283357778048662468 ) ) ;
#12702=DIRECTION ( 'NONE',  ( 0.000000000000000000, 0.000000000000000000, -1.000000000000000000 ) ) ;
#12710=CARTESIAN_POINT ( 'NONE',  ( 3.248936832696172505, -15.16081378324841289, 17.00000000000000000 ) ) ;
#12711=ORIENTED_EDGE ( 'NONE', *, *, #11811, .T. ) ;
#12716=CARTESIAN_POINT ( 'NONE',  ( 31.93198502805756789, -2.935734224299280548, 3.627061608673666893 ) ) ;
#12720=CARTESIAN_POINT ( 'NONE',  ( 26.41562710823574278, -3.600346414165641828, 3.627061608673666893 ) ) ;
#12721=CARTESIAN_POINT ( 'NONE',  ( -19.90989778724008019, -21.66613080872904717, 15.52824432210780259 ) ) ;
#12722=CARTESIAN_POINT ( 'NONE',  ( 29.11750682573587312, -2.010685337989277954, 6.453230759126474148 ) ) ;
#12723=ORIENTED_EDGE ( 'NONE', *, *, #3322, .T. ) ;
#12727=ORIENTED_EDGE ( 'NONE', *, *, #7718, .T. ) ;
#12736=EDGE_CURVE ( 'NONE', #6730, #11134, #12114, .T. ) ;
#12739=CARTESIAN_POINT ( 'NONE',  ( 30.30787278169304244, -6.266260340387784566, 6.861505862736157368 ) ) ;
#12742=EDGE_LOOP ( 'NONE', ( #8595, #14439, #9733, #1792, #11155, #5794, #16191, #3965, #4659, #15495, #2314, #1617, #3058, #1565, #14583, #1354, #4479, #9442, #8807, #3599, #13493, #204, #9032, #14746, #16028, #4174, #17305, #8040 ) ) ;
#12743=CARTESIAN_POINT ( 'NONE',  ( 29.01637427789896151, -7.048830937829683840, 5.783357778048658027 ) ) ;
#12745=CARTESIAN_POINT ( 'NONE',  ( 45.50000000000000000, -16.03270077640482683, 2.787981825772262390 ) ) ;
#12750=CARTESIAN_POINT ( 'NONE',  ( -3.248936832696171617, 7.999999999999989342, 17.00000000000000000 ) ) ;
#12759=CARTESIAN_POINT ( 'NONE',  ( 3.538288549924106796, -15.34800872113743431, 16.99955934415557479 ) ) ;
#12760=( NAMED_UNIT ( * ) SI_UNIT ( $, .STERADIAN. ) SOLID_ANGLE_UNIT ( ) );
#12762=EDGE_LOOP ( 'NONE', ( #3637, #10717, #4049, #14207 ) ) ;
#12770=CARTESIAN_POINT ( 'NONE',  ( 28.24571643650507369, -4.633797857156355171, 3.627061608673664228 ) ) ;
#12775=DIRECTION ( 'NONE',  ( 0.000000000000000000, 0.000000000000000000, 1.000000000000000000 ) ) ;
#12779=CARTESIAN_POINT ( 'NONE',  ( -1.917618200156724081E-28, -7.000000000000001776, 17.00000000000000000 ) ) ;
#12781=CARTESIAN_POINT ( 'NONE',  ( -8.876997858717690093, 16.38553564496311310, 16.83638096351226920 ) ) ;
#12789=CARTESIAN_POINT ( 'NONE',  ( 29.54600080245929306, -4.477139269648729325, 8.283357778048662468 ) ) ;
#12793=EDGE_LOOP ( 'NONE', ( #12711, #1591, #3881, #7205 ) ) ;
#12795=CARTESIAN_POINT ( 'NONE',  ( -2.016448651773435938E-27, -20.49999999999999645, 6.000000000000000000 ) ) ;
#12801=ORIENTED_EDGE ( 'NONE', *, *, #5177, .F. ) ;
#12807=DIRECTION ( 'NONE',  ( 0.000000000000000000, 0.000000000000000000, -1.000000000000000000 ) ) ;
#12811=( BOUNDED_SURFACE ( )  B_SPLINE_SURFACE ( 1, 2, ( 
 ( #16588, #4170, #6234, #15675, #4778, #3252, #10489, #14322, #1904, #13219, #10300, #4600, #17143, #530, #8956, #16050, #15767, #6146, #17424, #10218, #7513, #15854, #7606, #11846, #8789, #8872, #6045, #2176, #7428, #3427, #13036, #14500, #796, #12944, #4865, #10395, #6323, #4957, #3619, #17238, #9141, #17046, #14680, #15947, #11574, #2085, #3517, #2261, #13132, #4692, #9051, #712, #14406, #14601, #3341, #1988, #623, #7693, #12864, #451, #11755, #17326, #5952, #11478, #10122, #11672, #9803, #11151, #2602, #888, #16134, #14768, #14934, #17786, #15354, #3961, #10827, #2512, #16721, #9392, #1066, #5307, #13492, #2353, #5048, #16221, #3788, #10738, #5218, #6678, #8129, #3696, #16313, #7872, #10570, #12025, #13403, #6587, #4292, #12209, #1155, #12544, #9476, #984, #15015, #13308, #16395, #9220, #6513, #5130, #13574, #7779, #17611, #10651, #9310, #14849, #2437, #7958, #12113, #17695, #3879, #8038, #13899, #1491, #7024, #126, #5637, #6421, #11939, #17529, #15626, #577, #7295, #10261, #14001, #5724, #9897, #10077, #12814, #5818, #3301, #488, #11341, #3202, #15448, #1584, #3113, #6095, #12991, #11625, #406, #8468, #4554 ),
 ( #11241, #14274, #17190, #309, #17094, #16818, #5912, #4736, #5998, #1861, #3030, #215, #7206, #8553, #1765, #2933, #7390, #12905, #7468, #4648, #14085, #10174, #7117, #11526, #4383, #1671, #16917, #8744, #12631, #12716, #4472, #9987, #15532, #8644, #14173, #11436, #17002, #15726, #8830, #14363, #1948, #11712, #13087, #666, #2035, #3383, #17283, #6189, #4818, #7560, #15809, #8917, #14453, #3956, #4140, #6850, #17865, #15276, #12467, #5387, #15194, #9470, #13570, #15103, #142, #7045, #12561, #12376, #2507, #16556, #6766, #2776, #1151, #10904, #16738, #6672, #9556, #17943, #10823, #16391, #9644, #12204, #5655, #8297, #15010, #11167, #17781, #13916, #56, #2597, #13825, #5567, #1511, #1413, #8123, #11085, #5476, #16471, #16650, #13657, #1246, #2688, #6936, #4225, #8386, #9725, #2858, #8033, #4310, #10997, #12299, #14931, #5302, #4042, #8217, #13748, #1326, #16217, #3781, #15102, #6671, #6506, #1061, #2432, #10820, #12375, #17689, #8032, #1325, #12108, #9386, #12202, #9469, #13745, #17605, #10732, #7952, #4039, #16390, #17942, #5213, #13569, #6848, #16306, #14929, #17780, #15009, #5474, #5125, #3874, #13486, #9555, #10646 ) ),
 .UNSPECIFIED., .F., .F., .T. ) 
 B_SPLINE_SURFACE_WITH_KNOTS ( ( 2, 2 ),
 ( 3, 2, 2, 2, 2, 2, 2, 2, 2, 2, 2, 2, 2, 2, 2, 2, 2, 2, 2, 2, 2, 2, 2, 2, 2, 2, 2, 2, 2, 2, 2, 2, 2, 2, 2, 2, 2, 2, 2, 2, 2, 2, 2, 2, 2, 2, 2, 2, 2, 2, 2, 2, 2, 2, 2, 2, 2, 2, 2, 2, 2, 2, 2, 2, 2, 2, 2, 2, 2, 2, 2, 2, 2, 2, 2, 2, 3 ),
 ( 0.000000000000000000, 1.000000000000000000 ),
 ( 0.000000000000000000, 0.01282051282051282007, 0.02564102564102564014, 0.03846153846153846367, 0.05128205128205128027, 0.06410256410256409687, 0.07692307692307692735, 0.08974358974358974395, 0.1025641025641025605, 0.1153846153846153910, 0.1282051282051281937, 0.1410256410256410242, 0.1538461538461538547, 0.1666666666666666574, 0.1794871794871794879, 0.1923076923076923184, 0.2051282051282051211, 0.2179487179487179516, 0.2307692307692307820, 0.2435897435897435848, 0.2564102564102563875, 0.2692307692307692180, 0.2820512820512820484, 0.2948717948717948789, 0.3076923076923077094, 0.3205128205128205399, 0.3333333333333333148, 0.3461538461538461453, 0.3589743589743589758, 0.3717948717948718063, 0.3846153846153846367, 0.3974358974358974117, 0.4102564102564102422, 0.4230769230769230727, 0.4358974358974359031, 0.4487179487179487336, 0.4615384615384615641, 0.4743589743589743390, 0.4871794871794871695, 0.5000000000000000000, 0.5128205128205127750, 0.5256410256410256610, 0.5384615384615384359, 0.5512820512820513219, 0.5641025641025640969, 0.5769230769230768718, 0.5897435897435897578, 0.6025641025641025328, 0.6153846153846154188, 0.6282051282051281937, 0.6410256410256410797, 0.6538461538461538547, 0.6666666666666666297, 0.6794871794871795156, 0.6923076923076922906, 0.7051282051282051766, 0.7179487179487179516, 0.7307692307692307265, 0.7435897435897436125, 0.7564102564102563875, 0.7692307692307692735, 0.7820512820512820484, 0.7948717948717948234, 0.8076923076923077094, 0.8205128205128204844, 0.8333333333333333703, 0.8461538461538461453, 0.8589743589743589203, 0.8717948717948718063, 0.8846153846153845812, 0.8974358974358974672, 0.9102564102564102422, 0.9230769230769231282, 0.9358974358974359031, 0.9487179487179486781, 0.9615384615384615641, 0.9690837704703162414 ),
 .UNSPECIFIED. ) 
 GEOMETRIC_REPRESENTATION_ITEM ( )  RATIONAL_B_SPLINE_SURFACE ( (
 ( 1.000000000000000000, 0.8660254037844387076, 1.000000000000000000, 0.8660254037844387076, 1.000000000000000000, 0.8660254037844387076, 1.000000000000000000, 0.8660254037844387076, 1.000000000000000000, 0.8660254037844387076, 1.000000000000000000, 0.8660254037844387076, 1.000000000000000000, 0.8660254037844387076, 1.000000000000000000, 0.8660254037844387076, 1.000000000000000000, 0.8660254037844387076, 1.000000000000000000, 0.8660254037844387076, 1.000000000000000000, 0.8660254037844387076, 1.000000000000000000, 0.8660254037844387076, 1.000000000000000000, 0.8660254037844387076, 1.000000000000000000, 0.8660254037844387076, 1.000000000000000000, 0.8660254037844387076, 1.000000000000000000, 0.8660254037844387076, 1.000000000000000000, 0.8660254037844387076, 1.000000000000000000, 0.8660254037844387076, 1.000000000000000000, 0.8660254037844387076, 1.000000000000000000, 0.8660254037844387076, 1.000000000000000000, 0.8660254037844387076, 1.000000000000000000, 0.8660254037844387076, 1.000000000000000000, 0.8660254037844387076, 1.000000000000000000, 0.8660254037844387076, 1.000000000000000000, 0.8660254037844387076, 1.000000000000000000, 0.8660254037844387076, 1.000000000000000000, 0.8660254037844387076, 1.000000000000000000, 0.8660254037844387076, 1.000000000000000000, 0.8660254037844387076, 1.000000000000000000, 0.8660254037844387076, 1.000000000000000000, 0.8660254037844387076, 1.000000000000000000, 0.8660254037844387076, 1.000000000000000000, 0.8660254037844387076, 1.000000000000000000, 0.8660254037844387076, 1.000000000000000000, 0.8660254037844387076, 1.000000000000000000, 0.8660254037844387076, 1.000000000000000000, 0.8660254037844387076, 1.000000000000000000, 0.8660254037844387076, 1.000000000000000000, 0.8660254037844387076, 1.000000000000000000, 0.8660254037844387076, 1.000000000000000000, 0.8660254037844387076, 1.000000000000000000, 0.8660254037844387076, 1.000000000000000000, 0.8660254037844387076, 1.000000000000000000, 0.8660254037844387076, 1.000000000000000000, 0.8660254037844387076, 1.000000000000000000, 0.8660254037844387076, 1.000000000000000000, 0.8660254037844387076, 1.000000000000000000, 0.8660254037844387076, 1.000000000000000000, 0.8660254037844387076, 1.000000000000000000, 0.8660254037844387076, 1.000000000000000000, 0.8660254037844387076, 1.000000000000000000, 0.8660254037844387076, 1.000000000000000000, 0.8660254037844387076, 1.000000000000000000, 0.8660254037844387076, 1.000000000000000000, 0.8660254037844387076, 1.000000000000000000, 0.8660254037844387076, 1.000000000000000000, 0.8660254037844387076, 1.000000000000000000, 0.8660254037844387076, 1.000000000000000000, 0.8660254037844387076, 1.000000000000000000, 0.8660254037844387076, 1.000000000000000000, 0.8660254037844387076, 1.000000000000000000, 0.8660254037844387076, 1.000000000000000000, 0.8660254037844387076, 1.000000000000000000, 0.8660254037844387076, 1.000000000000000000, 0.8660254037844387076, 1.000000000000000000, 0.8660254037844387076, 1.000000000000000000, 0.8660254037844387076, 1.000000000000000000, 0.8660254037844387076, 1.000000000000000000, 0.8660254037844387076, 1.000000000000000000, 0.8660254037844387076, 1.000000000000000000, 0.8660254037844387076, 1.000000000000000000, 0.8660254037844387076, 1.000000000000000000, 0.8660254037844387076, 1.000000000000000000, 0.8660254037844387076, 1.000000000000000000, 0.8660254037844387076, 1.000000000000000000, 0.9211513820375816231, 0.9351129643698559146),
 ( 1.000000000000000000, 0.8660254037844387076, 1.000000000000000000, 0.8660254037844387076, 1.000000000000000000, 0.8660254037844387076, 1.000000000000000000, 0.8660254037844387076, 1.000000000000000000, 0.8660254037844387076, 1.000000000000000000, 0.8660254037844387076, 1.000000000000000000, 0.8660254037844387076, 1.000000000000000000, 0.8660254037844387076, 1.000000000000000000, 0.8660254037844387076, 1.000000000000000000, 0.8660254037844387076, 1.000000000000000000, 0.8660254037844387076, 1.000000000000000000, 0.8660254037844387076, 1.000000000000000000, 0.8660254037844387076, 1.000000000000000000, 0.8660254037844387076, 1.000000000000000000, 0.8660254037844387076, 1.000000000000000000, 0.8660254037844387076, 1.000000000000000000, 0.8660254037844387076, 1.000000000000000000, 0.8660254037844387076, 1.000000000000000000, 0.8660254037844387076, 1.000000000000000000, 0.8660254037844387076, 1.000000000000000000, 0.8660254037844387076, 1.000000000000000000, 0.8660254037844387076, 1.000000000000000000, 0.8660254037844387076, 1.000000000000000000, 0.8660254037844387076, 1.000000000000000000, 0.8660254037844387076, 1.000000000000000000, 0.8660254037844387076, 1.000000000000000000, 0.8660254037844387076, 1.000000000000000000, 0.8660254037844387076, 1.000000000000000000, 0.8660254037844387076, 1.000000000000000000, 0.8660254037844387076, 1.000000000000000000, 0.8660254037844387076, 1.000000000000000000, 0.8660254037844387076, 1.000000000000000000, 0.8660254037844387076, 1.000000000000000000, 0.8660254037844387076, 1.000000000000000000, 0.8660254037844387076, 1.000000000000000000, 0.8660254037844387076, 1.000000000000000000, 0.8660254037844387076, 1.000000000000000000, 0.8660254037844387076, 1.000000000000000000, 0.8660254037844387076, 1.000000000000000000, 0.8660254037844387076, 1.000000000000000000, 0.8660254037844387076, 1.000000000000000000, 0.8660254037844387076, 1.000000000000000000, 0.8660254037844387076, 1.000000000000000000, 0.8660254037844387076, 1.000000000000000000, 0.8660254037844387076, 1.000000000000000000, 0.8660254037844387076, 1.000000000000000000, 0.8660254037844387076, 1.000000000000000000, 0.8660254037844387076, 1.000000000000000000, 0.8660254037844387076, 1.000000000000000000, 0.8660254037844387076, 1.000000000000000000, 0.8660254037844387076, 1.000000000000000000, 0.8660254037844387076, 1.000000000000000000, 0.8660254037844387076, 1.000000000000000000, 0.8660254037844387076, 1.000000000000000000, 0.8660254037844387076, 1.000000000000000000, 0.8660254037844387076, 1.000000000000000000, 0.8660254037844387076, 1.000000000000000000, 0.8660254037844387076, 1.000000000000000000, 0.8660254037844387076, 1.000000000000000000, 0.8660254037844387076, 1.000000000000000000, 0.8660254037844387076, 1.000000000000000000, 0.8660254037844387076, 1.000000000000000000, 0.8660254037844387076, 1.000000000000000000, 0.8660254037844387076, 1.000000000000000000, 0.8660254037844387076, 1.000000000000000000, 0.8660254037844387076, 1.000000000000000000, 0.8660254037844387076, 1.000000000000000000, 0.8660254037844387076, 1.000000000000000000, 0.8660254037844387076, 1.000000000000000000, 0.8660254037844387076, 1.000000000000000000, 0.8660254037844387076, 1.000000000000000000, 0.8660254037844387076, 1.000000000000000000, 0.8660254037844387076, 1.000000000000000000, 0.8660254037844387076, 1.000000000000000000, 0.8660254037844387076, 1.000000000000000000, 0.9211513820375816231, 0.9351129643698559146) ) ) 
 REPRESENTATION_ITEM ( '' )  SURFACE ( )  );
#12814=CARTESIAN_POINT ( 'NONE',  ( 26.15738093914773543, -4.885401043216321959, 3.283357778048664244 ) ) ;
#12817=CARTESIAN_POINT ( 'NONE',  ( -20.83887142315839469, -22.08617648736154493, 15.35754594250728999 ) ) ;
#12822=ORIENTED_EDGE ( 'NONE', *, *, #8861, .T. ) ;
#12823=FACE_OUTER_BOUND ( 'NONE', #6790, .T. ) ;
#12824=ADVANCED_FACE ( 'NONE', ( #763, #17486 ), #16101, .T. ) ;
#12827=EDGE_LOOP ( 'NONE', ( #9313, #5341, #17918, #14261 ) ) ;
#12831=VECTOR ( 'NONE', #11494, 1000.000000000000000 ) ;
#12834=CARTESIAN_POINT ( 'NONE',  ( 33.47428445112562656, -1.485779673698265135, 5.113484796970859669 ) ) ;
#12839=CARTESIAN_POINT ( 'NONE',  ( 29.18947247604338102, -3.066280307211263434, 3.283357778048666464 ) ) ;
#12840=CARTESIAN_POINT ( 'NONE',  ( 29.76058531221316628, -5.705227139567997874, 3.627061608673662896 ) ) ;
#12842=CARTESIAN_POINT ( 'NONE',  ( 25.95642634701329499, -4.403549397486667516, 7.880302681851837576 ) ) ;
#12843=ORIENTED_EDGE ( 'NONE', *, *, #9625, .F. ) ;
#12844=CARTESIAN_POINT ( 'NONE',  ( 27.93049598394382116, -4.671775696577297410, 7.939653947423662039 ) ) ;
#12849=VERTEX_POINT ( 'NONE', #16947 ) ;
#12858=DIRECTION ( 'NONE',  ( 0.000000000000000000, 0.000000000000000000, 1.000000000000000000 ) ) ;
#12864=CARTESIAN_POINT ( 'NONE',  ( 30.61929490284659394, -6.528548903775525325, 7.033357778048657138 ) ) ;
#12865=ADVANCED_FACE ( 'NONE', ( #2142, #17388 ), #14733, .F. ) ;
#12868=EDGE_LOOP ( 'NONE', ( #15243, #8139, #13153, #4337 ) ) ;
#12869=CARTESIAN_POINT ( 'NONE',  ( 30.23341599105502908, -5.648260380436596506, 3.627061608673662896 ) ) ;
#12876=CARTESIAN_POINT ( 'NONE',  ( 29.16815758536418102, -2.004582921727632971, 5.783357778048662468 ) ) ;
#12879=EDGE_LOOP ( 'NONE', ( #11199, #10222, #16769, #14639, #2492, #6099 ) ) ;
#12883=DIRECTION ( 'NONE',  ( -1.000000000000000000, 0.000000000000000000, 0.000000000000000000 ) ) ;
#12885=EDGE_CURVE ( 'NONE', #11393, #4229, #9322, .T. ) ;
#12886=CARTESIAN_POINT ( 'NONE',  ( 28.05993251931039012, -3.202367565343739564, 8.283357778048664244 ) ) ;
#12891=VERTEX_POINT ( 'NONE', #13365 ) ;
#12900=LINE ( 'NONE', #4731, #11853 ) ;
#12905=CARTESIAN_POINT ( 'NONE',  ( 32.56242593318007295, -2.859778545457410281, 3.627061608673666893 ) ) ;
#12907=CARTESIAN_POINT ( 'NONE',  ( 32.95080301609915097, -1.548848848676412260, 5.783357778048663356 ) ) ;
#12909=CARTESIAN_POINT ( 'NONE',  ( -6.935828204433864386, -17.68137362934027479, 16.94363565911716663 ) ) ;
#12920=CARTESIAN_POINT ( 'NONE',  ( 29.30958546476020743, -4.505622649006972402, 3.283357778048664244 ) ) ;
#12921=CARTESIAN_POINT ( 'NONE',  ( 31.03886041246737548, -3.043338102658604161, 7.939653947423664704 ) ) ;
#12924=ORIENTED_EDGE ( 'NONE', *, *, #8160, .T. ) ;
#12925=CARTESIAN_POINT ( 'NONE',  ( 26.06962060539356330, -5.343074812781619443, 7.975991048337257361 ) ) ;
#12926=EDGE_LOOP ( 'NONE', ( #6381, #2481, #13519, #11923 ) ) ;
#12927=CARTESIAN_POINT ( 'NONE',  ( 26.25801688195511474, -3.619335333876111171, 3.627061608673666893 ) ) ;
#12929=DIRECTION ( 'NONE',  ( 1.000000000000000000, 0.000000000000000000, 0.000000000000000000 ) ) ;
#12937=ORIENTED_EDGE ( 'NONE', *, *, #3486, .F. ) ;
#12942=ORIENTED_EDGE ( 'NONE', *, *, #3653, .T. ) ;
#12944=CARTESIAN_POINT ( 'NONE',  ( 32.01903832059031174, -7.086814257134402162, 5.783357778048657138 ) ) ;
#12946=EDGE_LOOP ( 'NONE', ( #17589, #12727, #8558, #5851 ) ) ;
#12948=ORIENTED_EDGE ( 'NONE', *, *, #14036, .F. ) ;
#12951=CARTESIAN_POINT ( 'NONE',  ( 35.41536221060850664, -16.03270077640482683, 0.5379818257722508434 ) ) ;
#12952=EDGE_CURVE ( 'NONE', #11466, #3807, #8524, .T. ) ;
#12954=VECTOR ( 'NONE', #11711, 1000.000000000000000 ) ;
#12955=CARTESIAN_POINT ( 'NONE',  ( 28.11132641904908169, -7.168068194032743534, 5.783357778048657138 ) ) ;
#12960=CARTESIAN_POINT ( 'NONE',  ( 25.17121605730381972, -3.996982838752419553, 5.783357778048662468 ) ) ;
#12973=CARTESIAN_POINT ( 'NONE',  ( 29.23078034989804763, -4.515117109069654688, 3.283357778048664244 ) ) ;
#12979=PLANE ( 'NONE',  #11875 ) ;
#12984=CARTESIAN_POINT ( 'NONE',  ( 26.31556265977298992, -7.384422263489805793, 5.783357778048663356 ) ) ;
#12988=CARTESIAN_POINT ( 'NONE',  ( 27.16987539990068612, -2.245336462116964249, 5.113484796970861446 ) ) ;
#12990=DIRECTION ( 'NONE',  ( -0.000000000000000000, -0.000000000000000000, -1.000000000000000000 ) ) ;
#12991=CARTESIAN_POINT ( 'NONE',  ( 25.37303892199676270, -2.799178389412888546, 4.533357778048667797 ) ) ;
#12996=PLANE ( 'NONE',  #3741 ) ;
#13000=VERTEX_POINT ( 'NONE', #16837 ) ;
#13002=CARTESIAN_POINT ( 'NONE',  ( 26.01595305975170547, -2.384361315936983416, 5.783357778048657138 ) ) ;
#13005=VECTOR ( 'NONE', #16636, 1000.000000000000000 ) ;
#13013=CARTESIAN_POINT ( 'NONE',  ( 27.88665588685489993, -3.423116496867954162, 7.939653947423664704 ) ) ;
#13015=AXIS2_PLACEMENT_3D ( 'NONE', #11900, #17483, #10535 ) ;
#13018=CARTESIAN_POINT ( 'NONE',  ( 33.32855701603872234, -2.140504347050403045, 4.705209693361168455 ) ) ;
#13019=CARTESIAN_POINT ( 'NONE',  ( -23.83446850436624587, -10.01089291621719646, 14.74374009921848483 ) ) ;
#13026=DIRECTION ( 'NONE',  ( -1.000000000000000000, 0.000000000000000000, 0.000000000000000000 ) ) ;
#13029=CARTESIAN_POINT ( 'NONE',  ( 27.27683486999669427, -2.232449958253242883, 5.783357778048667797 ) ) ;
#13030=CARTESIAN_POINT ( 'NONE',  ( 3.443595183066687326, -15.28297513750540837, 16.99984776326510172 ) ) ;
#13033=CIRCLE ( 'NONE', #585, 5.000000000000000000 ) ;
#13036=CARTESIAN_POINT ( 'NONE',  ( 31.83134908525019213, -4.201799933639492224, 3.283357778048664244 ) ) ;
#13042=CARTESIAN_POINT ( 'NONE',  ( 27.12505156253147831, -7.276697974355292864, 5.783357778048658915 ) ) ;
#13045=CARTESIAN_POINT ( 'NONE',  ( -2.749999999999992895, -20.49999999999999645, 6.000000000000000000 ) ) ;
#13051=DIRECTION ( 'NONE',  ( 0.000000000000000000, 0.000000000000000000, -1.000000000000000000 ) ) ;
#13055=CARTESIAN_POINT ( 'NONE',  ( 25.71748644841968456, -2.420320648352046078, 5.783357778048663356 ) ) ;
#13056=ORIENTED_EDGE ( 'NONE', *, *, #9691, .T. ) ;
#13060=ORIENTED_EDGE ( 'NONE', *, *, #9985, .F. ) ;
#13064=CARTESIAN_POINT ( 'NONE',  ( 26.79905070906540132, -3.354278923027479209, 8.283357778048664244 ) ) ;
#13067=AXIS2_PLACEMENT_3D ( 'NONE', #11706, #3378, #1942 ) ;
#13072=EDGE_LOOP ( 'NONE', ( #4983, #13890, #15268, #5683, #12638 ) ) ;
#13080=FACE_OUTER_BOUND ( 'NONE', #15235, .T. ) ;
#13085=VECTOR ( 'NONE', #614, 1000.000000000000000 ) ;
#13087=CARTESIAN_POINT ( 'NONE',  ( 31.39792096211754924, -4.254019462947003838, 3.627061608673664228 ) ) ;
#13088=B_SPLINE_CURVE_WITH_KNOTS ( 'NONE', 3,
 ( #413, #4825, #3391, #13184, #6198, #11719 ),
 .UNSPECIFIED., .F., .F.,
 ( 4, 2, 4 ),
 ( 0.8480943072472125754, 0.9070911586903380730, 0.9660880101334634595 ),
 .UNSPECIFIED. ) ;
#13090=VERTEX_POINT ( 'NONE', #1204 ) ;
#13098=EDGE_CURVE ( 'NONE', #11309, #11700, #6817, .T. ) ;
#13099=CARTESIAN_POINT ( 'NONE',  ( 26.31556265977298992, -7.384422263489805793, 5.783357778048663356 ) ) ;
#13108=DIRECTION ( 'NONE',  ( 1.000000000000000000, 0.000000000000000000, 0.000000000000000000 ) ) ;
#13109=CARTESIAN_POINT ( 'NONE',  ( -5.499998817156067865, -20.49639288455253450, 12.00000000000000000 ) ) ;
#13110=CARTESIAN_POINT ( 'NONE',  ( 26.01127209431523113, -6.877383572197488526, 4.531664423152620635 ) ) ;
#13115=CARTESIAN_POINT ( 'NONE',  ( 32.07220196432897552, -5.426722983814484813, 7.939653947423658487 ) ) ;
#13128=( NAMED_UNIT ( * ) SI_UNIT ( $, .STERADIAN. ) SOLID_ANGLE_UNIT ( ) );
#13132=CARTESIAN_POINT ( 'NONE',  ( 30.88568772756644520, -4.315733451902305617, 8.283357778048662468 ) ) ;
#13134=EDGE_LOOP ( 'NONE', ( #9597, #4656, #13135, #11849, #4629 ) ) ;
#13135=ORIENTED_EDGE ( 'NONE', *, *, #11460, .T. ) ;
#13137=CARTESIAN_POINT ( 'NONE',  ( 27.38828526237195504, -6.917821758047558056, 7.033357778048657138 ) ) ;
#13138=FACE_OUTER_BOUND ( 'NONE', #8573, .T. ) ;
#13141=CARTESIAN_POINT ( 'NONE',  ( -19.71718888926883650, -28.93397812220196030, 15.64003640126278682 ) ) ;
#13144=LINE ( 'NONE', #14333, #17134 ) ;
#13148=CARTESIAN_POINT ( 'NONE',  ( 21.03312194624853149, -10.28219102306256971, 15.32075016948875934 ) ) ;
#13150=CIRCLE ( 'NONE', #15177, 5.500000000000000000 ) ;
#13153=ORIENTED_EDGE ( 'NONE', *, *, #3475, .T. ) ;
#13155=CARTESIAN_POINT ( 'NONE',  ( 29.14074637024071635, -5.979778010479330774, 8.283357778048658915 ) ) ;
#13170=ORIENTED_EDGE ( 'NONE', *, *, #8391, .F. ) ;
#13171=CARTESIAN_POINT ( 'NONE',  ( -36.27615609941022257, -23.17738945083361557, 12.00000000000000000 ) ) ;
#13173=CARTESIAN_POINT ( 'NONE',  ( 25.71748644841968456, -2.420320648352046078, 5.783357778048663356 ) ) ;
#13181=CYLINDRICAL_SURFACE ( 'NONE', #11833, 2.500000000000001776 ) ;
#13184=CARTESIAN_POINT ( 'NONE',  ( 26.28640587110349713, -7.142417550747740762, 4.663187713370804843 ) ) ;
#13188=CARTESIAN_POINT ( 'NONE',  ( 29.77044413525282707, -1.932019286686802895, 5.113484796970859669 ) ) ;
#13193=CARTESIAN_POINT ( 'NONE',  ( -45.50000000000000000, -19.03270077640483038, 5.537981825772250843 ) ) ;
#13198=CARTESIAN_POINT ( 'NONE',  ( 27.28266178881210280, -7.257709054644824853, 5.783357778048657138 ) ) ;
#13200=EDGE_LOOP ( 'NONE', ( #6473, #15359, #2989, #17953 ) ) ;
#13201=CARTESIAN_POINT ( 'NONE',  ( 26.19644603989336318, -6.395740563884610097, 7.560328637605171487 ) ) ;
#13203=CARTESIAN_POINT ( 'NONE',  ( 32.91278983782564183, -5.325448745358647429, 3.627061608673662896 ) ) ;
#13204=DIRECTION ( 'NONE',  ( 0.000000000000000000, 0.000000000000000000, 1.000000000000000000 ) ) ;
#13208=CARTESIAN_POINT ( 'NONE',  ( 30.37154917142620292, -2.923863409590206519, 3.283357778048666464 ) ) ;
#13209=VERTEX_POINT ( 'NONE', #2906 ) ;
#13210=DIRECTION ( 'NONE',  ( -0.9928203230275512992, -0.1196152422706610180, -4.006172263299093133E-17 ) ) ;
#13216=SHAPE_REPRESENTATION_RELATIONSHIP ( 'NONE' , 'NONE' ,  #691, #755 ) ;
#13219=CARTESIAN_POINT ( 'NONE',  ( 33.27992013083530054, -6.934902899450660740, 5.783357778048657138 ) ) ;
#13222=ORIENTED_EDGE ( 'NONE', *, *, #8234, .F. ) ;
#13223=CARTESIAN_POINT ( 'NONE',  ( 27.08121146544255353, -6.028038774645947839, 3.627061608673662896 ) ) ;
#13224=CARTESIAN_POINT ( 'NONE',  ( 33.56515079149260572, -5.873822666371450119, 4.705209693361159573 ) ) ;
#13229=CARTESIAN_POINT ( 'NONE',  ( 29.23078034989804763, -4.515117109069654688, 3.283357778048664244 ) ) ;
#13230=DIRECTION ( 'NONE',  ( -0.7866107318554605987, 0.6174492339697383869, 8.659560562354860135E-17 ) ) ;
#13234=CARTESIAN_POINT ( 'NONE',  ( 16.79147592569384173, -15.38964587861223166, 16.02981638571824163 ) ) ;
#13240=CARTESIAN_POINT ( 'NONE',  ( 33.15485366002904755, -6.560422763297783177, 5.783357778048664244 ) ) ;
#13242=ORIENTED_EDGE ( 'NONE', *, *, #8118, .F. ) ;
#13245=ORIENTED_EDGE ( 'NONE', *, *, #14935, .F. ) ;
#13249=CARTESIAN_POINT ( 'NONE',  ( 25.11802603177690330, -19.03270077640483038, 0.5379818257722508434 ) ) ;
#13251=EDGE_CURVE ( 'NONE', #3432, #4167, #16521, .T. ) ;
#13260=EDGE_CURVE ( 'NONE', #9480, #7608, #10928, .T. ) ;
#13275=DIRECTION ( 'NONE',  ( 0.9928203230275512992, 0.1196152422706610180, 4.006172263299093133E-17 ) ) ;
#13282=CARTESIAN_POINT ( 'NONE',  ( 27.17934203385504333, -30.00000000000000355, 13.93658524716016878 ) ) ;
#13284=CARTESIAN_POINT ( 'NONE',  ( 27.86926259684567597, -5.933094176093606897, 3.627061608673662896 ) ) ;
#13287=( BOUNDED_CURVE ( )  B_SPLINE_CURVE ( 2, ( #12082, #2326, #6739, #12177, #15082, #9364, #6829, #10543, #2665 ),
 .UNSPECIFIED., .F., .T. ) 
 B_SPLINE_CURVE_WITH_KNOTS ( ( 3, 2, 2, 2, 3 ),
 ( 0.2500000000000000000, 0.2564102564102563875, 0.2692307692307692180, 0.2820512820512820484, 0.2884615384615384914 ),
 .UNSPECIFIED. ) 
 CURVE ( )  GEOMETRIC_REPRESENTATION_ITEM ( )  RATIONAL_B_SPLINE_CURVE ( ( 0.9330127018922194093, 0.9330127018922195203, 1.000000000000000000, 0.8660254037844387076, 1.000000000000000000, 0.8660254037844387076, 1.000000000000000000, 0.9330127018922190762, 0.9330127018922194093 ) ) 
 REPRESENTATION_ITEM ( '' )  );
#13289=CARTESIAN_POINT ( 'NONE',  ( 33.35047706458318828, -2.764833946905071560, 3.627061608673666893 ) ) ;
#13294=AXIS2_PLACEMENT_3D ( 'NONE', #9574, #1346, #13767 ) ;
#13308=CARTESIAN_POINT ( 'NONE',  ( 28.23639288985533824, -7.542548330185622874, 5.783357778048657138 ) ) ;
#13312=ORIENTED_EDGE ( 'NONE', *, *, #16894, .T. ) ;
#13315=CARTESIAN_POINT ( 'NONE',  ( 26.99805802979993885, -6.665027654307603022, 6.861505862736158257 ) ) ;
#13318=ORIENTED_EDGE ( 'NONE', *, *, #1216, .F. ) ;
#13322=CARTESIAN_POINT ( 'NONE',  ( 29.38468146192651886, -6.677295441714964142, 4.533357778048659803 ) ) ;
#13323=LINE ( 'NONE', #3632, #1197 ) ;
#13324=VECTOR ( 'NONE', #5920, 1000.000000000000000 ) ;
#13325=DIRECTION ( 'NONE',  ( 1.000000000000000000, 0.000000000000000000, 0.000000000000000000 ) ) ;
#13329=CARTESIAN_POINT ( 'NONE',  ( 22.62608969754382215, -9.966271075498049470, 15.00374444583767897 ) ) ;
#13332=ORIENTED_EDGE ( 'NONE', *, *, #9471, .F. ) ;
#13334=CARTESIAN_POINT ( 'NONE',  ( 33.76207435632690590, -3.969185667289998332, 7.939653947423662039 ) ) ;
#13341=CARTESIAN_POINT ( 'NONE',  ( 28.21828588914510050, -7.155181690169023057, 5.113484796970857005 ) ) ;
#13342=AXIS2_PLACEMENT_3D ( 'NONE', #13812, #1051, #12186 ) ;
#13344=CYLINDRICAL_SURFACE ( 'NONE', #8702, 2.500000000000001776 ) ;
#13363=ORIENTED_EDGE ( 'NONE', *, *, #83, .T. ) ;
#13365=CARTESIAN_POINT ( 'NONE',  ( 45.00000000000000711, -19.03270077640483038, 0.5379818257722508434 ) ) ;
#13367=DIRECTION ( 'NONE',  ( 0.000000000000000000, 0.000000000000000000, -1.000000000000000000 ) ) ;
#13372=DIRECTION ( 'NONE',  ( 1.000000000000000000, 0.000000000000000000, 0.000000000000000000 ) ) ;
#13376=CARTESIAN_POINT ( 'NONE',  ( 29.46348657678868577, -6.667800981652280967, 4.533357778048659803 ) ) ;
#13377=CARTESIAN_POINT ( 'NONE',  ( 28.28502977505876359, -2.748149777785362957, 4.705209693361168455 ) ) ;
#13378=EDGE_LOOP ( 'NONE', ( #12407, #15750, #154, #14769, #15839 ) ) ;
#13379=( BOUNDED_CURVE ( )  B_SPLINE_CURVE ( 2, ( #10781, #10955, #1373, #105, #15158, #6718, #2905, #12259, #17827 ),
 .UNSPECIFIED., .F., .F. ) 
 B_SPLINE_CURVE_WITH_KNOTS ( ( 3, 2, 2, 2, 3 ),
 ( 0.3653846153846154188, 0.3717948717948718063, 0.3846153846153846367, 0.3974358974358974117, 0.4038461538461538547 ),
 .UNSPECIFIED. ) 
 CURVE ( )  GEOMETRIC_REPRESENTATION_ITEM ( )  RATIONAL_B_SPLINE_CURVE ( ( 0.9330127018922194093, 0.9330127018922196314, 1.000000000000000000, 0.8660254037844387076, 1.000000000000000000, 0.8660254037844387076, 1.000000000000000000, 0.9330127018922190762, 0.9330127018922194093 ) ) 
 REPRESENTATION_ITEM ( '' )  );
#13383=CARTESIAN_POINT ( 'NONE',  ( 31.56875459193803124, -6.114348982704044921, 6.861505862736157368 ) ) ;
#13384=CARTESIAN_POINT ( 'NONE',  ( -28.06754645621478517, -12.55420304724502323, 13.70087619851170757 ) ) ;
#13399=AXIS2_PLACEMENT_3D ( 'NONE', #17485, #10790, #2404 ) ;
#13403=CARTESIAN_POINT ( 'NONE',  ( 28.36392410707646761, -4.619556167269785796, 8.283357778048662468 ) ) ;
#13404=( BOUNDED_CURVE ( )  B_SPLINE_CURVE ( 2, ( #6583, #5300, #2505, #3954, #8216, #1147, #6765, #12297, #10996 ),
 .UNSPECIFIED., .F., .T. ) 
 B_SPLINE_CURVE_WITH_KNOTS ( ( 3, 2, 2, 2, 3 ),
 ( 0.05769230769230771633, 0.06410256410256409687, 0.07692307692307692735, 0.08974358974358974395, 0.09615384615384617306 ),
 .UNSPECIFIED. ) 
 CURVE ( )  GEOMETRIC_REPRESENTATION_ITEM ( )  RATIONAL_B_SPLINE_CURVE ( ( 0.9330127018922194093, 0.9330127018922196314, 1.000000000000000000, 0.8660254037844387076, 1.000000000000000000, 0.8660254037844387076, 1.000000000000000000, 0.9330127018922191873, 0.9330127018922194093 ) ) 
 REPRESENTATION_ITEM ( '' )  );
#13405=ORIENTED_EDGE ( 'NONE', *, *, #3743, .T. ) ;
#13406=EDGE_LOOP ( 'NONE', ( #1160, #3029, #11673, #4300 ) ) ;
#13410=CARTESIAN_POINT ( 'NONE',  ( 30.12381574833269937, -2.526612381163247267, 6.861505862736165362 ) ) ;
#13411=CARTESIAN_POINT ( 'NONE',  ( 30.82871344409320713, -3.068656662272551294, 3.627061608673666449 ) ) ;
#13412=ORIENTED_EDGE ( 'NONE', *, *, #6791, .F. ) ;
#13413=DIRECTION ( 'NONE',  ( -0.000000000000000000, -0.000000000000000000, 1.000000000000000000 ) ) ;
#13414=CARTESIAN_POINT ( 'NONE',  ( 0.000000000000000000, 0.000000000000000000, 12.00000000000000000 ) ) ;
#13420=CIRCLE ( 'NONE', #3283, 3.999999999999994671 ) ;
#13424=CARTESIAN_POINT ( 'NONE',  ( 16.91330062320331962, -14.78391025039656625, 16.01216328675237577 ) ) ;
#13426=EDGE_CURVE ( 'NONE', #4804, #4963, #7803, .T. ) ;
#13430=EDGE_LOOP ( 'NONE', ( #6262, #16228, #13682, #9495 ) ) ;
#13442=EDGE_CURVE ( 'NONE', #17902, #2263, #11693, .T. ) ;
#13450=EDGE_CURVE ( 'NONE', #7608, #9808, #10360, .T. ) ;
#13457=DIRECTION ( 'NONE',  ( -0.9928203230275512992, -0.1196152422706610180, -4.006172263299093133E-17 ) ) ;
#13459=CARTESIAN_POINT ( 'NONE',  ( 15.92260893619738837, -28.39189527176317540, 16.15082599432113142 ) ) ;
#13460=EDGE_LOOP ( 'NONE', ( #15219, #16365, #13222, #2342 ) ) ;
#13467=EDGE_CURVE ( 'NONE', #6659, #9791, #15834, .T. ) ;
#13470=VERTEX_POINT ( 'NONE', #6874 ) ;
#13473=CARTESIAN_POINT ( 'NONE',  ( 33.06225340847440464, -6.234220648470727433, 7.033357778048657138 ) ) ;
#13475=CARTESIAN_POINT ( 'NONE',  ( 29.04699097144805364, -6.418171698071525100, 6.861505862736157368 ) ) ;
#13476=CARTESIAN_POINT ( 'NONE',  ( 28.48022645605872327, -3.151730446115816875, 3.283357778048666464 ) ) ;
#13479=DIRECTION ( 'NONE',  ( 0.000000000000000000, 1.000000000000000000, 0.000000000000000000 ) ) ;
#13486=CARTESIAN_POINT ( 'NONE',  ( 25.72395281601508898, -4.937620572523835349, 3.627061608673664228 ) ) ;
#13489=CARTESIAN_POINT ( 'NONE',  ( 33.04340326765378677, -1.875050963503474222, 7.033357778048666020 ) ) ;
#13491=DIRECTION ( 'NONE',  ( -1.000000000000000000, 0.000000000000000000, 0.000000000000000000 ) ) ;
#13492=CARTESIAN_POINT ( 'NONE',  ( 29.35841309260160159, -6.680460261459264970, 7.033357778048657138 ) ) ;
#13493=ORIENTED_EDGE ( 'NONE', *, *, #12160, .T. ) ;
#13497=CARTESIAN_POINT ( 'NONE',  ( 31.25770402584614516, -1.763030703431812674, 5.783357778048668685 ) ) ;
#13498=CARTESIAN_POINT ( 'NONE',  ( 30.80679339554874119, -2.444327062417882779, 4.705209693361168455 ) ) ;
#13504=DIRECTION ( 'NONE',  ( -0.1196152422706614343, 0.9928203230275510771, 0.000000000000000000 ) ) ;
#13508=CARTESIAN_POINT ( 'NONE',  ( -17.24286622940504188, 11.12094428624988218, 15.96573730347181019 ) ) ;
#13512=( BOUNDED_CURVE ( )  B_SPLINE_CURVE ( 2, ( #6384, #13188, #5098, #14648, #766, #14817, #6292, #11813, #17391 ),
 .UNSPECIFIED., .F., .T. ) 
 B_SPLINE_CURVE_WITH_KNOTS ( ( 3, 2, 2, 2, 3 ),
 ( 0.4038461538461538547, 0.4102564102564102422, 0.4230769230769230727, 0.4358974358974359031, 0.4423076923076923461 ),
 .UNSPECIFIED. ) 
 CURVE ( )  GEOMETRIC_REPRESENTATION_ITEM ( )  RATIONAL_B_SPLINE_CURVE ( ( 0.9330127018922194093, 0.9330127018922196314, 1.000000000000000000, 0.8660254037844387076, 1.000000000000000000, 0.8660254037844387076, 1.000000000000000000, 0.9330127018922190762, 0.9330127018922194093 ) ) 
 REPRESENTATION_ITEM ( '' )  );
#13515=ORIENTED_EDGE ( 'NONE', *, *, #4448, .F. ) ;
#13516=CARTESIAN_POINT ( 'NONE',  ( 15.92260893619738837, -28.39189527176317540, 6.000000000000000000 ) ) ;
#13517=CARTESIAN_POINT ( 'NONE',  ( 26.18945719470476163, -6.341381504099093291, 3.746363773741651304 ) ) ;
#13519=ORIENTED_EDGE ( 'NONE', *, *, #7285, .T. ) ;
#13520=CARTESIAN_POINT ( 'NONE',  ( 33.27602027394517847, -2.146833986953896822, 6.861505862736165362 ) ) ;
#13523=CARTESIAN_POINT ( 'NONE',  ( 13.00000000000000178, 0.000000000000000000, 12.00000000000000000 ) ) ;
#13524=CARTESIAN_POINT ( 'NONE',  ( 26.01652455409633902, -4.902371455920926380, 5.783357778048663356 ) ) ;
#13527=AXIS2_PLACEMENT_3D ( 'NONE', #6717, #10527, #16174 ) ;
#13534=CIRCLE ( 'NONE', #12362, 6.249999999999998224 ) ;
#13537=VERTEX_POINT ( 'NONE', #9243 ) ;
#13543=VECTOR ( 'NONE', #8794, 1000.000000000000227 ) ;
#13545=CARTESIAN_POINT ( 'NONE',  ( 7.499998387031003411, -20.49508120620799900, 12.00000000000000000 ) ) ;
#13551=DIRECTION ( 'NONE',  ( -1.000000000000000000, -1.501955125927555231E-12, 0.000000000000000000 ) ) ;
#13552=CARTESIAN_POINT ( 'NONE',  ( 31.66250999073069750, -5.675955295111851484, 8.283357778048658915 ) ) ;
#13553=EDGE_CURVE ( 'NONE', #11836, #17698, #432, .T. ) ;
#13554=CARTESIAN_POINT ( 'NONE',  ( 28.49970350196817392, -5.857138497251738407, 3.627061608673662896 ) ) ;
#13556=CARTESIAN_POINT ( 'NONE',  ( 28.60033944477555323, -4.591072787911525843, 3.283357778048664244 ) ) ;
#13557=EDGE_CURVE ( 'NONE', #7755, #1473, #16497, .T. ) ;
#13560=EDGE_LOOP ( 'NONE', ( #11595, #17697, #4919, #7019, #7627, #13845 ) ) ;
#13561=LINE ( 'NONE', #5557, #9534 ) ;
#13567=CARTESIAN_POINT ( 'NONE',  ( 30.03080348965042745, -6.936809113706096319, 5.113484796970857005 ) ) ;
#13569=CARTESIAN_POINT ( 'NONE',  ( 26.49461065740898036, -7.352653653197164019, 5.783357778048658027 ) ) ;
#13570=CARTESIAN_POINT ( 'NONE',  ( 30.12381574833269937, -2.526612381163247267, 6.861505862736165362 ) ) ;
#13573=CARTESIAN_POINT ( 'NONE',  ( 32.06767520579373354, -2.292415704734142690, 4.705209693361168455 ) ) ;
#13574=CARTESIAN_POINT ( 'NONE',  ( 27.36943512155133362, -2.558652073080304845, 7.033357778048666020 ) ) ;
#13577=VECTOR ( 'NONE', #5200, 1000.000000000000227 ) ;
#13580=CARTESIAN_POINT ( 'NONE',  ( 30.86385689617752348, -5.572304701594726239, 3.627061608673662896 ) ) ;
#13582=CARTESIAN_POINT ( 'NONE',  ( 29.80442540930208750, -6.953886339277345563, 5.783357778048657138 ) ) ;
#13583=ORIENTED_EDGE ( 'NONE', *, *, #1381, .T. ) ;
#13584=CARTESIAN_POINT ( 'NONE',  ( 30.03006034954003667, -2.965006068755446478, 8.283357778048666020 ) ) ;
#13590=AXIS2_PLACEMENT_3D ( 'NONE', #5190, #5102, #14738 ) ;
#13598=EDGE_LOOP ( 'NONE', ( #2147, #7411 ) ) ;
#13601=VECTOR ( 'NONE', #4773, 1000.000000000000000 ) ;
#13604=ORIENTED_EDGE ( 'NONE', *, *, #532, .T. ) ;
#13605=CARTESIAN_POINT ( 'NONE',  ( 32.12473870642251939, -5.420393343910986594, 3.627061608673662896 ) ) ;
#13607=CIRCLE ( 'NONE', #10960, 2.000000000000001776 ) ;
#13611=CARTESIAN_POINT ( 'NONE',  ( 25.78162057792671291, -2.952641328940848631, 6.684592198966492482 ) ) ;
#13618=CARTESIAN_POINT ( 'NONE',  ( 5.500000000000000888, -20.49999999999999645, 12.00000000000000000 ) ) ;
#13619=DIRECTION ( 'NONE',  ( 0.000000000000000000, 0.000000000000000000, -1.000000000000000000 ) ) ;
#13624=AXIS2_PLACEMENT_3D ( 'NONE', #14820, #6561, #2410 ) ;
#13625=DIRECTION ( 'NONE',  ( 0.9899494936611662466, 0.1414213562373111965, 0.000000000000000000 ) ) ;
#13629=CARTESIAN_POINT ( 'NONE',  ( 26.14833026707293229, -5.996374093462649491, 3.562504011865185838 ) ) ;
#13632=FACE_OUTER_BOUND ( 'NONE', #15046, .T. ) ;
#13637=ADVANCED_FACE ( 'NONE', ( #8509 ), #9670, .T. ) ;
#13640=CARTESIAN_POINT ( 'NONE',  ( 29.97942892559193950, -4.424919740341219487, 7.939653947423662039 ) ) ;
#13641=CARTESIAN_POINT ( 'NONE',  ( 30.71189515440122975, -6.854751018602581958, 5.783357778048664244 ) ) ;
#13642=CARTESIAN_POINT ( 'NONE',  ( 23.84191717697471091, -22.42419738538529472, 14.74207411150917757 ) ) ;
#13647=EDGE_LOOP ( 'NONE', ( #1212, #2753 ) ) ;
#13648=CARTESIAN_POINT ( 'NONE',  ( -20.00000000000000000, -30.00000000000000355, 17.00000000000000000 ) ) ;
#13653=CARTESIAN_POINT ( 'NONE',  ( -2.016448651773435938E-27, -20.49999999999999645, 12.00000000000000000 ) ) ;
#13654=DIRECTION ( 'NONE',  ( -0.5999999999999999778, 0.7999999999999999334, 0.000000000000000000 ) ) ;
#13657=CARTESIAN_POINT ( 'NONE',  ( 28.10549950023366961, -2.142809097641162897, 5.783357778048668685 ) ) ;
#13662=CARTESIAN_POINT ( 'NONE',  ( 32.95662993491455950, -6.574107945067995118, 5.783357778048657138 ) ) ;
#13663=ORIENTED_EDGE ( 'NONE', *, *, #2959, .T. ) ;
#13666=ORIENTED_EDGE ( 'NONE', *, *, #10315, .T. ) ;
#13667=CARTESIAN_POINT ( 'NONE',  ( 32.64557936882268052, -2.222789665795767089, 6.861505862736165362 ) ) ;
#13670=CARTESIAN_POINT ( 'NONE',  ( 29.17398450417959310, -7.029842018119214941, 5.783357778048657138 ) ) ;
#13673=CARTESIAN_POINT ( 'NONE',  ( 35.62429925076629189, -17.76690233603958902, 0.5379818257722508434 ) ) ;
#13679=CARTESIAN_POINT ( 'NONE',  ( 31.67744797322171735, -2.039621600994187656, 4.533357778048667797 ) ) ;
#13682=ORIENTED_EDGE ( 'NONE', *, *, #8965, .F. ) ;
#13688=ORIENTED_EDGE ( 'NONE', *, *, #13782, .T. ) ;
#13689=CARTESIAN_POINT ( 'NONE',  ( 31.05948030073166066, -1.776715885202022394, 5.783357778048665132 ) ) ;
#13690=CARTESIAN_POINT ( 'NONE',  ( -20.00000000000000000, 7.999999999999996447, 12.00000000000000000 ) ) ;
#13693=EDGE_LOOP ( 'NONE', ( #11367, #14491, #14198, #7786 ) ) ;
#13694=CARTESIAN_POINT ( 'NONE',  ( 32.16857880351144416, -6.669052543620333395, 5.783357778048658915 ) ) ;
#13698=DIRECTION ( 'NONE',  ( 0.000000000000000000, 0.000000000000000000, -1.000000000000000000 ) ) ;
#13716=CARTESIAN_POINT ( 'NONE',  ( -2.016448651773435938E-27, -20.49999999999999645, 6.000000000000000000 ) ) ;
#13728=ADVANCED_FACE ( 'NONE', ( #5505 ), #12811, .F. ) ;
#13729=CARTESIAN_POINT ( 'NONE',  ( 29.77797860222238313, -3.195249460342344250, 7.939653947423664704 ) ) ;
#13730=DIRECTION ( 'NONE',  ( 0.000000000000000000, 0.000000000000000000, -1.000000000000000000 ) ) ;
#13735=DIRECTION ( 'NONE',  ( 0.3420201433256631063, 0.000000000000000000, -0.9396926207859104263 ) ) ;
#13736=EDGE_CURVE ( 'NONE', #7124, #8875, #2687, .T. ) ;
#13741=DIRECTION ( 'NONE',  ( 1.000000000000000000, 0.000000000000000000, 0.000000000000000000 ) ) ;
#13742=CARTESIAN_POINT ( 'NONE',  ( 29.71979337562451207, -1.938121702948446323, 5.783357778048662468 ) ) ;
#13745=CARTESIAN_POINT ( 'NONE',  ( 26.46816385032927599, -3.594016774262162706, 7.939653947423664704 ) ) ;
#13748=CARTESIAN_POINT ( 'NONE',  ( 27.71165237056504438, -5.952083095804076684, 3.627061608673662896 ) ) ;
#13749=EDGE_CURVE ( 'NONE', #11624, #15791, #13404, .T. ) ;
#13752=VERTEX_POINT ( 'NONE', #8122 ) ;
#13754=CARTESIAN_POINT ( 'NONE',  ( 32.34358231980129261, -4.140085944684206432, 7.939653947423662039 ) ) ;
#13757=CARTESIAN_POINT ( 'NONE',  ( 29.76058531221316272, -5.705227139567997874, 3.627061608673662896 ) ) ;
#13766=DIRECTION ( 'NONE',  ( 0.9928203230275512992, 0.1196152422706610180, 4.006172263299093133E-17 ) ) ;
#13767=DIRECTION ( 'NONE',  ( 0.9396926207859104263, 0.000000000000000000, -0.3420201433256631618 ) ) ;
#13768=CARTESIAN_POINT ( 'NONE',  ( 28.40059689994085801, -13.06564623954105464, 13.61006631438115200 ) ) ;
#13774=ORIENTED_EDGE ( 'NONE', *, *, #3022, .F. ) ;
#13776=PLANE ( 'NONE',  #6112 ) ;
#13778=ORIENTED_EDGE ( 'NONE', *, *, #14153, .T. ) ;
#13780=DIRECTION ( 'NONE',  ( -0.6000000000000001998, -0.7999999999999999334, 0.000000000000000000 ) ) ;
#13782=EDGE_CURVE ( 'NONE', #9735, #7756, #1593, .T. ) ;
#13785=CARTESIAN_POINT ( 'NONE',  ( 32.34167700165585302, -2.686501913001913433, 3.283357778048666464 ) ) ;
#13787=CARTESIAN_POINT ( 'NONE',  ( 23.00000000000000000, -16.21813761408365195, 13.00000000000000178 ) ) ;
#13803=PLANE ( 'NONE',  #7594 ) ;
#13810=CIRCLE ( 'NONE', #14404, 2.749999999999991118 ) ;
#13811=CARTESIAN_POINT ( 'NONE',  ( 26.49878054387835746, -2.963357534503999968, 6.861505862736166250 ) ) ;
#13812=CARTESIAN_POINT ( 'NONE',  ( 0.000000000000000000, 0.000000000000000000, 12.00000000000000000 ) ) ;
#13813=LINE ( 'NONE', #8557, #6916 ) ;
#13815=CARTESIAN_POINT ( 'NONE',  ( -27.17934203385504333, -30.00000000000000355, -0.000000000000000000 ) ) ;
#13822=CARTESIAN_POINT ( 'NONE',  ( 30.01512236704901682, -6.601339762873093875, 4.533357778048659803 ) ) ;
#13825=CARTESIAN_POINT ( 'NONE',  ( 28.87615734162756453, -4.557842178314484016, 3.627061608673664228 ) ) ;
#13828=CARTESIAN_POINT ( 'NONE',  ( 32.49625839967270480, -6.639770485940693412, 6.453230759126467042 ) ) ;
#13829=CARTESIAN_POINT ( 'NONE',  ( 32.70264286945147347, -5.350767304972614546, 7.939653947423658487 ) ) ;
#13833=CARTESIAN_POINT ( 'NONE',  ( 28.35948656569675919, -3.366149737736551906, 7.939653947423664704 ) ) ;
#13834=CARTESIAN_POINT ( 'NONE',  ( 26.67454832010805532, -2.305013593294074514, 6.453230759126474148 ) ) ;
#13836=CARTESIAN_POINT ( 'NONE',  ( 28.28955653359400557, -5.882457056865704637, 7.939653947423658487 ) ) ;
#13837=( BOUNDED_CURVE ( )  B_SPLINE_CURVE ( 2, ( #13742, #9721, #9384, #16553, #8381, #9467, #13822, #13567, #4037 ),
 .UNSPECIFIED., .F., .T. ) 
 B_SPLINE_CURVE_WITH_KNOTS ( ( 3, 2, 2, 2, 3 ),
 ( 0.4807692307692307820, 0.4871794871794871695, 0.5000000000000000000, 0.5128205128205127750, 0.5192307692307692735 ),
 .UNSPECIFIED. ) 
 CURVE ( )  GEOMETRIC_REPRESENTATION_ITEM ( )  RATIONAL_B_SPLINE_CURVE ( ( 0.9330127018922194093, 0.9330127018922196314, 1.000000000000000000, 0.8660254037844387076, 1.000000000000000000, 0.8660254037844387076, 1.000000000000000000, 0.9330127018922187432, 0.9330127018922192983 ) ) 
 REPRESENTATION_ITEM ( '' )  );
#13838=DIRECTION ( 'NONE',  ( 0.9928203230275510771, 0.1196152422706614205, 0.000000000000000000 ) ) ;
#13839=AXIS2_PLACEMENT_3D ( 'NONE', #14811, #16597, #843 ) ;
#13840=CARTESIAN_POINT ( 'NONE',  ( 26.01652455409633902, -4.902371455920926380, 5.783357778048663356 ) ) ;
#13841=ADVANCED_FACE ( 'NONE', ( #16930 ), #4400, .F. ) ;
#13845=ORIENTED_EDGE ( 'NONE', *, *, #7617, .F. ) ;
#13847=DIRECTION ( 'NONE',  ( 0.000000000000000000, -1.000000000000000000, 0.000000000000000000 ) ) ;
#13849=CARTESIAN_POINT ( 'NONE',  ( 26.12124691615246874, -10.79952268558355755, 14.20570119594951208 ) ) ;
#13857=VERTEX_POINT ( 'NONE', #4488 ) ;
#13859=CARTESIAN_POINT ( 'NONE',  ( 28.97253418081003673, -5.800171738120336151, 3.627061608673662896 ) ) ;
#13862=CARTESIAN_POINT ( 'NONE',  ( 30.45719375084302527, -1.849279520242854469, 6.453230759126474148 ) ) ;
#13871=CARTESIAN_POINT ( 'NONE',  ( 27.90727577511918867, -2.156494279411373061, 5.783357778048657138 ) ) ;
#13879=CARTESIAN_POINT ( 'NONE',  ( 32.33415724766913257, -1.960501102408027219, 7.033357778048666020 ) ) ;
#13881=AXIS2_PLACEMENT_3D ( 'NONE', #13414, #7882, #9229 ) ;
#13889=DIRECTION ( 'NONE',  ( 0.000000000000000000, 1.000000000000000000, 0.000000000000000000 ) ) ;
#13890=ORIENTED_EDGE ( 'NONE', *, *, #9412, .T. ) ;
#13892=DIRECTION ( 'NONE',  ( -0.000000000000000000, -0.000000000000000000, 1.000000000000000000 ) ) ;
#13899=CARTESIAN_POINT ( 'NONE',  ( 26.73899421642883567, -2.634607751922174224, 7.033357778048666020 ) ) ;
#13902=CARTESIAN_POINT ( 'NONE',  ( 27.88665588685489993, -3.423116496867954162, 7.939653947423664704 ) ) ;
#13903=CARTESIAN_POINT ( 'NONE',  ( -21.62109127008995557, -22.31747812791595464, 15.20678566061929615 ) ) ;
#13904=DIRECTION ( 'NONE',  ( 0.000000000000000000, 0.000000000000000000, -1.000000000000000000 ) ) ;
#13907=DIRECTION ( 'NONE',  ( 0.9899494936611662466, 0.1414213562373111965, 0.000000000000000000 ) ) ;
#13909=CARTESIAN_POINT ( 'NONE',  ( -21.42601376483257880, 2.765314980223223529, 6.000000000000000000 ) ) ;
#13912=DIRECTION ( 'NONE',  ( 0.9928203230275512992, 0.1196152422706610180, 4.006172263299093133E-17 ) ) ;
#13916=CARTESIAN_POINT ( 'NONE',  ( 28.73594040535616756, -2.066853418799292630, 5.783357778048668685 ) ) ;
#13917=VECTOR ( 'NONE', #7360, 1000.000000000000000 ) ;
#13918=CARTESIAN_POINT ( 'NONE',  ( -15.92260893619738837, -28.39189527176317540, 6.000000000000000000 ) ) ;
#13920=CARTESIAN_POINT ( 'NONE',  ( 28.93739072872572393, -3.296523698798161650, 3.627061608673666893 ) ) ;
#13922=ORIENTED_EDGE ( 'NONE', *, *, #11694, .T. ) ;
#13925=ORIENTED_EDGE ( 'NONE', *, *, #12952, .T. ) ;
#13926=CARTESIAN_POINT ( 'NONE',  ( 30.27725608814395031, -6.896919580145944195, 5.783357778048658027 ) ) ;
#13932=DIRECTION ( 'NONE',  ( -0.000000000000000000, -0.000000000000000000, 1.000000000000000000 ) ) ;
#13953=CARTESIAN_POINT ( 'NONE',  ( 27.50150540219088313, -5.977401655418041138, 7.939653947423658487 ) ) ;
#13954=EDGE_CURVE ( 'NONE', #9735, #14980, #3591, .T. ) ;
#13963=DIRECTION ( 'NONE',  ( -0.6000000000000000888, 0.7999999999999999334, 0.000000000000000000 ) ) ;
#13967=ADVANCED_FACE ( 'NONE', ( #3316 ), #502, .T. ) ;
#13976=CARTESIAN_POINT ( 'NONE',  ( 33.13353876934984754, -5.498725377814142945, 3.283357778048663800 ) ) ;
#13982=ORIENTED_EDGE ( 'NONE', *, *, #5609, .F. ) ;
#13987=ORIENTED_EDGE ( 'NONE', *, *, #10576, .T. ) ;
#13993=( BOUNDED_CURVE ( )  B_SPLINE_CURVE ( 2, ( #9319, #17437, #10497, #996, #16324, #803, #12127, #17707, #5227 ),
 .UNSPECIFIED., .F., .T. ) 
 B_SPLINE_CURVE_WITH_KNOTS ( ( 3, 2, 2, 2, 3 ),
 ( 0.1346153846153846367, 0.1410256410256410242, 0.1538461538461538547, 0.1666666666666666574, 0.1730769230769231004 ),
 .UNSPECIFIED. ) 
 CURVE ( )  GEOMETRIC_REPRESENTATION_ITEM ( )  RATIONAL_B_SPLINE_CURVE ( ( 0.9330127018922194093, 0.9330127018922196314, 1.000000000000000000, 0.8660254037844387076, 1.000000000000000000, 0.8660254037844387076, 1.000000000000000000, 0.9330127018922190762, 0.9330127018922194093 ) ) 
 REPRESENTATION_ITEM ( '' )  );
#13994=ORIENTED_EDGE ( 'NONE', *, *, #7842, .F. ) ;
#13996=CARTESIAN_POINT ( 'NONE',  ( 31.78252145740879797, -2.026962321187214311, 7.033357778048666020 ) ) ;
#14000=VERTEX_POINT ( 'NONE', #1879 ) ;
#14001=CARTESIAN_POINT ( 'NONE',  ( 26.10855331130634127, -2.710563430764044490, 7.033357778048666020 ) ) ;
#14002=CIRCLE ( 'NONE', #16343, 2.749999999999995559 ) ;
#14003=CARTESIAN_POINT ( 'NONE',  ( 27.89118264539014547, -6.557423775948280742, 4.705209693361159573 ) ) ;
#14004=CARTESIAN_POINT ( 'NONE',  ( -20.27016866188220945, -21.85533094420792466, 15.46350303853101593 ) ) ;
#14009=CYLINDRICAL_SURFACE ( 'NONE', #8107, 2.500000000000001776 ) ;
#14012=DIRECTION ( 'NONE',  ( -0.1196152422706620172, 0.9928203230275510771, 0.000000000000000000 ) ) ;
#14022=CARTESIAN_POINT ( 'NONE',  ( 31.67382807612511542, -6.101689702897060030, 4.705209693361159573 ) ) ;
#14025=CARTESIAN_POINT ( 'NONE',  ( 29.60297508593253468, -5.724216059278466773, 3.627061608673662896 ) ) ;
#14028=CARTESIAN_POINT ( 'NONE',  ( 26.39823381822652593, -6.110324093391315436, 7.939653947423658487 ) ) ;
#14030=CARTESIAN_POINT ( 'NONE',  ( 26.92924972366625980, -7.310485091653801781, 5.783357778048669573 ) ) ;
#14031=VERTEX_POINT ( 'NONE', #3399 ) ;
#14032=CARTESIAN_POINT ( 'NONE',  ( 29.21955148510287614, -5.970283550416647600, 8.283357778048660691 ) ) ;
#14036=EDGE_CURVE ( 'NONE', #15379, #6312, #5459, .T. ) ;
#14037=CARTESIAN_POINT ( 'NONE',  ( -3.443595183066686438, -15.28297513750540837, 16.99984776326509106 ) ) ;
#14048=CARTESIAN_POINT ( 'NONE',  ( 28.25893984004492765, -6.513116296623863377, 6.861505862736158257 ) ) ;
#14062=ADVANCED_FACE ( 'NONE', ( #5021, #16195 ), #6487, .T. ) ;
#14063=DIRECTION ( 'NONE',  ( -0.1196152422706618645, 0.9928203230275510771, 0.000000000000000000 ) ) ;
#14064=LINE ( 'NONE', #4623, #14133 ) ;
#14065=EDGE_CURVE ( 'NONE', #6631, #15247, #13287, .T. ) ;
#14066=( BOUNDED_CURVE ( )  B_SPLINE_CURVE ( 2, ( #4521, #5960, #10037 ),
 .UNSPECIFIED., .F., .T. ) 
 B_SPLINE_CURVE_WITH_KNOTS ( ( 3, 3 ),
 ( 0.000000000000000000, 1.000000000000000000 ),
 .UNSPECIFIED. ) 
 CURVE ( )  GEOMETRIC_REPRESENTATION_ITEM ( )  RATIONAL_B_SPLINE_CURVE ( ( 0.9436786787937823107, 0.9410169847269389543, 0.9390195162974519505 ) ) 
 REPRESENTATION_ITEM ( '' )  );
#14068=CARTESIAN_POINT ( 'NONE',  ( 30.67935139548315604, -7.248220074880824981, 5.783357778048657138 ) ) ;
#14071=CARTESIAN_POINT ( 'NONE',  ( 26.01652455409633902, -4.902371455920926380, 5.783357778048663356 ) ) ;
#14073=VERTEX_POINT ( 'NONE', #17496 ) ;
#14085=CARTESIAN_POINT ( 'NONE',  ( 32.77709966008947617, -5.968767264923789284, 4.705209693361160461 ) ) ;
#14086=ADVANCED_FACE ( 'NONE', ( #12002, #3760 ), #1222, .T. ) ;
#14087=CARTESIAN_POINT ( 'NONE',  ( 27.15566825608056689, -6.646038734597135011, 6.861505862736157368 ) ) ;
#14088=CARTESIAN_POINT ( 'NONE',  ( -18.31859240410168255, -20.37927276054855596, 15.79761704335050077 ) ) ;
#14089=CARTESIAN_POINT ( 'NONE',  ( 29.91004888286193619, -6.613999042680076990, 7.033357778048657138 ) ) ;
#14092=CARTESIAN_POINT ( 'NONE',  ( 31.24221605398236079, -5.726592414339752857, 3.283357778048663356 ) ) ;
#14094=CARTESIAN_POINT ( 'NONE',  ( 26.66770885555339987, -3.370103022578743612, 3.283357778048666464 ) ) ;
#14095=ORIENTED_EDGE ( 'NONE', *, *, #13450, .T. ) ;
#14099=CARTESIAN_POINT ( 'NONE',  ( 28.13948077428293715, -7.164676150231702678, 5.113484796970851676 ) ) ;
#14106=CARTESIAN_POINT ( 'NONE',  ( 29.80442540930208750, -6.953886339277345563, 5.783357778048657138 ) ) ;
#14110=ORIENTED_EDGE ( 'NONE', *, *, #83, .F. ) ;
#14111=CARTESIAN_POINT ( 'NONE',  ( 28.98992747081925359, -3.290194058894681639, 7.939653947423664704 ) ) ;
#14112=CARTESIAN_POINT ( 'NONE',  ( -45.00000000000000711, -19.03270077640483038, 0.5379818257722508434 ) ) ;
#14115=CARTESIAN_POINT ( 'NONE',  ( 27.14244485254070938, -4.766720295129625029, 3.627061608673664228 ) ) ;
#14116=DIRECTION ( 'NONE',  ( 0.000000000000000000, 1.000000000000000000, 0.000000000000000000 ) ) ;
#14117=CARTESIAN_POINT ( 'NONE',  ( 27.58784498402260610, -7.231137369010889770, 5.113484796970851676 ) ) ;
#14119=CARTESIAN_POINT ( 'NONE',  ( -1.917618200156724081E-28, -7.000000000000001776, 12.00000000000000000 ) ) ;
#14120=VERTEX_POINT ( 'NONE', #2487 ) ;
#14122=AXIS2_PLACEMENT_3D ( 'NONE', #6452, #17554, #7900 ) ;
#14124=CARTESIAN_POINT ( 'NONE',  ( 25.71748644841968456, -2.420320648352046078, 5.783357778048663356 ) ) ;
#14126=FACE_OUTER_BOUND ( 'NONE', #10263, .T. ) ;
#14129=EDGE_LOOP ( 'NONE', ( #11696, #15564, #14813, #1102 ) ) ;
#14132=CARTESIAN_POINT ( 'NONE',  ( 29.19137779418881351, -4.519864338893556877, 7.939653947423662039 ) ) ;
#14133=VECTOR ( 'NONE', #1649, 1000.000000000000000 ) ;
#14136=CARTESIAN_POINT ( 'NONE',  ( 33.68326924318660076, -3.978680127145231893, 8.283357778048662468 ) ) ;
#14141=DIRECTION ( 'NONE',  ( -0.000000000000000000, -0.000000000000000000, -1.000000000000000000 ) ) ;
#14143=DIRECTION ( 'NONE',  ( -0.1196152422706610735, 0.9928203230275511881, 0.000000000000000000 ) ) ;
#14144=EDGE_LOOP ( 'NONE', ( #15288, #17812, #16566, #11674 ) ) ;
#14147=CARTESIAN_POINT ( 'NONE',  ( 5.237433445017501299, -16.51494876461869410, 16.99438405180048761 ) ) ;
#14150=CARTESIAN_POINT ( 'NONE',  ( 29.95125523467787687, -2.974500528818130096, 8.283357778048664244 ) ) ;
#14153=EDGE_CURVE ( 'NONE', #15480, #6423, #6080, .T. ) ;
#14156=AXIS2_PLACEMENT_3D ( 'NONE', #12094, #16543, #3772 ) ;
#14163=( BOUNDED_CURVE ( )  B_SPLINE_CURVE ( 2, ( #14576, #7319, #14296, #12839, #12920, #4669, #13376, #9118, #10548 ),
 .UNSPECIFIED., .F., .T. ) 
 B_SPLINE_CURVE_WITH_KNOTS ( ( 3, 2, 2, 2, 3 ),
 ( 0.4807692307692307820, 0.4871794871794871695, 0.5000000000000000000, 0.5128205128205127750, 0.5192307692307692735 ),
 .UNSPECIFIED. ) 
 CURVE ( )  GEOMETRIC_REPRESENTATION_ITEM ( )  RATIONAL_B_SPLINE_CURVE ( ( 0.9330127018922194093, 0.9330127018922196314, 1.000000000000000000, 0.8660254037844387076, 1.000000000000000000, 0.8660254037844387076, 1.000000000000000000, 0.9330127018922187432, 0.9330127018922192983 ) ) 
 REPRESENTATION_ITEM ( '' )  );
#14167=CARTESIAN_POINT ( 'NONE',  ( 29.26075783691881682, -2.330785036554694489, 7.033357778048666020 ) ) ;
#14168=CARTESIAN_POINT ( 'NONE',  ( 27.48088551392658729, -7.244023872874614689, 5.783357778048669573 ) ) ;
#14169=EDGE_LOOP ( 'NONE', ( #8367, #6836, #6105, #5807 ) ) ;
#14171=CARTESIAN_POINT ( 'NONE',  ( -20.00000000000000355, 7.999999999999996447, 6.000000000000000000 ) ) ;
#14173=CARTESIAN_POINT ( 'NONE',  ( 32.04158527077989760, -6.057382223572642665, 6.861505862736158257 ) ) ;
#14178=CARTESIAN_POINT ( 'NONE',  ( -16.75000000000000000, -16.63059030033399921, 16.03574476417184869 ) ) ;
#14183=CARTESIAN_POINT ( 'NONE',  ( 26.01652455409633902, -4.902371455920926380, 5.783357778048663356 ) ) ;
#14194=LINE ( 'NONE', #1513, #9050 ) ;
#14196=CARTESIAN_POINT ( 'NONE',  ( 29.03376756790819613, -4.538853258604016006, 3.627061608673664228 ) ) ;
#14197=ADVANCED_FACE ( 'NONE', ( #4113 ), #12354, .T. ) ;
#14198=ORIENTED_EDGE ( 'NONE', *, *, #7265, .F. ) ;
#14199=CARTESIAN_POINT ( 'NONE',  ( 26.31376129264123165, -7.369470708288995198, 5.576845458699811076 ) ) ;
#14201=CARTESIAN_POINT ( 'NONE',  ( 28.75786045390062995, -2.691183018653962034, 4.705209693361167567 ) ) ;
#14206=CARTESIAN_POINT ( 'NONE',  ( 26.39370705969127684, -2.976016814310973313, 4.705209693361168455 ) ) ;
#14207=ORIENTED_EDGE ( 'NONE', *, *, #10576, .F. ) ;
#14220=ORIENTED_EDGE ( 'NONE', *, *, #9883, .F. ) ;
#14221=CIRCLE ( 'NONE', #10708, 2.749999999999991118 ) ;
#14230=AXIS2_PLACEMENT_3D ( 'NONE', #16408, #6784, #13504 ) ;
#14232=CARTESIAN_POINT ( 'NONE',  ( 27.60205212784272177, -2.830435096530727446, 6.861505862736165362 ) ) ;
#14242=CARTESIAN_POINT ( 'NONE',  ( -12.26589791205140045, 14.78806204439702121, 16.57179146834700845 ) ) ;
#14243=EDGE_CURVE ( 'NONE', #8961, #1004, #15241, .T. ) ;
#14250=DIRECTION ( 'NONE',  ( -0.000000000000000000, -0.000000000000000000, 1.000000000000000000 ) ) ;
#14251=CARTESIAN_POINT ( 'NONE',  ( 28.28511899221430070, -4.629050627332469858, 8.283357778048662468 ) ) ;
#14252=CARTESIAN_POINT ( 'NONE',  ( 29.74110826630370497, -2.999819088432076786, 3.283357778048666464 ) ) ;
#14261=ORIENTED_EDGE ( 'NONE', *, *, #6372, .F. ) ;
#14268=DIRECTION ( 'NONE',  ( -0.1196152422706610735, 0.9928203230275511881, 0.000000000000000000 ) ) ;
#14269=VECTOR ( 'NONE', #15373, 1000.000000000000000 ) ;
#14274=CARTESIAN_POINT ( 'NONE',  ( 33.40301380667672504, -2.758504307001591549, 7.939653947423664704 ) ) ;
#14275=EDGE_LOOP ( 'NONE', ( #4434, #6047, #14751, #6065, #17220 ) ) ;
#14278=CARTESIAN_POINT ( 'NONE',  ( 31.31418170428987224, -6.782187383561751659, 6.453230759126467042 ) ) ;
#14279=CARTESIAN_POINT ( 'NONE',  ( -28.39989834181360706, -19.37183319909320645, 13.61025820885934223 ) ) ;
#14281=VERTEX_POINT ( 'NONE', #7199 ) ;
#14282=AXIS2_PLACEMENT_3D ( 'NONE', #228, #9190, #14567 ) ;
#14286=LINE ( 'NONE', #13099, #7863 ) ;
#14293=CARTESIAN_POINT ( 'NONE',  ( -2.016448651773435938E-27, -20.49999999999999645, 12.00000000000000000 ) ) ;
#14296=CARTESIAN_POINT ( 'NONE',  ( 29.15568435273173264, -2.343444316361667834, 4.533357778048667797 ) ) ;
#14299=CARTESIAN_POINT ( 'NONE',  ( 30.15443244188179150, -1.895953141405084086, 5.783357778048668685 ) ) ;
#14300=EDGE_CURVE ( 'NONE', #3035, #11992, #8094, .T. ) ;
#14302=CARTESIAN_POINT ( 'NONE',  ( 26.23123039439649418, -6.684454722870805554, 7.310947845559079283 ) ) ;
#14304=EDGE_CURVE ( 'NONE', #2542, #15022, #1741, .T. ) ;
#14305=CARTESIAN_POINT ( 'NONE',  ( 26.66961417369883591, -4.823687054261037055, 7.939653947423662039 ) ) ;
#14308=EDGE_LOOP ( 'NONE', ( #5646, #15731, #12843, #7721 ) ) ;
#14309=DIRECTION ( 'NONE',  ( 0.000000000000000000, 0.000000000000000000, -1.000000000000000000 ) ) ;
#14317=( LENGTH_UNIT ( ) NAMED_UNIT ( * ) SI_UNIT ( .MILLI., .METRE. ) );
#14321=CARTESIAN_POINT ( 'NONE',  ( 23.47400307746859482, -29.47066586337335892, 14.90105725137469506 ) ) ;
#14322=CARTESIAN_POINT ( 'NONE',  ( 33.21234388421201089, -5.489230917751459771, 3.283357778048663800 ) ) ;
#14323=ORIENTED_EDGE ( 'NONE', *, *, #14935, .T. ) ;
#14324=ORIENTED_EDGE ( 'NONE', *, *, #14387, .F. ) ;
#14328=CARTESIAN_POINT ( 'NONE',  ( 32.67619606237177265, -1.592130426037604352, 5.783357778048668685 ) ) ;
#14333=CARTESIAN_POINT ( 'NONE',  ( 33.48062616923409962, 0.02583177435455490112, 5.783357778048664244 ) ) ;
#14344=CARTESIAN_POINT ( 'NONE',  ( 28.55151181693415907, -2.416235175459247486, 7.033357778048666020 ) ) ;
#14352=FACE_OUTER_BOUND ( 'NONE', #2515, .T. ) ;
#14361=CARTESIAN_POINT ( 'NONE',  ( -34.91600907648203389, -11.88801210197604341, 12.00000000000000000 ) ) ;
#14363=CARTESIAN_POINT ( 'NONE',  ( 31.25770402584614516, -1.763030703431812674, 5.783357778048668685 ) ) ;
#14368=CARTESIAN_POINT ( 'NONE',  ( 29.25000000000000000, -16.21813761408365195, 13.00000000000000178 ) ) ;
#14371=CARTESIAN_POINT ( 'NONE',  ( 25.74999999999998934, -16.21813761408365195, 13.00000000000000355 ) ) ;
#14373=DIRECTION ( 'NONE',  ( -0.1196152422706610735, 0.9928203230275511881, 0.000000000000000000 ) ) ;
#14374=CARTESIAN_POINT ( 'NONE',  ( 15.92260893619738837, -28.39189527176317540, 6.000000000000000000 ) ) ;
#14375=CARTESIAN_POINT ( 'NONE',  ( -35.77680296528374271, -19.03270077640482683, 10.53798182577225084 ) ) ;
#14377=B_SPLINE_CURVE_WITH_KNOTS ( 'NONE', 3,
 ( #8093, #3662, #13629, #11902, #7831, #8003, #945, #10700, #16100, #9103, #16187, #1215, #2568, #6729, #1035, #16007, #12074, #2315 ),
 .UNSPECIFIED., .F., .F.,
 ( 4, 2, 2, 2, 2, 2, 2, 2, 4 ),
 ( 0.000000000000000000, 0.0005705796246920900351, 0.001141159249384180070, 0.001711738874076270322, 0.002282318498768360140, 0.002852898123460450176, 0.003423477748152541078, 0.003994057372844632414, 0.004564636997536723750 ),
 .UNSPECIFIED. ) ;
#14384=CARTESIAN_POINT ( 'NONE',  ( 33.48996557372703364, -1.821249024531260696, 4.533357778048667797 ) ) ;
#14385=EDGE_LOOP ( 'NONE', ( #2105, #88, #1047, #15652, #8392, #15531 ) ) ;
#14387=EDGE_CURVE ( 'NONE', #8190, #15002, #12900, .T. ) ;
#14388=ORIENTED_EDGE ( 'NONE', *, *, #9016, .F. ) ;
#14389=CARTESIAN_POINT ( 'NONE',  ( 25.83772294520678159, -3.669972453104032084, 7.939653947423664704 ) ) ;
#14393=DIRECTION ( 'NONE',  ( 0.000000000000000000, 1.000000000000000000, 0.000000000000000000 ) ) ;
#14396=EDGE_CURVE ( 'NONE', #13000, #2940, #3470, .T. ) ;
#14399=CARTESIAN_POINT ( 'NONE',  ( 27.69265652961275848, -20.36619546179435503, 13.80192434669152490 ) ) ;
#14404=AXIS2_PLACEMENT_3D ( 'NONE', #13193, #17583, #3761 ) ;
#14406=CARTESIAN_POINT ( 'NONE',  ( 30.41656616297672500, -2.191532958677927745, 4.533357778048667797 ) ) ;
#14407=VERTEX_POINT ( 'NONE', #14448 ) ;
#14412=CARTESIAN_POINT ( 'NONE',  ( 26.46816385032927599, -3.594016774262162262, 7.939653947423662927 ) ) ;
#14414=( NAMED_UNIT ( * ) SI_UNIT ( $, .STERADIAN. ) SOLID_ANGLE_UNIT ( ) );
#14422=FACE_OUTER_BOUND ( 'NONE', #412, .T. ) ;
#14428=VERTEX_POINT ( 'NONE', #17375 ) ;
#14430=CARTESIAN_POINT ( 'NONE',  ( 28.15758777499317489, -7.552042790248305160, 5.783357778048657138 ) ) ;
#14432=ORIENTED_EDGE ( 'NONE', *, *, #2742, .F. ) ;
#14439=ORIENTED_EDGE ( 'NONE', *, *, #4462, .F. ) ;
#14440=( BOUNDED_CURVE ( )  B_SPLINE_CURVE ( 3, ( #6036, #17133, #1709, #7337 ),
 .UNSPECIFIED., .F., .T. ) 
 B_SPLINE_CURVE_WITH_KNOTS ( ( 4, 4 ),
 ( 0.000000000000000000, 3.141592653589793116 ),
 .UNSPECIFIED. ) 
 CURVE ( )  GEOMETRIC_REPRESENTATION_ITEM ( )  RATIONAL_B_SPLINE_CURVE ( ( 1.000000000000000000, 0.3333333333333333703, 0.3333333333333333703, 1.000000000000000000 ) ) 
 REPRESENTATION_ITEM ( '' )  );
#14441=AXIS2_PLACEMENT_3D ( 'NONE', #457, #9855, #7255 ) ;
#14443=AXIS2_PLACEMENT_3D ( 'NONE', #7270, #16048, #12883 ) ;
#14448=CARTESIAN_POINT ( 'NONE',  ( 45.50000000000000000, -19.03270077640483038, 2.787981825772258837 ) ) ;
#14453=CARTESIAN_POINT ( 'NONE',  ( 30.64918316926811315, -2.463315982128351678, 4.705209693361167567 ) ) ;
#14455=EDGE_CURVE ( 'NONE', #5885, #16382, #15619, .T. ) ;
#14459=LINE ( 'NONE', #14559, #17126 ) ;
#14461=VERTEX_POINT ( 'NONE', #7822 ) ;
#14463=VECTOR ( 'NONE', #7577, 1000.000000000000227 ) ;
#14466=FACE_OUTER_BOUND ( 'NONE', #14385, .T. ) ;
#14468=EDGE_CURVE ( 'NONE', #13537, #3035, #5001, .T. ) ;
#14470=CARTESIAN_POINT ( 'NONE',  ( 33.95908713831673964, -3.945449517755637014, 5.783357778048663356 ) ) ;
#14476=CARTESIAN_POINT ( 'NONE',  ( 28.28955653359400557, -5.882457056865704637, 7.939653947423658487 ) ) ;
#14477=VECTOR ( 'NONE', #7425, 1000.000000000000227 ) ;
#14482=CARTESIAN_POINT ( 'NONE',  ( 32.18597209352066812, -4.159074864394664672, 3.627061608673664228 ) ) ;
#14483=CARTESIAN_POINT ( 'NONE',  ( 27.95866967485789090, -6.122194908100387245, 8.283357778048660691 ) ) ;
#14487=CARTESIAN_POINT ( 'NONE',  ( 30.32207992551315812, -1.865558067907615802, 5.113484796970859669 ) ) ;
#14491=ORIENTED_EDGE ( 'NONE', *, *, #13442, .T. ) ;
#14493=CARTESIAN_POINT ( 'NONE',  ( 50.00000000000000000, -16.03270077640482683, 5.537981825772250843 ) ) ;
#14496=ORIENTED_EDGE ( 'NONE', *, *, #3384, .F. ) ;
#14500=CARTESIAN_POINT ( 'NONE',  ( 31.95146207396702565, -5.641142275435198528, 3.283357778048663800 ) ) ;
#14501=VECTOR ( 'NONE', #17286, 1000.000000000000114 ) ;
#14504=ORIENTED_EDGE ( 'NONE', *, *, #8896, .F. ) ;
#14506=CARTESIAN_POINT ( 'NONE',  ( -3.538288549924106796, -15.34800872113743431, 16.99955934415556769 ) ) ;
#14509=CIRCLE ( 'NONE', #7833, 25.00000000000000000 ) ;
#14515=CARTESIAN_POINT ( 'NONE',  ( 45.00000000000000711, 0.000000000000000000, 5.537981825772250843 ) ) ;
#14518=CARTESIAN_POINT ( 'NONE',  ( 17.93919565825226670, -12.54482367096064621, 15.85739159820981747 ) ) ;
#14525=ORIENTED_EDGE ( 'NONE', *, *, #549, .T. ) ;
#14526=CARTESIAN_POINT ( 'NONE',  ( 25.90899358965569022, -2.397247819800704782, 5.113484796970861446 ) ) ;
#14528=CARTESIAN_POINT ( 'NONE',  ( 28.64916707261694384, -6.765910400363817523, 7.033357778048657138 ) ) ;
#14529=EDGE_CURVE ( 'NONE', #3522, #4898, #7164, .T. ) ;
#14532=AXIS2_PLACEMENT_3D ( 'NONE', #8424, #12775, #12600 ) ;
#14535=ORIENTED_EDGE ( 'NONE', *, *, #6253, .F. ) ;
#14553=AXIS2_PLACEMENT_3D ( 'NONE', #9617, #15172, #2752 ) ;
#14557=VERTEX_POINT ( 'NONE', #5086 ) ;
#14559=CARTESIAN_POINT ( 'NONE',  ( 25.11802603177690330, -16.03270077640482683, 0.5379818257722508434 ) ) ;
#14561=ORIENTED_EDGE ( 'NONE', *, *, #16719, .F. ) ;
#14567=DIRECTION ( 'NONE',  ( 0.000000000000000000, 0.000000000000000000, -1.000000000000000000 ) ) ;
#14576=CARTESIAN_POINT ( 'NONE',  ( 29.16815758536418102, -2.004582921727632971, 5.783357778048662468 ) ) ;
#14577=CARTESIAN_POINT ( 'NONE',  ( 25.88156304229571703, -4.918631652813365562, 3.627061608673664228 ) ) ;
#14581=CARTESIAN_POINT ( 'NONE',  ( 26.13631296615020361, -5.896629108145334364, 7.834650323883576739 ) ) ;
#14582=( BOUNDED_CURVE ( )  B_SPLINE_CURVE ( 2, ( #14735, #11997, #2048, #9108, #4831, #8925, #9017, #678, #16012 ),
 .UNSPECIFIED., .F., .T. ) 
 B_SPLINE_CURVE_WITH_KNOTS ( ( 3, 2, 2, 2, 3 ),
 ( 0.09615384615384617306, 0.1025641025641025605, 0.1153846153846153910, 0.1282051282051281937, 0.1346153846153846367 ),
 .UNSPECIFIED. ) 
 CURVE ( )  GEOMETRIC_REPRESENTATION_ITEM ( )  RATIONAL_B_SPLINE_CURVE ( ( 0.9330127018922194093, 0.9330127018922196314, 1.000000000000000000, 0.8660254037844387076, 1.000000000000000000, 0.8660254037844387076, 1.000000000000000000, 0.9330127018922190762, 0.9330127018922194093 ) ) 
 REPRESENTATION_ITEM ( '' )  );
#14583=ORIENTED_EDGE ( 'NONE', *, *, #16289, .T. ) ;
#14585=CARTESIAN_POINT ( 'NONE',  ( 25.72395281601508898, -4.937620572523835349, 3.627061608673664228 ) ) ;
#14586=CARTESIAN_POINT ( 'NONE',  ( -29.03633718710667466, -14.58471626061076520, 13.43311195353574305 ) ) ;
#14591=DIRECTION ( 'NONE',  ( 0.000000000000000000, 0.000000000000000000, -1.000000000000000000 ) ) ;
#14597=CARTESIAN_POINT ( 'NONE',  ( 3.538288549924106796, -15.34800872113743431, 13.00000000000000178 ) ) ;
#14598=( LENGTH_UNIT ( ) NAMED_UNIT ( * ) SI_UNIT ( .MILLI., .METRE. ) );
#14600=CARTESIAN_POINT ( 'NONE',  ( 27.99987602667382802, -2.482696394238434578, 7.033357778048666020 ) ) ;
#14601=CARTESIAN_POINT ( 'NONE',  ( 30.45035428628836627, -2.914368949527523789, 3.283357778048666464 ) ) ;
#14603=ORIENTED_EDGE ( 'NONE', *, *, #13749, .F. ) ;
#14604=CARTESIAN_POINT ( 'NONE',  ( 30.35023428074701002, -1.862166024106576057, 5.783357778048662468 ) ) ;
#14605=DIRECTION ( 'NONE',  ( 0.000000000000000000, 0.000000000000000000, -1.000000000000000000 ) ) ;
#14610=CARTESIAN_POINT ( 'NONE',  ( 19.43845002722867221, 2.988003976273735596, 6.000000000000000000 ) ) ;
#14621=CARTESIAN_POINT ( 'NONE',  ( 26.24565837299761739, -7.163851760794091916, 4.332150178794286433 ) ) ;
#14639=ORIENTED_EDGE ( 'NONE', *, *, #8818, .F. ) ;
#14640=CARTESIAN_POINT ( 'NONE',  ( 29.25000000000000000, -16.21813761408365195, 13.37255996287876236 ) ) ;
#14646=LINE ( 'NONE', #3392, #16576 ) ;
#14648=CARTESIAN_POINT ( 'NONE',  ( 29.81991338116587542, -2.990324628369393611, 3.283357778048666464 ) ) ;
#14655=EDGE_CURVE ( 'NONE', #11687, #2087, #9724, .T. ) ;
#14657=CARTESIAN_POINT ( 'NONE',  ( 33.60446413004628141, -3.988174587000466342, 7.939653947423662039 ) ) ;
#14658=CARTESIAN_POINT ( 'NONE',  ( 27.02414796481377124, -2.900061135469103490, 4.705209693361168455 ) ) ;
#14663=CARTESIAN_POINT ( 'NONE',  ( 26.23609683341064525, -2.995005734021441768, 4.705209693361167567 ) ) ;
#14664=CARTESIAN_POINT ( 'NONE',  ( 13.00000000000000178, 0.000000000000000000, 8.700000000000001066 ) ) ;
#14677=FACE_OUTER_BOUND ( 'NONE', #13134, .T. ) ;
#14679=CARTESIAN_POINT ( 'NONE',  ( -9.099998387031003944, -19.29508120620799616, 16.81964500401478091 ) ) ;
#14680=CARTESIAN_POINT ( 'NONE',  ( 31.20090818012769773, -4.277755612481361602, 3.283357778048664244 ) ) ;
#14681=( BOUNDED_CURVE ( )  B_SPLINE_CURVE ( 2, ( #17054, #12678, #9758, #4607, #15226, #10036, #4258, #15313, #2803 ),
 .UNSPECIFIED., .F., .T. ) 
 B_SPLINE_CURVE_WITH_KNOTS ( ( 3, 2, 2, 2, 3 ),
 ( 0.2884615384615384914, 0.2948717948717948789, 0.3076923076923077094, 0.3205128205128205399, 0.3269230769230769273 ),
 .UNSPECIFIED. ) 
 CURVE ( )  GEOMETRIC_REPRESENTATION_ITEM ( )  RATIONAL_B_SPLINE_CURVE ( ( 0.9330127018922194093, 0.9330127018922196314, 1.000000000000000000, 0.8660254037844387076, 1.000000000000000000, 0.8660254037844387076, 1.000000000000000000, 0.9330127018922194093, 0.9330127018922194093 ) ) 
 REPRESENTATION_ITEM ( '' )  );
#14683=ORIENTED_EDGE ( 'NONE', *, *, #10415, .F. ) ;
#14685=CARTESIAN_POINT ( 'NONE',  ( 26.03917326857634151, -4.899642733102906433, 7.939653947423662039 ) ) ;
#14686=CARTESIAN_POINT ( 'NONE',  ( 32.19919549706052209, -6.038393303862174655, 6.861505862736157368 ) ) ;
#14690=DIRECTION ( 'NONE',  ( 0.000000000000000000, 1.000000000000000000, -0.000000000000000000 ) ) ;
#14701=VERTEX_POINT ( 'NONE', #15326 ) ;
#14703=CARTESIAN_POINT ( 'NONE',  ( 25.95846283556874212, -3.455553161483297053, 3.283357778048666464 ) ) ;
#14706=ORIENTED_EDGE ( 'NONE', *, *, #837, .F. ) ;
#14723=ADVANCED_FACE ( 'NONE', ( #9688 ), #16517, .T. ) ;
#14725=EDGE_LOOP ( 'NONE', ( #16982, #16528, #10880, #16051 ) ) ;
#14728=CYLINDRICAL_SURFACE ( 'NONE', #17050, 2.749999999999992006 ) ;
#14733=PLANE ( 'NONE',  #2939 ) ;
#14735=CARTESIAN_POINT ( 'NONE',  ( 32.87199790123699472, -1.558343308739095656, 5.783357778048663356 ) ) ;
#14737=CARTESIAN_POINT ( 'NONE',  ( 26.18940075748478691, -6.337263906362392341, 3.743184633113769699 ) ) ;
#14738=DIRECTION ( 'NONE',  ( 0.000000000000000000, 3.469446951953614189E-16, 1.000000000000000000 ) ) ;
#14740=EDGE_LOOP ( 'NONE', ( #17431, #7720, #10067, #10164, #17933 ) ) ;
#14745=CARTESIAN_POINT ( 'NONE',  ( 25.93488947238681774, -5.606027099510431988, 3.627061608673663784 ) ) ;
#14746=ORIENTED_EDGE ( 'NONE', *, *, #8118, .T. ) ;
#14749=CARTESIAN_POINT ( 'NONE',  ( 29.66420847303068697, -4.462897579762144851, 3.627061608673664228 ) ) ;
#14751=ORIENTED_EDGE ( 'NONE', *, *, #5656, .T. ) ;
#14754=CARTESIAN_POINT ( 'NONE',  ( 20.00000000000000000, 7.999999999999996447, 6.000000000000000000 ) ) ;
#14755=ADVANCED_FACE ( 'NONE', ( #1648 ), #5612, .T. ) ;
#14768=CARTESIAN_POINT ( 'NONE',  ( 29.84999239022537409, -5.894327871574777333, 8.283357778048658915 ) ) ;
#14769=ORIENTED_EDGE ( 'NONE', *, *, #15671, .F. ) ;
#14771=CARTESIAN_POINT ( 'NONE',  ( 31.71314141467879111, -4.216041623526076698, 7.939653947423662039 ) ) ;
#14773=CARTESIAN_POINT ( 'NONE',  ( 29.65098506949083301, -2.583579140294649523, 6.861505862736166250 ) ) ;
#14777=ADVANCED_FACE ( 'NONE', ( #12692 ), #4187, .T. ) ;
#14788=ORIENTED_EDGE ( 'NONE', *, *, #4330, .F. ) ;
#14795=DIRECTION ( 'NONE',  ( 0.000000000000000000, 0.000000000000000000, 1.000000000000000000 ) ) ;
#14798=CARTESIAN_POINT ( 'NONE',  ( 25.92409770820621162, -4.135217962343409326, 7.801241002635260102 ) ) ;
#14799=LINE ( 'NONE', #13249, #6711 ) ;
#14811=CARTESIAN_POINT ( 'NONE',  ( 23.00000000000000000, -16.21813761408365195, 13.00000000000000355 ) ) ;
#14813=ORIENTED_EDGE ( 'NONE', *, *, #11266, .T. ) ;
#14815=ADVANCED_FACE ( 'NONE', ( #14677, #7775 ), #10145, .T. ) ;
#14817=CARTESIAN_POINT ( 'NONE',  ( 30.06013935859953534, -5.869009311960809328, 3.283357778048663356 ) ) ;
#14818=AXIS2_PLACEMENT_3D ( 'NONE', #11204, #5602, #3083 ) ;
#14820=CARTESIAN_POINT ( 'NONE',  ( -21.42601376483257880, 2.765314980223223529, 0.000000000000000000 ) ) ;
#14824=AXIS2_PLACEMENT_3D ( 'NONE', #16623, #4201, #1303 ) ;
#14828=CARTESIAN_POINT ( 'NONE',  ( 33.95908713831673964, -3.945449517755641455, 8.283357778048662468 ) ) ;
#14829=CARTESIAN_POINT ( 'NONE',  ( 31.12210306526553083, -4.287250072544045665, 3.283357778048664244 ) ) ;
#14832=ORIENTED_EDGE ( 'NONE', *, *, #532, .F. ) ;
#14833=CARTESIAN_POINT ( 'NONE',  ( 29.55043834383899437, -5.730545699181964991, 7.939653947423658487 ) ) ;
#14834=CARTESIAN_POINT ( 'NONE',  ( 16.79145860028663151, -17.04903085677362640, 16.02982020200856184 ) ) ;
#14838=EDGE_CURVE ( 'NONE', #7363, #10674, #15350, .T. ) ;
#14843=VECTOR ( 'NONE', #17952, 1000.000000000000227 ) ;
#14849=CARTESIAN_POINT ( 'NONE',  ( 27.53837573810956130, -6.172832027328289506, 3.283357778048663800 ) ) ;
#14853=ORIENTED_EDGE ( 'NONE', *, *, #7444, .F. ) ;
#14854=CARTESIAN_POINT ( 'NONE',  ( 31.27962407439061110, -2.387360303286481855, 4.705209693361167567 ) ) ;
#14855=CARTESIAN_POINT ( 'NONE',  ( 30.91186687973582536, -2.431667782610909434, 6.861505862736166250 ) ) ;
#14856=ORIENTED_EDGE ( 'NONE', *, *, #9266, .T. ) ;
#14864=CARTESIAN_POINT ( 'NONE',  ( 31.68992120585416217, -1.700760206360153015, 5.783357778048662468 ) ) ;
#14866=CARTESIAN_POINT ( 'NONE',  ( 18.90607966454165734, -11.47788193099826692, 15.70134094032044736 ) ) ;
#14874=LINE ( 'NONE', #2461, #909 ) ;
#14877=CARTESIAN_POINT ( 'NONE',  ( 31.25770402584614871, -1.763030703431812451, 5.783357778048668685 ) ) ;
#14885=ORIENTED_EDGE ( 'NONE', *, *, #16722, .T. ) ;
#14909=CARTESIAN_POINT ( 'NONE',  ( 31.07327543742414022, -2.112412460091767308, 7.033357778048666020 ) ) ;
#14911=EDGE_CURVE ( 'NONE', #10340, #122, #159, .T. ) ;
#14913=CARTESIAN_POINT ( 'NONE',  ( 28.28502977505876359, -2.748149777785362957, 4.705209693361168455 ) ) ;
#14914=CARTESIAN_POINT ( 'NONE',  ( -20.00000000000000000, 7.999999999999996447, 0.000000000000000000 ) ) ;
#14915=CARTESIAN_POINT ( 'NONE',  ( 22.22189723075623036, -22.43265299876153662, 15.08700452545048343 ) ) ;
#14918=CARTESIAN_POINT ( 'NONE',  ( 27.17934203385504333, -30.00000000000000355, 12.00000000000000000 ) ) ;
#14923=DIRECTION ( 'NONE',  ( -0.000000000000000000, -0.000000000000000000, 1.000000000000000000 ) ) ;
#14929=CARTESIAN_POINT ( 'NONE',  ( 26.03917326857634151, -4.899642733102906433, 7.939653947423662039 ) ) ;
#14931=CARTESIAN_POINT ( 'NONE',  ( 27.47505859511117521, -2.218764776483033163, 5.783357778048668685 ) ) ;
#14932=CARTESIAN_POINT ( 'NONE',  ( 33.66004903264009585, -1.463398710186758267, 5.783357778048663356 ) ) ;
#14933=CARTESIAN_POINT ( 'NONE',  ( 32.29974222271236073, -2.891426744974864071, 7.939653947423664704 ) ) ;
#14934=CARTESIAN_POINT ( 'NONE',  ( 29.62480591732145996, -4.467644809586046151, 8.283357778048662468 ) ) ;
#14935=EDGE_CURVE ( 'NONE', #10223, #15284, #10828, .T. ) ;
#14938=CARTESIAN_POINT ( 'NONE',  ( 30.25080928106424594, -3.138282701210941994, 7.939653947423664704 ) ) ;
#14941=CARTESIAN_POINT ( 'NONE',  ( 29.66420847303068697, -4.462897579762144851, 3.627061608673664228 ) ) ;
#14943=LINE ( 'NONE', #8309, #11527 ) ;
#14944=FACE_OUTER_BOUND ( 'NONE', #5012, .T. ) ;
#14951=DIRECTION ( 'NONE',  ( 0.9928203230275512992, 0.1196152422706610180, 4.006172263299093133E-17 ) ) ;
#14957=ORIENTED_EDGE ( 'NONE', *, *, #10328, .T. ) ;
#14958=CARTESIAN_POINT ( 'NONE',  ( 30.90769699326645181, -6.820963901304073929, 5.783357778048658915 ) ) ;
#14960=DIRECTION ( 'NONE',  ( -1.000000000000000000, 0.000000000000000000, 0.000000000000000000 ) ) ;
#14963=CARTESIAN_POINT ( 'NONE',  ( 25.75741033704265703, -2.751693534003877062, 5.593203463216974036 ) ) ;
#14967=VERTEX_POINT ( 'NONE', #6674 ) ;
#14974=ADVANCED_FACE ( 'NONE', ( #10906 ), #17692, .F. ) ;
#14977=AXIS2_PLACEMENT_3D ( 'NONE', #9868, #15423, #14063 ) ;
#14978=CARTESIAN_POINT ( 'NONE',  ( -11.38175538881593774, -22.33742387525457573, 16.67884400577319681 ) ) ;
#14980=VERTEX_POINT ( 'NONE', #14932 ) ;
#14991=CARTESIAN_POINT ( 'NONE',  ( 32.29295089585319545, -5.599999616269980329, 8.283357778048658915 ) ) ;
#14993=CIRCLE ( 'NONE', #12104, 5.000000000000000888 ) ;
#14994=CARTESIAN_POINT ( 'NONE',  ( 28.52162355051263987, -6.481468097106410475, 4.705209693361159573 ) ) ;
#15000=CARTESIAN_POINT ( 'NONE',  ( 9.099998387031005720, -19.29508120620799971, 16.81964500401478091 ) ) ;
#15002=VERTEX_POINT ( 'NONE', #6937 ) ;
#15004=EDGE_CURVE ( 'NONE', #16224, #2940, #2963, .T. ) ;
#15007=CARTESIAN_POINT ( 'NONE',  ( 26.85044460880409645, -7.319979551716484067, 5.783357778048657138 ) ) ;
#15009=CARTESIAN_POINT ( 'NONE',  ( 25.71072941247523502, -3.058302133056337357, 6.861505862736165362 ) ) ;
#15010=CARTESIAN_POINT ( 'NONE',  ( 29.19137779418881351, -4.519864338893556877, 7.939653947423662039 ) ) ;
#15011=DIRECTION ( 'NONE',  ( 0.9928203230275512992, 0.1196152422706610180, 4.006172263299093133E-17 ) ) ;
#15013=CARTESIAN_POINT ( 'NONE',  ( 32.72003615946069743, -2.840789625746940938, 3.627061608673666893 ) ) ;
#15014=EDGE_LOOP ( 'NONE', ( #3500, #12948 ) ) ;
#15015=CARTESIAN_POINT ( 'NONE',  ( 28.20260476654369697, -6.819712339336020612, 4.533357778048659803 ) ) ;
#15019=ORIENTED_EDGE ( 'NONE', *, *, #2382, .F. ) ;
#15020=CARTESIAN_POINT ( 'NONE',  ( 32.54503264317084188, -5.369756224683081669, 7.939653947423658487 ) ) ;
#15022=VERTEX_POINT ( 'NONE', #4142 ) ;
#15023=CARTESIAN_POINT ( 'NONE',  ( 29.78250536075762867, -6.329556739422670830, 4.705209693361159573 ) ) ;
#15024=EDGE_LOOP ( 'NONE', ( #14220, #429 ) ) ;
#15027=CYLINDRICAL_SURFACE ( 'NONE', #15394, 2.500000000000001776 ) ;
#15029=CARTESIAN_POINT ( 'NONE',  ( 30.54048978798443059, -6.538043363838207611, 7.033357778048657138 ) ) ;
#15035=CARTESIAN_POINT ( 'NONE',  ( 26.47260139170898441, -4.847423203795396596, 8.283357778048662468 ) ) ;
#15042=CARTESIAN_POINT ( 'NONE',  ( -7.499998387031003411, -20.49508120620799900, 13.00000000000000178 ) ) ;
#15046=EDGE_LOOP ( 'NONE', ( #14324, #8356, #2180, #8456 ) ) ;
#15047=CARTESIAN_POINT ( 'NONE',  ( 32.14213199643173624, -2.910415664685331638, 7.939653947423662927 ) ) ;
#15054=CARTESIAN_POINT ( 'NONE',  ( 25.76974524478944772, -2.854074692636066946, 6.425565898159212530 ) ) ;
#15057=B_SPLINE_CURVE_WITH_KNOTS ( 'NONE', 3,
 ( #12842, #3232, #4845, #1971, #12925, #10373, #14581, #6024, #13201, #14302, #3139, #4672, #777, #6306, #11826, #7493, #14199, #6123 ),
 .UNSPECIFIED., .F., .F.,
 ( 4, 2, 2, 2, 2, 2, 2, 2, 4 ),
 ( 0.000000000000000000, 0.0005710890023745246154, 0.001142178004749049231, 0.001713267007123573955, 0.002284356009498098462, 0.002855445011872622969, 0.003426534014247147909, 0.003997623016621672416, 0.004568712018996196923 ),
 .UNSPECIFIED. ) ;
#15065=AXIS2_PLACEMENT_3D ( 'NONE', #2210, #477, #17081 ) ;
#15068=AXIS2_PLACEMENT_3D ( 'NONE', #342, #5032, #13204 ) ;
#15069=AXIS2_PLACEMENT_3D ( 'NONE', #381, #11410, #3815 ) ;
#15070=CARTESIAN_POINT ( 'NONE',  ( 35.74085044863416982, 7.999999999999934275, 11.27079897466147429 ) ) ;
#15079=VERTEX_POINT ( 'NONE', #13918 ) ;
#15082=CARTESIAN_POINT ( 'NONE',  ( 31.75254397038802878, -4.211294393702175398, 3.283357778048664244 ) ) ;
#15088=VECTOR ( 'NONE', #7527, 1000.000000000000000 ) ;
#15090=CARTESIAN_POINT ( 'NONE',  ( 31.24031073583692475, -4.273008382657478954, 7.939653947423662039 ) ) ;
#15094=ORIENTED_EDGE ( 'NONE', *, *, #3962, .F. ) ;
#15100=CARTESIAN_POINT ( 'NONE',  ( 27.81599742762458050, -2.504850134108091098, 4.533357778048667797 ) ) ;
#15102=CARTESIAN_POINT ( 'NONE',  ( 27.50150540219088313, -5.977401655418042914, 7.939653947423658487 ) ) ;
#15103=CARTESIAN_POINT ( 'NONE',  ( 29.99682221560115991, -1.914942061115552541, 5.783357778048668685 ) ) ;
#15105=DIRECTION ( 'NONE',  ( -0.000000000000000000, -0.000000000000000000, 1.000000000000000000 ) ) ;
#15107=CARTESIAN_POINT ( 'NONE',  ( 33.35047706458318828, -2.764833946905071560, 3.627061608673666893 ) ) ;
#15110=EDGE_CURVE ( 'NONE', #8113, #17858, #5657, .T. ) ;
#15113=CARTESIAN_POINT ( 'NONE',  ( 30.23341599105502908, -5.648260380436597394, 3.627061608673662896 ) ) ;
#15115=ORIENTED_EDGE ( 'NONE', *, *, #13251, .F. ) ;
#15116=CARTESIAN_POINT ( 'NONE',  ( 29.04699097144805364, -6.418171698071525100, 6.861505862736157368 ) ) ;
#15125=CYLINDRICAL_SURFACE ( 'NONE', #11926, 2.500000000000001776 ) ;
#15135=CARTESIAN_POINT ( 'NONE',  ( 26.14456121274580624, -5.685614013951941992, 3.283357778048664688 ) ) ;
#15140=CARTESIAN_POINT ( 'NONE',  ( 33.40301380667672504, -2.758504307001591993, 7.939653947423662927 ) ) ;
#15141=AXIS2_PLACEMENT_3D ( 'NONE', #17293, #13367, #3485 ) ;
#15147=CARTESIAN_POINT ( 'NONE',  ( 32.58190297908952004, -5.565186596593329149, 3.283357778048663356 ) ) ;
#15158=CARTESIAN_POINT ( 'NONE',  ( 30.80688261270428541, -4.325227911964988792, 8.283357778048662468 ) ) ;
#15167=EDGE_CURVE ( 'NONE', #8906, #11992, #14194, .T. ) ;
#15169=ADVANCED_FACE ( 'NONE', ( #7047 ), #1690, .F. ) ;
#15172=DIRECTION ( 'NONE',  ( 0.000000000000000000, 1.000000000000000000, 0.000000000000000000 ) ) ;
#15175=CARTESIAN_POINT ( 'NONE',  ( 32.60321786976872005, -6.626883982076972046, 5.783357778048664244 ) ) ;
#15177=AXIS2_PLACEMENT_3D ( 'NONE', #13716, #15244, #1297 ) ;
#15179=CARTESIAN_POINT ( 'NONE',  ( 27.02414796481377124, -2.900061135469103490, 4.705209693361168455 ) ) ;
#15180=CARTESIAN_POINT ( 'NONE',  ( -17.31608032955932330, -13.61075944537037508, 15.95276485144012035 ) ) ;
#15182=VERTEX_POINT ( 'NONE', #9726 ) ;
#15183=CARTESIAN_POINT ( 'NONE',  ( 30.95252083063564896, -1.789602389065743981, 5.113484796970861446 ) ) ;
#15188=UNCERTAINTY_MEASURE_WITH_UNIT (LENGTH_MEASURE( 1.000000000000000082E-05 ), #14598, 'distance_accuracy_value', 'NONE');
#15190=DIRECTION ( 'NONE',  ( -1.000000000000000000, 0.000000000000000000, 0.000000000000000000 ) ) ;
#15194=CARTESIAN_POINT ( 'NONE',  ( 30.45225960443380231, -4.367952981209816343, 7.939653947423662039 ) ) ;
#15197=CARTESIAN_POINT ( 'NONE',  ( 33.56062403295735663, -2.739515387291124426, 7.939653947423664704 ) ) ;
#15198=ORIENTED_EDGE ( 'NONE', *, *, #9588, .T. ) ;
#15199=EDGE_LOOP ( 'NONE', ( #266, #5578, #17498 ) ) ;
#15200=CARTESIAN_POINT ( 'NONE',  ( 29.38830135902312080, -2.615227339812091767, 4.705209693361167567 ) ) ;
#15201=DIRECTION ( 'NONE',  ( -0.1196152422706584506, 0.9928203230275515212, 0.000000000000000000 ) ) ;
#15203=CARTESIAN_POINT ( 'NONE',  ( 27.04606801335823718, -3.524390735323771118, 3.627061608673666449 ) ) ;
#15207=FACE_OUTER_BOUND ( 'NONE', #12050, .T. ) ;
#15211=EDGE_CURVE ( 'NONE', #2920, #15079, #12562, .T. ) ;
#15218=FACE_OUTER_BOUND ( 'NONE', #2264, .T. ) ;
#15219=ORIENTED_EDGE ( 'NONE', *, *, #8106, .F. ) ;
#15221=EDGE_LOOP ( 'NONE', ( #5622, #3571 ) ) ;
#15225=CARTESIAN_POINT ( 'NONE',  ( 30.88125018618674034, -3.062327022369072171, 7.939653947423662927 ) ) ;
#15226=CARTESIAN_POINT ( 'NONE',  ( 31.43732351782677625, -4.249272233123119413, 8.283357778048662468 ) ) ;
#15228=DIRECTION ( 'NONE',  ( -0.000000000000000000, -1.000000000000000000, -0.000000000000000000 ) ) ;
#15231=CARTESIAN_POINT ( 'NONE',  ( -25.11802603177690330, -19.03270077640482683, 10.53798182577225084 ) ) ;
#15235=EDGE_LOOP ( 'NONE', ( #9445, #1542, #3882, #125, #10786, #14432, #8288, #5536, #11918, #12073, #5991, #5419, #1133, #6584, #8726 ) ) ;
#15237=DIRECTION ( 'NONE',  ( 1.000000000000000000, 0.000000000000000000, 0.000000000000000000 ) ) ;
#15241=( BOUNDED_CURVE ( )  B_SPLINE_CURVE ( 2, ( #303, #5813, #8637, #4287, #12446, #32, #14167, #121, #5541 ),
 .UNSPECIFIED., .F., .T. ) 
 B_SPLINE_CURVE_WITH_KNOTS ( ( 3, 2, 2, 2, 3 ),
 ( 0.4423076923076923461, 0.4487179487179487336, 0.4615384615384615641, 0.4743589743589743390, 0.4807692307692307820 ),
 .UNSPECIFIED. ) 
 CURVE ( )  GEOMETRIC_REPRESENTATION_ITEM ( )  RATIONAL_B_SPLINE_CURVE ( ( 0.9330127018922194093, 0.9330127018922196314, 1.000000000000000000, 0.8660254037844387076, 1.000000000000000000, 0.8660254037844387076, 1.000000000000000000, 0.9330127018922190762, 0.9330127018922194093 ) ) 
 REPRESENTATION_ITEM ( '' )  );
#15243=ORIENTED_EDGE ( 'NONE', *, *, #10507, .T. ) ;
#15244=DIRECTION ( 'NONE',  ( -0.000000000000000000, -0.000000000000000000, 1.000000000000000000 ) ) ;
#15246=DIRECTION ( 'NONE',  ( -0.000000000000000000, -1.000000000000000000, 3.469446951953614189E-16 ) ) ;
#15247=VERTEX_POINT ( 'NONE', #16740 ) ;
#15252=ORIENTED_EDGE ( 'NONE', *, *, #15614, .T. ) ;
#15255=CARTESIAN_POINT ( 'NONE',  ( 32.60321786976872005, -6.626883982076972934, 5.783357778048664244 ) ) ;
#15257=CARTESIAN_POINT ( 'NONE',  ( 28.69037342443288452, -3.126411886501869741, 8.283357778048666020 ) ) ;
#15262=CARTESIAN_POINT ( 'NONE',  ( 0.000000000000000000, 0.000000000000000000, 8.700000000000001066 ) ) ;
#15263=CARTESIAN_POINT ( 'NONE',  ( 35.41536221060850664, -16.03270077640482683, 10.53798182577225084 ) ) ;
#15268=ORIENTED_EDGE ( 'NONE', *, *, #11541, .T. ) ;
#15275=CARTESIAN_POINT ( 'NONE',  ( 33.52375369703867847, -2.544085015380856518, 3.283357778048666464 ) ) ;
#15276=CARTESIAN_POINT ( 'NONE',  ( 30.90769699326644826, -6.820963901304073929, 5.783357778048658027 ) ) ;
#15279=CARTESIAN_POINT ( 'NONE',  ( -16.75000000000000000, -16.21813761408365195, 13.00000000000000178 ) ) ;
#15282=ORIENTED_EDGE ( 'NONE', *, *, #17819, .F. ) ;
#15284=VERTEX_POINT ( 'NONE', #426 ) ;
#15286=CARTESIAN_POINT ( 'NONE',  ( 27.71165237056504438, -5.952083095804076684, 3.627061608673662896 ) ) ;
#15288=ORIENTED_EDGE ( 'NONE', *, *, #17191, .T. ) ;
#15289=CARTESIAN_POINT ( 'NONE',  ( 28.54354359905709160, -7.105797696961086096, 5.783357778048657138 ) ) ;
#15294=CIRCLE ( 'NONE', #17659, 5.500000000000000888 ) ;
#15299=EDGE_CURVE ( 'NONE', #17262, #11389, #375, .T. ) ;
#15301=CARTESIAN_POINT ( 'NONE',  ( 26.79770707206266778, -11.23794579741151090, 14.03572743982056181 ) ) ;
#15310=ADVANCED_FACE ( 'NONE', ( #4668 ), #4839, .F. ) ;
#15311=CARTESIAN_POINT ( 'NONE',  ( 28.87615734162756453, -4.557842178314484016, 3.627061608673664228 ) ) ;
#15313=CARTESIAN_POINT ( 'NONE',  ( 31.00882954110335632, -1.782818301463667598, 6.453230759126474148 ) ) ;
#15314=CARTESIAN_POINT ( 'NONE',  ( -45.00000000000000711, -16.03270077640482683, 10.53798182577225084 ) ) ;
#15326=CARTESIAN_POINT ( 'NONE',  ( 33.76207435632690590, -3.969185667289998332, 7.939653947423662039 ) ) ;
#15330=CARTESIAN_POINT ( 'NONE',  ( 32.19529564017040002, -1.250324391365404741, 5.783357778048668685 ) ) ;
#15332=VECTOR ( 'NONE', #178, 1000.000000000000000 ) ;
#15334=EDGE_CURVE ( 'NONE', #6838, #12650, #861, .T. ) ;
#15342=CARTESIAN_POINT ( 'NONE',  ( 7.345582307948228973, 16.91090888051954977, 16.91488491921997195 ) ) ;
#15350=( BOUNDED_CURVE ( )  B_SPLINE_CURVE ( 3, ( #15511, #11598, #1836, #10484 ),
 .UNSPECIFIED., .F., .F. ) 
 B_SPLINE_CURVE_WITH_KNOTS ( ( 4, 4 ),
 ( 1.221730476396036824, 1.230954889131919305 ),
 .UNSPECIFIED. ) 
 CURVE ( )  GEOMETRIC_REPRESENTATION_ITEM ( )  RATIONAL_B_SPLINE_CURVE ( ( 1.000000000000000000, 0.9999929091967096895, 0.9999929091967096895, 1.000000000000000000 ) ) 
 REPRESENTATION_ITEM ( '' )  );
#15354=CARTESIAN_POINT ( 'NONE',  ( 29.26075783691881682, -2.330785036554694489, 7.033357778048666020 ) ) ;
#15358=CARTESIAN_POINT ( 'NONE',  ( 33.26181313012506280, -6.547536259434060923, 5.113484796970854340 ) ) ;
#15359=ORIENTED_EDGE ( 'NONE', *, *, #1356, .T. ) ;
#15360=CARTESIAN_POINT ( 'NONE',  ( 25.11802603177690330, -19.03270077640482683, 10.53798182577225084 ) ) ;
#15362=CARTESIAN_POINT ( 'NONE',  ( 26.78782184427022983, -4.809445364374452581, 3.283357778048664244 ) ) ;
#15370=CARTESIAN_POINT ( 'NONE',  ( 33.48996557372703364, -1.821249024531260696, 4.533357778048667797 ) ) ;
#15373=DIRECTION ( 'NONE',  ( -0.000000000000000000, -0.000000000000000000, 1.000000000000000000 ) ) ;
#15374=CARTESIAN_POINT ( 'NONE',  ( 31.84257795004536007, -2.746633492292519296, 8.283357778048666020 ) ) ;
#15375=CARTESIAN_POINT ( 'NONE',  ( 31.41531425212677675, -1.744041783721344219, 5.783357778048668685 ) ) ;
#15379=VERTEX_POINT ( 'NONE', #7751 ) ;
#15380=CARTESIAN_POINT ( 'NONE',  ( 29.41022140756759029, -3.239556939666760726, 3.627061608673666893 ) ) ;
#15383=VERTEX_POINT ( 'NONE', #4754 ) ;
#15384=CARTESIAN_POINT ( 'NONE',  ( 25.78291734803729796, -2.627872734613073913, 6.136288781622796229 ) ) ;
#15385=DIRECTION ( 'NONE',  ( -1.000000000000000000, 0.000000000000000000, 0.000000000000000000 ) ) ;
#15393=CARTESIAN_POINT ( 'NONE',  ( 26.79666222766753592, -21.19920099154242976, 14.03599807436713398 ) ) ;
#15394=AXIS2_PLACEMENT_3D ( 'NONE', #7883, #5141, #2447 ) ;
#15407=CARTESIAN_POINT ( 'NONE',  ( 28.76238721243587548, -5.825490297734302381, 7.939653947423658487 ) ) ;
#15408=VECTOR ( 'NONE', #4321, 1000.000000000000000 ) ;
#15415=DIRECTION ( 'NONE',  ( 1.000000000000000000, 0.000000000000000000, 0.000000000000000000 ) ) ;
#15417=CIRCLE ( 'NONE', #7323, 2.000000000000001776 ) ;
#15420=EDGE_CURVE ( 'NONE', #4895, #16872, #2058, .T. ) ;
#15422=DIRECTION ( 'NONE',  ( 0.000000000000000000, 0.000000000000000000, 1.000000000000000000 ) ) ;
#15423=DIRECTION ( 'NONE',  ( 0.9928203230275511881, 0.1196152422706610735, 9.614813431917827710E-17 ) ) ;
#15424=CARTESIAN_POINT ( 'NONE',  ( 20.25000000000000355, -16.21813761408365195, 0.000000000000000000 ) ) ;
#15427=CARTESIAN_POINT ( 'NONE',  ( 30.44283453230164227, -2.188368138933637574, 7.033357778048666020 ) ) ;
#15442=EDGE_CURVE ( 'NONE', #9693, #14407, #12246, .T. ) ;
#15444=DIRECTION ( 'NONE',  ( 0.6000000000000001998, -0.7999999999999999334, 0.000000000000000000 ) ) ;
#15446=CARTESIAN_POINT ( 'NONE',  ( 29.27960797773944179, -6.689954721521948144, 7.033357778048657138 ) ) ;
#15448=CARTESIAN_POINT ( 'NONE',  ( 25.84216048658649001, -4.923378882637265974, 8.283357778048662468 ) ) ;
#15449=CARTESIAN_POINT ( 'NONE',  ( 27.67650891848073158, -3.448435056481901295, 3.627061608673666893 ) ) ;
#15450=CARTESIAN_POINT ( 'NONE',  ( -28.68370877339674863, -18.82577899785919584, 13.53184763361698906 ) ) ;
#15451=CARTESIAN_POINT ( 'NONE',  ( 30.00264913441657555, -6.940201157507134511, 5.783357778048669573 ) ) ;
#15454=ORIENTED_EDGE ( 'NONE', *, *, #4512, .F. ) ;
#15461=CARTESIAN_POINT ( 'NONE',  ( -5.499998817156067865, -20.49639288455253450, 13.00000000000000178 ) ) ;
#15469=CARTESIAN_POINT ( 'NONE',  ( 29.55043834383899437, -5.730545699181964991, 7.939653947423658487 ) ) ;
#15473=CARTESIAN_POINT ( 'NONE',  ( 26.87106449706838873, -6.053357334259913181, 7.939653947423658487 ) ) ;
#15477=CARTESIAN_POINT ( 'NONE',  ( 26.60838078660069428, -6.085005533777348319, 3.627061608673662896 ) ) ;
#15480=VERTEX_POINT ( 'NONE', #1169 ) ;
#15481=DIRECTION ( 'NONE',  ( 1.000000000000000000, 0.000000000000000000, 0.000000000000000000 ) ) ;
#15482=LINE ( 'NONE', #3149, #13085 ) ;
#15486=CARTESIAN_POINT ( 'NONE',  ( 29.25000000000000000, -16.21813761408365195, 13.37255996287876236 ) ) ;
#15487=LINE ( 'NONE', #8587, #7521 ) ;
#15493=VERTEX_POINT ( 'NONE', #9570 ) ;
#15495=ORIENTED_EDGE ( 'NONE', *, *, #13553, .T. ) ;
#15497=CARTESIAN_POINT ( 'NONE',  ( 29.62036837594175154, -3.214238380052812261, 7.939653947423662927 ) ) ;
#15500=CYLINDRICAL_SURFACE ( 'NONE', #14441, 14.00000000000000178 ) ;
#15505=CYLINDRICAL_SURFACE ( 'NONE', #2349, 2.500000000000001776 ) ;
#15511=CARTESIAN_POINT ( 'NONE',  ( 35.74085044863416982, -18.73429073671341172, 11.27079897466147251 ) ) ;
#15513=ORIENTED_EDGE ( 'NONE', *, *, #15957, .F. ) ;
#15515=CARTESIAN_POINT ( 'NONE',  ( 29.41846958523816724, -7.400131432564565515, 5.783357778048657138 ) ) ;
#15518=CARTESIAN_POINT ( 'NONE',  ( 26.53943449477818106, -2.321292140958837624, 5.113484796970856117 ) ) ;
#15531=ORIENTED_EDGE ( 'NONE', *, *, #7093, .T. ) ;
#15532=CARTESIAN_POINT ( 'NONE',  ( 32.14665875496697822, -6.044722943765660439, 4.705209693361160461 ) ) ;
#15535=CARTESIAN_POINT ( 'NONE',  ( 29.18195272205665347, -2.340279496617377664, 7.033357778048666020 ) ) ;
#15544=CYLINDRICAL_SURFACE ( 'NONE', #12451, 2.500000000000001776 ) ;
#15545=ADVANCED_FACE ( 'NONE', ( #8778 ), #10210, .T. ) ;
#15552=DIRECTION ( 'NONE',  ( -1.000000000000000000, 0.000000000000000000, 0.000000000000000000 ) ) ;
#15553=CARTESIAN_POINT ( 'NONE',  ( 29.65098506949083301, -2.583579140294649523, 6.861505862736166250 ) ) ;
#15554=AXIS2_PLACEMENT_3D ( 'NONE', #955, #5191, #13372 ) ;
#15559=CARTESIAN_POINT ( 'NONE',  ( 29.62036837594175154, -3.214238380052812261, 7.939653947423664704 ) ) ;
#15563=CARTESIAN_POINT ( 'NONE',  ( 26.62577407660990758, -3.575027854551694695, 7.939653947423662927 ) ) ;
#15564=ORIENTED_EDGE ( 'NONE', *, *, #6625, .T. ) ;
#15571=CIRCLE ( 'NONE', #12089, 5.500000000000000000 ) ;
#15572=CARTESIAN_POINT ( 'NONE',  ( 29.08710323061924896, -17.65086537115787380, 13.41876697690134179 ) ) ;
#15573=DIRECTION ( 'NONE',  ( 0.000000000000000000, 0.000000000000000000, 1.000000000000000000 ) ) ;
#15582=CARTESIAN_POINT ( 'NONE',  ( 29.01637427789896151, -7.048830937829682064, 5.783357778048658915 ) ) ;
#15583=AXIS2_PLACEMENT_3D ( 'NONE', #1153, #15105, #9219 ) ;
#15590=CARTESIAN_POINT ( 'NONE',  ( 25.90934487712385348, 0.1208734971681838660, 5.783357778048663356 ) ) ;
#15596=CONICAL_SURFACE ( 'NONE', #11211, 3.999999999999986677, 0.7853981633974400633 ) ;
#15597=ORIENTED_EDGE ( 'NONE', *, *, #9850, .F. ) ;
#15602=CARTESIAN_POINT ( 'NONE',  ( 25.93714794488954212, -2.393855775999666591, 5.783357778048667797 ) ) ;
#15604=CARTESIAN_POINT ( 'NONE',  ( 27.21934464581372737, -3.303641803799556964, 3.283357778048666464 ) ) ;
#15607=DIRECTION ( 'NONE',  ( -0.1196152422706610735, 0.9928203230275511881, 0.000000000000000000 ) ) ;
#15614=EDGE_CURVE ( 'NONE', #9143, #1544, #11564, .T. ) ;
#15616=( BOUNDED_CURVE ( )  B_SPLINE_CURVE ( 2, ( #16639, #9992, #6837, #1678, #224, #4215, #8473, #5734, #7212 ),
 .UNSPECIFIED., .F., .T. ) 
 B_SPLINE_CURVE_WITH_KNOTS ( ( 3, 2, 2, 2, 3 ),
 ( 0.5576923076923077094, 0.5641025641025640969, 0.5769230769230768718, 0.5897435897435897578, 0.5961538461538461453 ),
 .UNSPECIFIED. ) 
 CURVE ( )  GEOMETRIC_REPRESENTATION_ITEM ( )  RATIONAL_B_SPLINE_CURVE ( ( 0.9330127018922194093, 0.9330127018922194093, 1.000000000000000000, 0.8660254037844387076, 1.000000000000000000, 0.8660254037844387076, 1.000000000000000000, 0.9330127018922194093, 0.9330127018922194093 ) ) 
 REPRESENTATION_ITEM ( '' )  );
#15619=LINE ( 'NONE', #8083, #6364 ) ;
#15626=CARTESIAN_POINT ( 'NONE',  ( 26.83664947211162399, -6.984282976826746037, 7.033357778048657138 ) ) ;
#15630=CARTESIAN_POINT ( 'NONE',  ( -26.79284261260708178, -21.20213040957736794, 14.03697675243215848 ) ) ;
#15632=VERTEX_POINT ( 'NONE', #1894 ) ;
#15647=CARTESIAN_POINT ( 'NONE',  ( 32.87199790123699472, -1.558343308739095656, 5.783357778048663356 ) ) ;
#15648=CARTESIAN_POINT ( 'NONE',  ( 30.93831368681553684, -6.190304661545915188, 6.861505862736157368 ) ) ;
#15651=LINE ( 'NONE', #7324, #15757 ) ;
#15652=ORIENTED_EDGE ( 'NONE', *, *, #14911, .F. ) ;
#15654=CARTESIAN_POINT ( 'NONE',  ( 31.41531425212677675, -1.744041783721344219, 5.783357778048668685 ) ) ;
#15657=CIRCLE ( 'NONE', #11318, 5.000000000000000888 ) ;
#15666=CARTESIAN_POINT ( 'NONE',  ( 28.59863824134335530, -19.00380184606325429, 13.55546330914018149 ) ) ;
#15671=EDGE_CURVE ( 'NONE', #16160, #118, #15482, .T. ) ;
#15672=CIRCLE ( 'NONE', #17141, 2.000000000000001776 ) ;
#15675=CARTESIAN_POINT ( 'NONE',  ( 32.90454166015506132, -1.164874252460851300, 5.783357778048668685 ) ) ;
#15679=CARTESIAN_POINT ( 'NONE',  ( 30.01874226414561875, -2.539271660970221944, 4.705209693361167567 ) ) ;
#15680=CARTESIAN_POINT ( 'NONE',  ( 33.30663696749426350, -1.516174747195734085, 5.783357778048668685 ) ) ;
#15682=CARTESIAN_POINT ( 'NONE',  ( 26.31556265977298992, -7.384422263489805793, 5.783357778048663356 ) ) ;
#15687=AXIS2_PLACEMENT_3D ( 'NONE', #3235, #12568, #16846 ) ;
#15690=UNCERTAINTY_MEASURE_WITH_UNIT (LENGTH_MEASURE( 1.000000000000000082E-05 ), #14317, 'distance_accuracy_value', 'NONE');
#15692=ORIENTED_EDGE ( 'NONE', *, *, #11592, .T. ) ;
#15700=CARTESIAN_POINT ( 'NONE',  ( 27.02423718196931546, -4.780961985016209503, 8.283357778048662468 ) ) ;
#15704=EDGE_CURVE ( 'NONE', #4898, #14980, #9878, .T. ) ;
#15710=( BOUNDED_CURVE ( )  B_SPLINE_CURVE ( 2, ( #8833, #15814, #17197, #7657, #2545, #17287, #4823, #16098, #10353 ),
 .UNSPECIFIED., .F., .T. ) 
 B_SPLINE_CURVE_WITH_KNOTS ( ( 3, 2, 2, 2, 3 ),
 ( 0.7500000000000000000, 0.7564102564102563875, 0.7692307692307692735, 0.7820512820512820484, 0.7884615384615384359 ),
 .UNSPECIFIED. ) 
 CURVE ( )  GEOMETRIC_REPRESENTATION_ITEM ( )  RATIONAL_B_SPLINE_CURVE ( ( 0.9330127018922194093, 0.9330127018922194093, 1.000000000000000000, 0.8660254037844387076, 1.000000000000000000, 0.8660254037844387076, 1.000000000000000000, 0.9330127018922194093, 0.9330127018922194093 ) ) 
 REPRESENTATION_ITEM ( '' )  );
#15712=CIRCLE ( 'NONE', #7026, 2.000000000000001776 ) ;
#15714=APPLICATION_CONTEXT ( 'automotive_design' ) ;
#15721=CARTESIAN_POINT ( 'NONE',  ( 27.82847066025702887, -2.165988739474055791, 5.783357778048667797 ) ) ;
#15724=EDGE_CURVE ( 'NONE', #2087, #172, #9300, .T. ) ;
#15726=CARTESIAN_POINT ( 'NONE',  ( 31.51169109130924184, -2.986371343527201905, 7.939653947423664704 ) ) ;
#15727=ADVANCED_FACE ( 'NONE', ( #11928, #2167 ), #3508, .T. ) ;
#15731=ORIENTED_EDGE ( 'NONE', *, *, #1311, .T. ) ;
#15735=( BOUNDED_CURVE ( )  B_SPLINE_CURVE ( 2, ( #6924, #15183, #11077, #5463, #45, #14092, #132, #5645, #2845 ),
 .UNSPECIFIED., .F., .T. ) 
 B_SPLINE_CURVE_WITH_KNOTS ( ( 3, 2, 2, 2, 3 ),
 ( 0.3269230769230769273, 0.3333333333333333148, 0.3461538461538461453, 0.3589743589743589758, 0.3653846153846154188 ),
 .UNSPECIFIED. ) 
 CURVE ( )  GEOMETRIC_REPRESENTATION_ITEM ( )  RATIONAL_B_SPLINE_CURVE ( ( 0.9330127018922194093, 0.9330127018922194093, 1.000000000000000000, 0.8660254037844387076, 1.000000000000000000, 0.8660254037844387076, 1.000000000000000000, 0.9330127018922190762, 0.9330127018922194093 ) ) 
 REPRESENTATION_ITEM ( '' )  );
#15736=CARTESIAN_POINT ( 'NONE',  ( 25.07353123778398896, 1.235291682954687165, 14.60266621045498425 ) ) ;
#15739=AXIS2_PLACEMENT_3D ( 'NONE', #3337, #10117, #12858 ) ;
#15744=CARTESIAN_POINT ( 'NONE',  ( 26.01652455409633902, -4.902371455920926380, 5.783357778048663356 ) ) ;
#15747=CARTESIAN_POINT ( 'NONE',  ( 28.89355063163679915, -2.047864499088824175, 5.783357778048668685 ) ) ;
#15750=ORIENTED_EDGE ( 'NONE', *, *, #10374, .T. ) ;
#15751=CARTESIAN_POINT ( 'NONE',  ( 32.29974222271236073, -2.891426744974864071, 7.939653947423664704 ) ) ;
#15753=CYLINDRICAL_SURFACE ( 'NONE', #2112, 6.249999999999998224 ) ;
#15754=ORIENTED_EDGE ( 'NONE', *, *, #9883, .T. ) ;
#15757=VECTOR ( 'NONE', #7412, 1000.000000000000114 ) ;
#15759=DIRECTION ( 'NONE',  ( 0.000000000000000000, 0.000000000000000000, -1.000000000000000000 ) ) ;
#15767=CARTESIAN_POINT ( 'NONE',  ( 32.30788887834420819, -1.963665922152317833, 4.533357778048667797 ) ) ;
#15770=ORIENTED_EDGE ( 'NONE', *, *, #3743, .F. ) ;
#15771=CARTESIAN_POINT ( 'NONE',  ( 25.99795558426325215, -4.648046406214923820, 7.939653947423662039 ) ) ;
#15772=CARTESIAN_POINT ( 'NONE',  ( 32.18597209352066812, -4.159074864394664672, 3.627061608673664228 ) ) ;
#15774=DIRECTION ( 'NONE',  ( 0.9928203230275510771, 0.1196152422706609902, 4.006172263299092517E-17 ) ) ;
#15775=EDGE_CURVE ( 'NONE', #3948, #10789, #3268, .T. ) ;
#15776=FACE_BOUND ( 'NONE', #11396, .T. ) ;
#15782=DIRECTION ( 'NONE',  ( 0.9928203230275512992, 0.1196152422706610180, 4.006172263299093133E-17 ) ) ;
#15790=CARTESIAN_POINT ( 'NONE',  ( 27.84978555093622177, -3.227686124957687586, 3.283357778048666464 ) ) ;
#15791=VERTEX_POINT ( 'NONE', #5118 ) ;
#15792=LINE ( 'NONE', #2634, #12377 ) ;
#15795=ADVANCED_FACE ( 'NONE', ( #10639, #2424 ), #5038, .F. ) ;
#15805=DIRECTION ( 'NONE',  ( 0.1113444980252557837, 0.9937818688019538493, 0.000000000000000000 ) ) ;
#15809=CARTESIAN_POINT ( 'NONE',  ( 30.75425665345519732, -2.450656702321377001, 6.861505862736165362 ) ) ;
#15810=( BOUNDED_CURVE ( )  B_SPLINE_CURVE ( 2, ( #16400, #5577, #65, #4233, #2609, #8138, #9732, #13834, #8224 ),
 .UNSPECIFIED., .F., .T. ) 
 B_SPLINE_CURVE_WITH_KNOTS ( ( 3, 2, 2, 2, 3 ),
 ( 0.7500000000000000000, 0.7564102564102563875, 0.7692307692307692735, 0.7820512820512820484, 0.7884615384615384359 ),
 .UNSPECIFIED. ) 
 CURVE ( )  GEOMETRIC_REPRESENTATION_ITEM ( )  RATIONAL_B_SPLINE_CURVE ( ( 0.9330127018922194093, 0.9330127018922194093, 1.000000000000000000, 0.8660254037844387076, 1.000000000000000000, 0.8660254037844387076, 1.000000000000000000, 0.9330127018922194093, 0.9330127018922194093 ) ) 
 REPRESENTATION_ITEM ( '' )  );
#15814=CARTESIAN_POINT ( 'NONE',  ( 28.08317206381523334, -7.171460237833785278, 6.453230759126462601 ) ) ;
#15821=ORIENTED_EDGE ( 'NONE', *, *, #2994, .T. ) ;
#15823=CARTESIAN_POINT ( 'NONE',  ( -35.62429925076629189, -17.76690233603958546, 10.53798182577225084 ) ) ;
#15830=CARTESIAN_POINT ( 'NONE',  ( 27.26074174026764751, -6.633379454790151009, 4.705209693361159573 ) ) ;
#15831=ORIENTED_EDGE ( 'NONE', *, *, #17819, .T. ) ;
#15834=( BOUNDED_CURVE ( )  B_SPLINE_CURVE ( 3, ( #7980, #10850, #1008, #9416 ),
 .UNSPECIFIED., .F., .T. ) 
 B_SPLINE_CURVE_WITH_KNOTS ( ( 4, 4 ),
 ( 4.363323129985829496, 4.457746946181837977 ),
 .UNSPECIFIED. ) 
 CURVE ( )  GEOMETRIC_REPRESENTATION_ITEM ( )  RATIONAL_B_SPLINE_CURVE ( ( 1.000000000000000000, 0.9992571499088201969, 0.9992571499088201969, 1.000000000000000000 ) ) 
 REPRESENTATION_ITEM ( '' )  );
#15836=CARTESIAN_POINT ( 'NONE',  ( 33.58707084003705745, -6.498152266226123963, 5.783357778048657138 ) ) ;
#15837=CARTESIAN_POINT ( 'NONE',  ( -25.20502126318114833, -10.36657009486825842, 14.42817146764052083 ) ) ;
#15839=ORIENTED_EDGE ( 'NONE', *, *, #6, .T. ) ;
#15847=DIRECTION ( 'NONE',  ( 0.9928203230275510771, 0.1196152422706609902, 4.006172263299092517E-17 ) ) ;
#15852=AXIS2_PLACEMENT_3D ( 'NONE', #17497, #6298, #9365 ) ;
#15854=CARTESIAN_POINT ( 'NONE',  ( 32.64947922571280259, -7.010858578292532783, 5.783357778048657138 ) ) ;
#15857=AXIS2_PLACEMENT_3D ( 'NONE', #16889, #1291, #15237 ) ;
#15858=PRODUCT_DEFINITION_FORMATION_WITH_SPECIFIED_SOURCE ( 'ANY', '', #9104, .NOT_KNOWN. ) ;
#15861=CARTESIAN_POINT ( 'NONE',  ( 26.79905070906539777, -3.354278923027479209, 8.283357778048666020 ) ) ;
#15862=DIRECTION ( 'NONE',  ( 0.000000000000000000, 0.000000000000000000, 1.000000000000000000 ) ) ;
#15864=VECTOR ( 'NONE', #7290, 1000.000000000000000 ) ;
#15865=DIRECTION ( 'NONE',  ( -1.000000000000000000, 0.000000000000000000, 0.000000000000000000 ) ) ;
#15869=FACE_OUTER_BOUND ( 'NONE', #3237, .T. ) ;
#15873=DIRECTION ( 'NONE',  ( 0.9928203230275510771, 0.1196152422706609902, 4.006172263299092517E-17 ) ) ;
#15877=ORIENTED_EDGE ( 'NONE', *, *, #9266, .F. ) ;
#15880=CARTESIAN_POINT ( 'NONE',  ( 27.29063000668916672, -2.568146533142987575, 7.033357778048666020 ) ) ;
#15881=EDGE_LOOP ( 'NONE', ( #7611, #10808, #3545, #1355 ) ) ;
#15890=AXIS2_PLACEMENT_3D ( 'NONE', #8398, #4324, #11098 ) ;
#15900=LINE ( 'NONE', #5997, #5989 ) ;
#15901=EDGE_CURVE ( 'NONE', #3432, #3677, #1503, .T. ) ;
#15906=CARTESIAN_POINT ( 'NONE',  ( 31.61111609099199171, -1.710254666422835745, 5.783357778048665132 ) ) ;
#15912=CARTESIAN_POINT ( 'NONE',  ( 34.91600907648203389, -11.88801210197604341, 0.000000000000000000 ) ) ;
#15919=DIRECTION ( 'NONE',  ( -0.000000000000000000, 1.000000000000000000, -3.469446951953614189E-16 ) ) ;
#15921=CARTESIAN_POINT ( 'NONE',  ( 27.89118264539014547, -6.557423775948280742, 4.705209693361159573 ) ) ;
#15930=CARTESIAN_POINT ( 'NONE',  ( 25.81100034576892455, -6.186289477007987259, 4.026422103237231376 ) ) ;
#15931=CARTESIAN_POINT ( 'NONE',  ( -21.03265992632394799, -10.27181489424398997, 15.32141966295701430 ) ) ;
#15935=ORIENTED_EDGE ( 'NONE', *, *, #7020, .T. ) ;
#15938=DIRECTION ( 'NONE',  ( -0.000000000000000000, -0.000000000000000000, 1.000000000000000000 ) ) ;
#15947=CARTESIAN_POINT ( 'NONE',  ( 31.32102116884452414, -5.717097954277069682, 3.283357778048663800 ) ) ;
#15956=PLANE ( 'NONE',  #10778 ) ;
#15957=EDGE_CURVE ( 'NONE', #1544, #4537, #5380, .T. ) ;
#15965=DIRECTION ( 'NONE',  ( -1.000000000000000000, 0.000000000000000000, 0.000000000000000000 ) ) ;
#15966=CARTESIAN_POINT ( 'NONE',  ( 9.700633612364448766, 16.10095840566074799, 16.79370834700961979 ) ) ;
#15980=CARTESIAN_POINT ( 'NONE',  ( 26.55511561737958814, -2.656761491791831187, 4.533357778048667797 ) ) ;
#15981=EDGE_LOOP ( 'NONE', ( #5714, #1517, #11946, #322 ) ) ;
#15983=VECTOR ( 'NONE', #12311, 1000.000000000000000 ) ;
#15987=CARTESIAN_POINT ( 'NONE',  ( 5.499998817156067865, -20.49639288455253450, 6.000000000000000000 ) ) ;
#16004=CARTESIAN_POINT ( 'NONE',  ( -20.00000000000000355, 7.999999999999996447, 6.000000000000000000 ) ) ;
#16005=CARTESIAN_POINT ( 'NONE',  ( -35.74085044863416272, -23.57886868891566223, 11.27079897466147607 ) ) ;
#16007=CARTESIAN_POINT ( 'NONE',  ( 25.77386970449396486, -2.888308184441639170, 4.943601421580931188 ) ) ;
#16012=CARTESIAN_POINT ( 'NONE',  ( 33.15485366002904755, -6.560422763297783177, 5.783357778048664244 ) ) ;
#16014=VECTOR ( 'NONE', #10232, 1000.000000000000000 ) ;
#16026=CARTESIAN_POINT ( 'NONE',  ( 26.49878054387835746, -2.963357534503999968, 6.861505862736166250 ) ) ;
#16028=ORIENTED_EDGE ( 'NONE', *, *, #7913, .T. ) ;
#16031=CARTESIAN_POINT ( 'NONE',  ( 31.54230778485832332, -2.355712103769039611, 6.861505862736166250 ) ) ;
#16032=CARTESIAN_POINT ( 'NONE',  ( 28.09753128235661279, -6.832371619143005503, 7.033357778048657138 ) ) ;
#16045=( NAMED_UNIT ( * ) PLANE_ANGLE_UNIT ( ) SI_UNIT ( $, .RADIAN. ) );
#16048=DIRECTION ( 'NONE',  ( -0.000000000000000000, -0.000000000000000000, -1.000000000000000000 ) ) ;
#16050=CARTESIAN_POINT ( 'NONE',  ( 32.27410075503257758, -1.240829931302721345, 5.783357778048668685 ) ) ;
#16051=ORIENTED_EDGE ( 'NONE', *, *, #7413, .F. ) ;
#16055=CARTESIAN_POINT ( 'NONE',  ( 32.08959525433819238, -2.916745304588811205, 3.627061608673666449 ) ) ;
#16065=CARTESIAN_POINT ( 'NONE',  ( 34.91600907648203389, -11.88801210197604341, 12.00000000000000000 ) ) ;
#16067=CARTESIAN_POINT ( 'NONE',  ( 22.22415228291801981, -10.00312865908476567, 15.08655899088414820 ) ) ;
#16071=ORIENTED_EDGE ( 'NONE', *, *, #3114, .T. ) ;
#16076=CARTESIAN_POINT ( 'NONE',  ( 26.32044349065828115, -7.243571858916999950, 4.872287503353643245 ) ) ;
#16094=ORIENTED_EDGE ( 'NONE', *, *, #1356, .F. ) ;
#16095=CARTESIAN_POINT ( 'NONE',  ( -36.27615609941022257, -23.17738945083361557, 12.00000000000000000 ) ) ;
#16097=DIRECTION ( 'NONE',  ( -0.1196152422706597551, 0.9928203230275514102, 0.000000000000000000 ) ) ;
#16098=CARTESIAN_POINT ( 'NONE',  ( 27.22618411036838637, -2.238552374514887866, 6.453230759126474148 ) ) ;
#16100=CARTESIAN_POINT ( 'NONE',  ( 25.94629020164263267, -4.319418220471660241, 3.500307223198195317 ) ) ;
#16101=PLANE ( 'NONE',  #9874 ) ;
#16104=VERTEX_POINT ( 'NONE', #5923 ) ;
#16106=DIRECTION ( 'NONE',  ( -0.9928203230275511881, -0.1196152422706614482, -0.000000000000000000 ) ) ;
#16107=CARTESIAN_POINT ( 'NONE',  ( -34.91600907648203389, -11.88801210197604341, 11.56671555609732671 ) ) ;
#16112=CARTESIAN_POINT ( 'NONE',  ( 33.59503905791412137, -1.808589744724287129, 7.033357778048666020 ) ) ;
#16113=CARTESIAN_POINT ( 'NONE',  ( 25.86833963875586306, -3.039313213345869791, 6.861505862736166250 ) ) ;
#16116=ORIENTED_EDGE ( 'NONE', *, *, #961, .T. ) ;
#16118=CARTESIAN_POINT ( 'NONE',  ( 28.54354359905709870, -7.105797696961086096, 5.783357778048657138 ) ) ;
#16119=CARTESIAN_POINT ( 'NONE',  ( 27.73348320195396965, -4.695511846111656062, 8.283357778048662468 ) ) ;
#16121=ORIENTED_EDGE ( 'NONE', *, *, #9154, .F. ) ;
#16134=CARTESIAN_POINT ( 'NONE',  ( 29.98885399772409954, -6.604504582617394703, 7.033357778048657138 ) ) ;
#16140=CARTESIAN_POINT ( 'NONE',  ( 26.31556265977298992, -7.384422263489805793, 5.783357778048663356 ) ) ;
#16141=CARTESIAN_POINT ( 'NONE',  ( 31.43723430067123914, -2.368371383576012956, 4.705209693361168455 ) ) ;
#16144=CARTESIAN_POINT ( 'NONE',  ( 36.27615609941022257, -23.17738945083361557, 0.000000000000000000 ) ) ;
#16147=CARTESIAN_POINT ( 'NONE',  ( -5.500000000000000888, -20.49999999999999645, 12.00000000000000000 ) ) ;
#16151=CARTESIAN_POINT ( 'NONE',  ( 16.75000000000000000, -16.21813761408365195, 16.03574476417184513 ) ) ;
#16155=ORIENTED_EDGE ( 'NONE', *, *, #15775, .T. ) ;
#16157=CARTESIAN_POINT ( 'NONE',  ( 26.02974819644417792, -2.720057890826728109, 7.033357778048666020 ) ) ;
#16160=VERTEX_POINT ( 'NONE', #14375 ) ;
#16161=CARTESIAN_POINT ( 'NONE',  ( 26.27749392786456895, -6.324743385012030927, 3.283357778048663356 ) ) ;
#16163=ORIENTED_EDGE ( 'NONE', *, *, #16260, .T. ) ;
#16167=DIRECTION ( 'NONE',  ( 0.9928203230275512992, 0.1196152422706610180, 4.006172263299093133E-17 ) ) ;
#16170=AXIS2_PLACEMENT_3D ( 'NONE', #1858, #12807, #304 ) ;
#16174=DIRECTION ( 'NONE',  ( 0.1196152422706596996, -0.9928203230275514102, 0.000000000000000000 ) ) ;
#16182=DIRECTION ( 'NONE',  ( 0.000000000000000000, 1.000000000000000000, 0.000000000000000000 ) ) ;
#16183=CARTESIAN_POINT ( 'NONE',  ( 34.43754810739937966, -7.916730809865823559, 5.783357778048663356 ) ) ;
#16184=VECTOR ( 'NONE', #10568, 1000.000000000000000 ) ;
#16185=EDGE_CURVE ( 'NONE', #5221, #11770, #13420, .T. ) ;
#16186=VERTEX_POINT ( 'NONE', #1596 ) ;
#16187=CARTESIAN_POINT ( 'NONE',  ( 25.88432464927661059, -3.805096980563281939, 3.751875008055423955 ) ) ;
#16188=ADVANCED_FACE ( 'NONE', ( #7128 ), #12639, .F. ) ;
#16191=ORIENTED_EDGE ( 'NONE', *, *, #883, .T. ) ;
#16192=CYLINDRICAL_SURFACE ( 'NONE', #15141, 2.000000000000001776 ) ;
#16195=FACE_OUTER_BOUND ( 'NONE', #2008, .T. ) ;
#16201=CARTESIAN_POINT ( 'NONE',  ( 31.21213704492286212, -2.822589171134389563, 8.283357778048664244 ) ) ;
#16205=CARTESIAN_POINT ( 'NONE',  ( 30.29464937815318493, -4.386941900920275472, 3.627061608673664228 ) ) ;
#16206=CARTESIAN_POINT ( 'NONE',  ( -27.11337801594864061, -11.49512195020015604, 13.95421129451976050 ) ) ;
#16211=DIRECTION ( 'NONE',  ( -1.000000000000000000, 0.000000000000000000, 0.000000000000000000 ) ) ;
#16214=CARTESIAN_POINT ( 'NONE',  ( 31.05948030073166066, -1.776715885202022394, 5.783357778048665132 ) ) ;
#16217=CARTESIAN_POINT ( 'NONE',  ( 27.75549246765397271, -7.200742295513423485, 5.783357778048658027 ) ) ;
#16219=CARTESIAN_POINT ( 'NONE',  ( 33.18226487515251932, -2.585227674546096477, 8.283357778048666020 ) ) ;
#16221=CARTESIAN_POINT ( 'NONE',  ( 28.76917853929504432, -3.116917426439186123, 8.283357778048664244 ) ) ;
#16224=VERTEX_POINT ( 'NONE', #11723 ) ;
#16225=CARTESIAN_POINT ( 'NONE',  ( 32.54050588463559990, -2.235448945602741766, 4.705209693361167567 ) ) ;
#16226=VECTOR ( 'NONE', #17017, 1000.000000000000000 ) ;
#16227=CARTESIAN_POINT ( 'NONE',  ( 31.67382807612511542, -6.101689702897060030, 4.705209693361159573 ) ) ;
#16228=ORIENTED_EDGE ( 'NONE', *, *, #16719, .T. ) ;
#16231=DIRECTION ( 'NONE',  ( -0.9928203230275511881, -0.1196152422706610041, -4.006172263299093133E-17 ) ) ;
#16239=CARTESIAN_POINT ( 'NONE',  ( 29.71979337562451207, -1.938121702948446323, 5.783357778048662468 ) ) ;
#16241=VERTEX_POINT ( 'NONE', #15912 ) ;
#16246=CARTESIAN_POINT ( 'NONE',  ( 31.29094215978502902, -2.813094711071706389, 8.283357778048666020 ) ) ;
#16248=EDGE_LOOP ( 'NONE', ( #13312, #2140, #13663, #13056 ) ) ;
#16249=CARTESIAN_POINT ( 'NONE',  ( 30.64918316926811315, -2.463315982128351678, 4.705209693361167567 ) ) ;
#16251=CARTESIAN_POINT ( 'NONE',  ( -14.00000000000000178, 0.000000000000000000, 8.700000000000001066 ) ) ;
#16254=CARTESIAN_POINT ( 'NONE',  ( 25.95642634701329499, -4.403549397486667516, 7.880302681851837576 ) ) ;
#16257=ADVANCED_FACE ( 'NONE', ( #14466 ), #16192, .F. ) ;
#16260=EDGE_CURVE ( 'NONE', #13000, #10514, #14582, .T. ) ;
#16270=CIRCLE ( 'NONE', #6695, 2.000000000000001776 ) ;
#16272=FACE_OUTER_BOUND ( 'NONE', #2821, .T. ) ;
#16274=ORIENTED_EDGE ( 'NONE', *, *, #5934, .T. ) ;
#16287=CARTESIAN_POINT ( 'NONE',  ( 33.40745134805642635, -4.011910736534825439, 8.283357778048662468 ) ) ;
#16288=CARTESIAN_POINT ( 'NONE',  ( 32.50309786422735669, -5.574681056656012323, 3.283357778048663800 ) ) ;
#16289=EDGE_CURVE ( 'NONE', #9288, #8961, #13512, .T. ) ;
#16291=ORIENTED_EDGE ( 'NONE', *, *, #5483, .F. ) ;
#16292=CARTESIAN_POINT ( 'NONE',  ( 29.67743187657054449, -6.342216019229654833, 6.861505862736157368 ) ) ;
#16294=CARTESIAN_POINT ( 'NONE',  ( 21.03881409870396624, -22.15596512169676302, 15.31966522629967464 ) ) ;
#16295=ORIENTED_EDGE ( 'NONE', *, *, #10315, .F. ) ;
#16301=ORIENTED_EDGE ( 'NONE', *, *, #3605, .F. ) ;
#16304=CARTESIAN_POINT ( 'NONE',  ( 27.82847066025702887, -2.165988739474055791, 5.783357778048667797 ) ) ;
#16306=CARTESIAN_POINT ( 'NONE',  ( 26.24062359194589078, -6.129313013101781671, 7.939653947423658487 ) ) ;
#16307=CIRCLE ( 'NONE', #1247, 2.749999999999995559 ) ;
#16311=DIRECTION ( 'NONE',  ( 0.000000000000000000, 0.000000000000000000, -1.000000000000000000 ) ) ;
#16313=CARTESIAN_POINT ( 'NONE',  ( 28.83304567166618781, -6.743756660494150346, 4.533357778048659803 ) ) ;
#16318=CARTESIAN_POINT ( 'NONE',  ( 30.75425665345519732, -2.450656702321377001, 6.861505862736165362 ) ) ;
#16321=CARTESIAN_POINT ( 'NONE',  ( 29.56783163384821833, -3.220568019956291383, 3.627061608673666449 ) ) ;
#16323=PLANE ( 'NONE',  #6327 ) ;
#16324=CARTESIAN_POINT ( 'NONE',  ( 32.69820532807177216, -4.097360875439379768, 8.283357778048662468 ) ) ;
#16329=ORIENTED_EDGE ( 'NONE', *, *, #8106, .T. ) ;
#16334=CARTESIAN_POINT ( 'NONE',  ( 16.75000000000000000, -15.80031936969768935, 16.03574476417183803 ) ) ;
#16336=ORIENTED_EDGE ( 'NONE', *, *, #12076, .T. ) ;
#16339=ORIENTED_EDGE ( 'NONE', *, *, #17955, .T. ) ;
#16343=AXIS2_PLACEMENT_3D ( 'NONE', #8879, #14605, #11949 ) ;
#16347=CARTESIAN_POINT ( 'NONE',  ( 32.02836186724004364, -4.178063784105134459, 3.627061608673664228 ) ) ;
#16363=B_SPLINE_CURVE_WITH_KNOTS ( 'NONE', 3,
 ( #1575, #2100, #7623, #6249, #11771, #3535, #17061, #636, #15966, #15342, #12622, #4615, #4284, #203 ),
 .UNSPECIFIED., .F., .F.,
 ( 4, 2, 2, 2, 2, 2, 4 ),
 ( 0.000000000000000000, 0.004968481363098090076, 0.007452722044647132511, 0.009936962726196174947, 0.01490544408929426155, 0.01738968477084330486, 0.01987392545239234642 ),
 .UNSPECIFIED. ) ;
#16365=ORIENTED_EDGE ( 'NONE', *, *, #12252, .F. ) ;
#16370=FACE_OUTER_BOUND ( 'NONE', #12346, .T. ) ;
#16376=CARTESIAN_POINT ( 'NONE',  ( 30.49166216014303643, -4.363205751385915931, 3.283357778048664244 ) ) ;
#16378=ADVANCED_FACE ( 'NONE', ( #9701 ), #10793, .F. ) ;
#16379=CARTESIAN_POINT ( 'NONE',  ( 28.26310972651430120, -2.123820177930694442, 5.783357778048668685 ) ) ;
#16380=CARTESIAN_POINT ( 'NONE',  ( -18.05564684537134568, -12.37312016356480449, 15.83930707548887895 ) ) ;
#16381=CARTESIAN_POINT ( 'NONE',  ( 18.06124445020232727, -20.07065898529088344, 15.83842874644866505 ) ) ;
#16382=VERTEX_POINT ( 'NONE', #1388 ) ;
#16385=ORIENTED_EDGE ( 'NONE', *, *, #10713, .T. ) ;
#16386=VERTEX_POINT ( 'NONE', #17751 ) ;
#16390=CARTESIAN_POINT ( 'NONE',  ( 26.35439372113758694, -4.861664893681965083, 3.627061608673664228 ) ) ;
#16391=CARTESIAN_POINT ( 'NONE',  ( 29.60297508593253468, -5.724216059278466773, 3.627061608673662896 ) ) ;
#16393=CARTESIAN_POINT ( 'NONE',  ( 32.55256711014040150, -6.632986398338614364, 5.113484796970852564 ) ) ;
#16395=CARTESIAN_POINT ( 'NONE',  ( 28.09753128235661279, -6.832371619143005503, 7.033357778048657138 ) ) ;
#16399=CARTESIAN_POINT ( 'NONE',  ( 30.67110321781257909, -3.087645581983020637, 3.627061608673666893 ) ) ;
#16400=CARTESIAN_POINT ( 'NONE',  ( 27.55969062878875064, -7.234529412811931515, 5.783357778048657138 ) ) ;
#16401=CARTESIAN_POINT ( 'NONE',  ( 30.41294626588012306, -6.253601060580800564, 4.705209693361159573 ) ) ;
#16404=DIRECTION ( 'NONE',  ( 0.9928203230275511881, 0.1196152422706614482, 0.000000000000000000 ) ) ;
#16408=CARTESIAN_POINT ( 'NONE',  ( 33.95908713831673964, -3.945449517755637903, 5.783357778048663356 ) ) ;
#16409=ADVANCED_FACE ( 'NONE', ( #9532, #16447 ), #4016, .T. ) ;
#16410=PLANE ( 'NONE',  #12265 ) ;
#16422=CARTESIAN_POINT ( 'NONE',  ( 33.17547354829333983, -5.293800545841212291, 7.939653947423658487 ) ) ;
#16428=CARTESIAN_POINT ( 'NONE',  ( 32.60321786976872005, -6.626883982076972934, 5.783357778048664244 ) ) ;
#16430=CARTESIAN_POINT ( 'NONE',  ( 3.538288549924106796, -15.34800872113743431, 13.00000000000000178 ) ) ;
#16434=DIRECTION ( 'NONE',  ( 0.000000000000000000, 0.000000000000000000, -1.000000000000000000 ) ) ;
#16440=EDGE_LOOP ( 'NONE', ( #17043, #600, #6191, #8903 ) ) ;
#16443=ORIENTED_EDGE ( 'NONE', *, *, #8234, .T. ) ;
#16447=FACE_OUTER_BOUND ( 'NONE', #14275, .T. ) ;
#16451=ADVANCED_FACE ( 'NONE', ( #16370, #8194 ), #3850, .F. ) ;
#16455=CARTESIAN_POINT ( 'NONE',  ( 29.37220822929407760, -7.016156836349003001, 5.783357778048657138 ) ) ;
#16458=CARTESIAN_POINT ( 'NONE',  ( 30.17635249042624679, -2.520282741259753045, 4.705209693361168455 ) ) ;
#16459=CARTESIAN_POINT ( 'NONE',  ( -16.75000000000000355, -15.80559819018441381, 16.03574476417185934 ) ) ;
#16460=CARTESIAN_POINT ( 'NONE',  ( 17.40734525178378078, -19.01589366988068974, 15.93907283187074775 ) ) ;
#16465=DIRECTION ( 'NONE',  ( 0.9928203230275510771, 0.1196152422706609902, 4.006172263299092517E-17 ) ) ;
#16471=CARTESIAN_POINT ( 'NONE',  ( 28.35948656569675919, -3.366149737736551906, 7.939653947423664704 ) ) ;
#16477=ADVANCED_FACE ( 'NONE', ( #6733 ), #28, .F. ) ;
#16480=CARTESIAN_POINT ( 'NONE',  ( 31.91006497951310550, -2.311404624444611589, 4.705209693361167567 ) ) ;
#16481=LINE ( 'NONE', #11094, #4120 ) ;
#16483=CARTESIAN_POINT ( 'NONE',  ( 28.51709679197738723, -3.347160818026084339, 7.939653947423662927 ) ) ;
#16494=ADVANCED_FACE ( 'NONE', ( #13632 ), #13803, .F. ) ;
#16497=LINE ( 'NONE', #13516, #11814 ) ;
#16498=DIRECTION ( 'NONE',  ( -1.000000000000000000, 0.000000000000000000, 0.000000000000000000 ) ) ;
#16500=ADVANCED_FACE ( 'NONE', ( #5449, #10970 ), #16531, .T. ) ;
#16504=CARTESIAN_POINT ( 'NONE',  ( 32.75517961154501023, -5.344437665069116328, 3.627061608673662896 ) ) ;
#16506=DIRECTION ( 'NONE',  ( 0.000000000000000000, 0.000000000000000000, -1.000000000000000000 ) ) ;
#16507=DIRECTION ( 'NONE',  ( 0.000000000000000000, 1.000000000000000000, -0.000000000000000000 ) ) ;
#16517=CYLINDRICAL_SURFACE ( 'NONE', #14977, 1.000000000000000000 ) ;
#16521=( BOUNDED_CURVE ( )  B_SPLINE_CURVE ( 2, ( #9963, #9870, #5976, #1464, #14251, #384, #3010, #4453, #5891 ),
 .UNSPECIFIED., .F., .T. ) 
 B_SPLINE_CURVE_WITH_KNOTS ( ( 3, 2, 2, 2, 3 ),
 ( 0.6730769230769231282, 0.6794871794871795156, 0.6923076923076922906, 0.7051282051282051766, 0.7115384615384615641 ),
 .UNSPECIFIED. ) 
 CURVE ( )  GEOMETRIC_REPRESENTATION_ITEM ( )  RATIONAL_B_SPLINE_CURVE ( ( 0.9330127018922192983, 0.9330127018922198534, 1.000000000000000000, 0.8660254037844387076, 1.000000000000000000, 0.8660254037844387076, 1.000000000000000000, 0.9330127018922194093, 0.9330127018922194093 ) ) 
 REPRESENTATION_ITEM ( '' )  );
#16522=VECTOR ( 'NONE', #2260, 1000.000000000000000 ) ;
#16525=EDGE_CURVE ( 'NONE', #6659, #14281, #8271, .T. ) ;
#16526=ORIENTED_EDGE ( 'NONE', *, *, #11293, .T. ) ;
#16528=ORIENTED_EDGE ( 'NONE', *, *, #15110, .T. ) ;
#16530=( GEOMETRIC_REPRESENTATION_CONTEXT ( 3 ) GLOBAL_UNCERTAINTY_ASSIGNED_CONTEXT ( ( #15690 ) ) GLOBAL_UNIT_ASSIGNED_CONTEXT ( ( #14317, #1900, #12760 ) ) REPRESENTATION_CONTEXT ( 'NONE', 'WORKASPACE' ) );
#16531=PLANE ( 'NONE',  #14553 ) ;
#16538=ORIENTED_EDGE ( 'NONE', *, *, #9524, .F. ) ;
#16540=ADVANCED_FACE ( 'NONE', ( #4706 ), #17254, .T. ) ;
#16541=DIRECTION ( 'NONE',  ( -0.000000000000000000, -0.000000000000000000, 1.000000000000000000 ) ) ;
#16543=DIRECTION ( 'NONE',  ( -0.000000000000000000, -0.000000000000000000, -1.000000000000000000 ) ) ;
#16544=ORIENTED_EDGE ( 'NONE', *, *, #4540, .T. ) ;
#16547=ORIENTED_EDGE ( 'NONE', *, *, #5941, .T. ) ;
#16550=VECTOR ( 'NONE', #10411, 1000.000000000000114 ) ;
#16552=FACE_OUTER_BOUND ( 'NONE', #5682, .T. ) ;
#16553=CARTESIAN_POINT ( 'NONE',  ( 29.74110826630371207, -2.999819088432076786, 3.283357778048666464 ) ) ;
#16556=CARTESIAN_POINT ( 'NONE',  ( 30.27725608814395031, -6.896919580145944195, 5.783357778048658027 ) ) ;
#16560=CARTESIAN_POINT ( 'NONE',  ( 33.43363050022580296, -2.127845067243429256, 6.861505862736166250 ) ) ;
#16566=ORIENTED_EDGE ( 'NONE', *, *, #11645, .F. ) ;
#16567=EDGE_CURVE ( 'NONE', #2813, #12087, #16363, .T. ) ;
#16568=CARTESIAN_POINT ( 'NONE',  ( 27.75549246765397271, -7.200742295513423485, 5.783357778048658027 ) ) ;
#16569=LINE ( 'NONE', #12217, #12223 ) ;
#16572=LINE ( 'NONE', #17956, #7500 ) ;
#16576=VECTOR ( 'NONE', #6200, 1000.000000000000000 ) ;
#16577=CARTESIAN_POINT ( 'NONE',  ( 29.95125523467787332, -2.974500528818129652, 8.283357778048666020 ) ) ;
#16581=CARTESIAN_POINT ( 'NONE',  ( 33.95908713831673964, -3.945449517755648561, 5.783357778048663356 ) ) ;
#16582=EDGE_CURVE ( 'NONE', #3948, #17429, #1919, .T. ) ;
#16588=CARTESIAN_POINT ( 'NONE',  ( 33.40745134805642635, -4.011910736534825439, 8.283357778048662468 ) ) ;
#16589=DIRECTION ( 'NONE',  ( 0.9928203230275512992, 0.1196152422706587698, 0.000000000000000000 ) ) ;
#16591=ORIENTED_EDGE ( 'NONE', *, *, #15420, .T. ) ;
#16594=DIRECTION ( 'NONE',  ( 0.9928203230275510771, 0.1196152422706609902, 4.006172263299092517E-17 ) ) ;
#16597=DIRECTION ( 'NONE',  ( 0.000000000000000000, 0.000000000000000000, -1.000000000000000000 ) ) ;
#16602=CARTESIAN_POINT ( 'NONE',  ( 32.32036211097666012, -1.624804527518282748, 5.783357778048663356 ) ) ;
#16610=DIRECTION ( 'NONE',  ( -0.1414213562373112243, -0.9899494936611663576, 0.000000000000000000 ) ) ;
#16619=CIRCLE ( 'NONE', #17809, 6.249999999999998224 ) ;
#16623=CARTESIAN_POINT ( 'NONE',  ( 23.00000000000000000, -16.21813761408365195, 13.00000000000000178 ) ) ;
#16624=EDGE_CURVE ( 'NONE', #4518, #11059, #4881, .T. ) ;
#16628=CARTESIAN_POINT ( 'NONE',  ( 32.14656953781143756, -4.163822094218565972, 8.283357778048662468 ) ) ;
#16634=CARTESIAN_POINT ( 'NONE',  ( 26.82722439997946395, -4.804698134550569044, 7.939653947423662039 ) ) ;
#16635=CYLINDRICAL_SURFACE ( 'NONE', #13342, 13.00000000000000178 ) ;
#16636=DIRECTION ( 'NONE',  ( -0.000000000000000000, -1.000000000000000000, -0.000000000000000000 ) ) ;
#16639=CARTESIAN_POINT ( 'NONE',  ( 28.53771668024168662, -2.080538600569502794, 5.783357778048667797 ) ) ;
#16641=DIRECTION ( 'NONE',  ( 1.000000000000000000, -1.734723475976805517E-15, 0.000000000000000000 ) ) ;
#16645=ORIENTED_EDGE ( 'NONE', *, *, #5941, .F. ) ;
#16650=CARTESIAN_POINT ( 'NONE',  ( 28.23249303296521617, -2.754479417688857179, 6.861505862736165362 ) ) ;
#16654=CARTESIAN_POINT ( 'NONE',  ( -2.016448651773435938E-27, -20.49999999999999645, 13.00000000000000355 ) ) ;
#16656=ORIENTED_EDGE ( 'NONE', *, *, #11645, .T. ) ;
#16658=CARTESIAN_POINT ( 'NONE',  ( 27.12505156253147476, -7.276697974355294640, 5.783357778048658027 ) ) ;
#16660=EDGE_CURVE ( 'NONE', #225, #2070, #10522, .T. ) ;
#16662=CARTESIAN_POINT ( 'NONE',  ( 26.63030083514515312, -6.709335133632020387, 4.705209693361159573 ) ) ;
#16664=EDGE_LOOP ( 'NONE', ( #7148, #5482, #9545, #11458, #7944 ) ) ;
#16670=CARTESIAN_POINT ( 'NONE',  ( -15.92260893619738837, -28.39189527176317540, 6.000000000000000000 ) ) ;
#16676=EDGE_CURVE ( 'NONE', #3230, #13090, #16619, .T. ) ;
#16677=ADVANCED_FACE ( 'NONE', ( #7705, #10503 ), #16410, .T. ) ;
#16682=EDGE_LOOP ( 'NONE', ( #16116, #16329, #6378, #15597 ) ) ;
#16683=CARTESIAN_POINT ( 'NONE',  ( 30.15026255541241440, -6.285249260098253465, 6.861505862736158257 ) ) ;
#16686=LINE ( 'NONE', #11203, #15332 ) ;
#16690=CARTESIAN_POINT ( 'NONE',  ( 0.000000000000000000, 0.000000000000000000, 6.000000000000000000 ) ) ;
#16700=CARTESIAN_POINT ( 'NONE',  ( 30.33776104811456165, -2.201027418740610919, 4.533357778048667797 ) ) ;
#16706=CARTESIAN_POINT ( 'NONE',  ( 7.499998387031003411, -20.49508120620799900, 12.00000000000000000 ) ) ;
#16719=EDGE_CURVE ( 'NONE', #10789, #2247, #15651, .T. ) ;
#16720=ORIENTED_EDGE ( 'NONE', *, *, #8934, .F. ) ;
#16721=CARTESIAN_POINT ( 'NONE',  ( 29.30958546476020743, -4.505622649006972402, 3.283357778048664244 ) ) ;
#16722=EDGE_CURVE ( 'NONE', #13752, #14031, #15057, .T. ) ;
#16724=CARTESIAN_POINT ( 'NONE',  ( 26.39823381822651882, -6.110324093391315436, 7.939653947423658487 ) ) ;
#16727=ORIENTED_EDGE ( 'NONE', *, *, #12056, .F. ) ;
#16738=CARTESIAN_POINT ( 'NONE',  ( 29.49337484321020497, -2.602568060005117090, 6.861505862736165362 ) ) ;
#16740=CARTESIAN_POINT ( 'NONE',  ( 31.89397184978405519, -6.712334120981523711, 5.783357778048664244 ) ) ;
#16742=CARTESIAN_POINT ( 'NONE',  ( 31.87075164095941915, -4.197052703815608687, 7.939653947423662039 ) ) ;
#16746=CARTESIAN_POINT ( 'NONE',  ( 29.62489513447700062, -6.348545659133139729, 4.705209693361160461 ) ) ;
#16750=CARTESIAN_POINT ( 'NONE',  ( 26.19678349485696955, -4.880653813392439311, 7.939653947423662039 ) ) ;
#16751=DIRECTION ( 'NONE',  ( -0.000000000000000000, -0.000000000000000000, 1.000000000000000000 ) ) ;
#16753=CARTESIAN_POINT ( 'NONE',  ( 26.31556265977298992, -7.384422263489805793, 5.783357778048663356 ) ) ;
#16761=PRESENTATION_STYLE_ASSIGNMENT (( #17138 ) ) ;
#16763=ORIENTED_EDGE ( 'NONE', *, *, #4209, .F. ) ;
#16766=VECTOR ( 'NONE', #5435, 1000.000000000000000 ) ;
#16769=ORIENTED_EDGE ( 'NONE', *, *, #9212, .F. ) ;
#16770=CARTESIAN_POINT ( 'NONE',  ( 30.25080928106424594, -3.138282701210941994, 7.939653947423662927 ) ) ;
#16780=ADVANCED_FACE ( 'NONE', ( #4100 ), #12164, .T. ) ;
#16786=ORIENTED_EDGE ( 'NONE', *, *, #16660, .T. ) ;
#16789=LINE ( 'NONE', #4452, #8633 ) ;
#16794=CARTESIAN_POINT ( 'NONE',  ( 30.80688261270428541, -4.325227911964988792, 8.283357778048662468 ) ) ;
#16796=AXIS2_PLACEMENT_3D ( 'NONE', #2728, #15228, #16506 ) ;
#16798=ORIENTED_EDGE ( 'NONE', *, *, #14304, .F. ) ;
#16801=EDGE_CURVE ( 'NONE', #8474, #7363, #1210, .T. ) ;
#16804=ORIENTED_EDGE ( 'NONE', *, *, #17955, .F. ) ;
#16805=VECTOR ( 'NONE', #6295, 1000.000000000000227 ) ;
#16812=EDGE_CURVE ( 'NONE', #14428, #13470, #13150, .T. ) ;
#16818=CARTESIAN_POINT ( 'NONE',  ( 33.19286683830256379, -2.783822866615540903, 3.627061608673666893 ) ) ;
#16819=CARTESIAN_POINT ( 'NONE',  ( 27.25621498173240198, -3.499072175709823984, 7.939653947423664704 ) ) ;
#16820=CARTESIAN_POINT ( 'NONE',  ( -17.40358024347774091, -19.00834140588416332, 15.93963985190277910 ) ) ;
#16833=DIRECTION ( 'NONE',  ( -0.1196152422706610735, 0.9928203230275511881, 0.000000000000000000 ) ) ;
#16837=CARTESIAN_POINT ( 'NONE',  ( 32.87199790123699472, -1.558343308739095656, 5.783357778048663356 ) ) ;
#16841=CARTESIAN_POINT ( 'NONE',  ( 29.56783163384821833, -3.220568019956291383, 3.627061608673666893 ) ) ;
#16845=CARTESIAN_POINT ( 'NONE',  ( 27.51889869220010354, -3.467423976192371082, 3.627061608673666893 ) ) ;
#16846=DIRECTION ( 'NONE',  ( -0.1196152422706610735, 0.9928203230275511881, 0.000000000000000000 ) ) ;
#16849=CARTESIAN_POINT ( 'NONE',  ( 26.52522735095806894, -6.721994413439005278, 6.861505862736157368 ) ) ;
#16854=CARTESIAN_POINT ( 'NONE',  ( 29.42285898892238549, -7.010054420087358018, 6.453230759126468818 ) ) ;
#16864=AXIS2_PLACEMENT_3D ( 'NONE', #10865, #1461, #4356 ) ;
#16870=ORIENTED_EDGE ( 'NONE', *, *, #6385, .F. ) ;
#16872=VERTEX_POINT ( 'NONE', #12264 ) ;
#16873=CARTESIAN_POINT ( 'NONE',  ( 26.97161122272022382, -2.906390775372597712, 6.861505862736165362 ) ) ;
#16877=CARTESIAN_POINT ( 'NONE',  ( -23.00000000000000000, -16.21813761408365195, 13.00000000000000178 ) ) ;
#16881=PLANE ( 'NONE',  #4361 ) ;
#16883=AXIS2_PLACEMENT_3D ( 'NONE', #9492, #13847, #10664 ) ;
#16888=CARTESIAN_POINT ( 'NONE',  ( -20.00000000000000000, 7.999999999999996447, 15.51150668642334374 ) ) ;
#16889=CARTESIAN_POINT ( 'NONE',  ( 25.11802603177690330, -19.03270077640483038, 0.5379818257722508434 ) ) ;
#16892=CARTESIAN_POINT ( 'NONE',  ( 26.85044460880409645, -7.319979551716484067, 5.783357778048657138 ) ) ;
#16894=EDGE_CURVE ( 'NONE', #17327, #16872, #8266, .T. ) ;
#16895=CARTESIAN_POINT ( 'NONE',  ( 29.11066736118121057, -3.075774767273946608, 3.283357778048666464 ) ) ;
#16898=ORIENTED_EDGE ( 'NONE', *, *, #17864, .T. ) ;
#16912=CARTESIAN_POINT ( 'NONE',  ( 27.50903986916043920, -7.240631829073577386, 5.113484796970857005 ) ) ;
#16916=ORIENTED_EDGE ( 'NONE', *, *, #11922, .T. ) ;
#16917=CARTESIAN_POINT ( 'NONE',  ( 32.01513846370018967, -2.298745344637636912, 6.861505862736165362 ) ) ;
#16918=CARTESIAN_POINT ( 'NONE',  ( 27.86926259684567597, -5.933094176093606897, 3.627061608673662896 ) ) ;
#16919=CARTESIAN_POINT ( 'NONE',  ( -29.25000000000000000, -16.63595338719256844, 13.37255996287877124 ) ) ;
#16921=ORIENTED_EDGE ( 'NONE', *, *, #6696, .T. ) ;
#16924=EDGE_LOOP ( 'NONE', ( #15198, #1771, #8815, #13515 ) ) ;
#16930=FACE_OUTER_BOUND ( 'NONE', #12926, .T. ) ;
#16935=CARTESIAN_POINT ( 'NONE',  ( 30.60986983071443390, -4.348964061499348333, 7.939653947423662039 ) ) ;
#16939=CARTESIAN_POINT ( 'NONE',  ( 27.09860475545177039, -3.518061095420291995, 7.939653947423664704 ) ) ;
#16941=DIRECTION ( 'NONE',  ( -1.000000000000000000, 0.000000000000000000, 0.000000000000000000 ) ) ;
#16944=CARTESIAN_POINT ( 'NONE',  ( 26.51200394741821498, -4.842675973971495296, 3.627061608673664228 ) ) ;
#16946=ORIENTED_EDGE ( 'NONE', *, *, #1611, .F. ) ;
#16947=CARTESIAN_POINT ( 'NONE',  ( 36.27615609941022257, -23.17738945083361557, 0.000000000000000000 ) ) ;
#16961=CARTESIAN_POINT ( 'NONE',  ( 29.38830135902312080, -2.615227339812091767, 4.705209693361167567 ) ) ;
#16962=EDGE_CURVE ( 'NONE', #2920, #10340, #7733, .T. ) ;
#16963=CARTESIAN_POINT ( 'NONE',  ( -20.00000000000000355, 7.999999999999996447, 0.000000000000000000 ) ) ;
#16964=DIRECTION ( 'NONE',  ( -0.000000000000000000, -1.000000000000000000, -0.000000000000000000 ) ) ;
#16973=ORIENTED_EDGE ( 'NONE', *, *, #6097, .T. ) ;
#16976=CARTESIAN_POINT ( 'NONE',  ( 34.91600907648203389, -11.88801210197604341, 12.00000000000000000 ) ) ;
#16978=CARTESIAN_POINT ( 'NONE',  ( 26.16860980394290337, -3.430234601869349920, 8.283357778048666020 ) ) ;
#16980=CARTESIAN_POINT ( 'NONE',  ( 28.78802868011566929, -7.476087111406434893, 5.783357778048657138 ) ) ;
#16982=ORIENTED_EDGE ( 'NONE', *, *, #17544, .T. ) ;
#16986=ORIENTED_EDGE ( 'NONE', *, *, #4996, .T. ) ;
#17002=CARTESIAN_POINT ( 'NONE',  ( 31.71314141467879111, -4.216041623526076698, 7.939653947423662039 ) ) ;
#17004=CARTESIAN_POINT ( 'NONE',  ( -23.43613571611706803, -22.46619466838626877, 14.83130101496670861 ) ) ;
#17009=DIRECTION ( 'NONE',  ( 0.9928203230275512992, 0.1196152422706610180, 4.006172263299093133E-17 ) ) ;
#17011=EDGE_CURVE ( 'NONE', #5885, #9480, #9560, .T. ) ;
#17017=DIRECTION ( 'NONE',  ( 0.000000000000000000, 0.000000000000000000, -1.000000000000000000 ) ) ;
#17023=CARTESIAN_POINT ( 'NONE',  ( 33.69269431359690969, -6.158264969628857166, 7.033357778048657138 ) ) ;
#17024=CARTESIAN_POINT ( 'NONE',  ( 29.17398450417959310, -7.029842018119214941, 5.783357778048657138 ) ) ;
#17026=ORIENTED_EDGE ( 'NONE', *, *, #17, .F. ) ;
#17029=CARTESIAN_POINT ( 'NONE',  ( 31.43723430067123914, -2.368371383576012956, 4.705209693361168455 ) ) ;
#17030=DIRECTION ( 'NONE',  ( -1.000000000000000000, 0.000000000000000000, 0.000000000000000000 ) ) ;
#17031=FACE_OUTER_BOUND ( 'NONE', #1128, .T. ) ;
#17033=CARTESIAN_POINT ( 'NONE',  ( 27.29814976067589072, -3.294147343736874234, 3.283357778048666464 ) ) ;
#17038=CIRCLE ( 'NONE', #4282, 14.00000000000000178 ) ;
#17039=CARTESIAN_POINT ( 'NONE',  ( 29.03578327489625011, -17.85349083735938081, 13.43326801114178615 ) ) ;
#17043=ORIENTED_EDGE ( 'NONE', *, *, #3192, .F. ) ;
#17045=CARTESIAN_POINT ( 'NONE',  ( -45.00000000000000711, 0.000000000000000000, 5.537981825772250843 ) ) ;
#17046=CARTESIAN_POINT ( 'NONE',  ( 31.08079519141086777, -2.838413270685653078, 3.283357778048666464 ) ) ;
#17049=ORIENTED_EDGE ( 'NONE', *, *, #14455, .T. ) ;
#17050=AXIS2_PLACEMENT_3D ( 'NONE', #12071, #16182, #11898 ) ;
#17052=CARTESIAN_POINT ( 'NONE',  ( 29.39282811755836988, -5.749534618892433002, 7.939653947423658487 ) ) ;
#17054=CARTESIAN_POINT ( 'NONE',  ( 31.89397184978405519, -6.712334120981523711, 5.783357778048664244 ) ) ;
#17056=CYLINDRICAL_SURFACE ( 'NONE', #5772, 6.249999999999998224 ) ;
#17061=CARTESIAN_POINT ( 'NONE',  ( 13.34918303132433692, 14.15390528054681596, 16.46429318744779025 ) ) ;
#17064=CARTESIAN_POINT ( 'NONE',  ( -6.528882441595574626, 17.18907124314410950, 16.95629972507819971 ) ) ;
#17065=CIRCLE ( 'NONE', #8946, 2.749999999999988454 ) ;
#17069=CARTESIAN_POINT ( 'NONE',  ( -9.099998387031003944, -19.29508120620799616, 16.81964500401478091 ) ) ;
#17071=ADVANCED_FACE ( 'NONE', ( #5618 ), #1749, .F. ) ;
#17073=CARTESIAN_POINT ( 'NONE',  ( 29.18195272205665347, -2.340279496617377664, 7.033357778048666020 ) ) ;
#17081=DIRECTION ( 'NONE',  ( 1.000000000000000000, 0.000000000000000000, 0.000000000000000000 ) ) ;
#17084=AXIS2_PLACEMENT_3D ( 'NONE', #8929, #954, #3935 ) ;
#17092=CIRCLE ( 'NONE', #16796, 2.749999999999988454 ) ;
#17093=DIRECTION ( 'NONE',  ( -0.000000000000000000, -1.000000000000000000, -0.000000000000000000 ) ) ;
#17094=CARTESIAN_POINT ( 'NONE',  ( 33.17094678975809074, -2.159493266760871499, 4.705209693361167567 ) ) ;
#17095=EDGE_CURVE ( 'NONE', #9480, #7391, #11323, .T. ) ;
#17099=CARTESIAN_POINT ( 'NONE',  ( -17.22607755114822226, -18.63699807132245212, 15.96626374682043981 ) ) ;
#17100=FACE_OUTER_BOUND ( 'NONE', #4602, .T. ) ;
#17110=CARTESIAN_POINT ( 'NONE',  ( -2.016448651773435938E-27, -20.49999999999999645, 13.00000000000000178 ) ) ;
#17116=CARTESIAN_POINT ( 'NONE',  ( 30.43486631442457835, -6.877930660435475296, 5.783357778048657138 ) ) ;
#17123=CARTESIAN_POINT ( 'NONE',  ( 32.80318959510331212, -2.203800746085299522, 6.861505862736166250 ) ) ;
#17125=CARTESIAN_POINT ( 'NONE',  ( -7.499998387031003411, -20.49508120620799900, 6.000000000000000000 ) ) ;
#17126=VECTOR ( 'NONE', #3304, 1000.000000000000000 ) ;
#17127=EDGE_LOOP ( 'NONE', ( #12607, #797 ) ) ;
#17133=CARTESIAN_POINT ( 'NONE',  ( 32.83754810739938534, -9.116730809865837060, -4.216642221951339309 ) ) ;
#17134=VECTOR ( 'NONE', #13230, 1000.000000000000000 ) ;
#17138=SURFACE_STYLE_USAGE ( .BOTH. , #11190 ) ;
#17141=AXIS2_PLACEMENT_3D ( 'NONE', #827, #6358, #11880 ) ;
#17142=CARTESIAN_POINT ( 'NONE',  ( 27.17934203385504333, -30.00000000000000355, 13.93658524716016878 ) ) ;
#17143=CARTESIAN_POINT ( 'NONE',  ( 32.77701044293393551, -4.087866415376695706, 8.283357778048662468 ) ) ;
#17144=EDGE_CURVE ( 'NONE', #15247, #17612, #14681, .T. ) ;
#17146=AXIS2_PLACEMENT_3D ( 'NONE', #16706, #12702, #5804 ) ;
#17148=CARTESIAN_POINT ( 'NONE',  ( 25.95642634701329499, -4.403549397486667516, 7.880302681851837576 ) ) ;
#17149=CARTESIAN_POINT ( 'NONE',  ( 33.56062403295735663, -2.739515387291123982, 7.939653947423662927 ) ) ;
#17150=SURFACE_STYLE_USAGE ( .BOTH. , #17336 ) ;
#17154=CIRCLE ( 'NONE', #6110, 5.000000000000000000 ) ;
#17159=CARTESIAN_POINT ( 'NONE',  ( -36.07773319708005744, -23.32620662758124297, 11.14818368178938357 ) ) ;
#17164=DIRECTION ( 'NONE',  ( 0.9928203230275512992, 0.1196152422706610180, 4.006172263299093133E-17 ) ) ;
#17167=CARTESIAN_POINT ( 'NONE',  ( 29.38468146192651886, -6.677295441714964142, 4.533357778048659803 ) ) ;
#17169=EDGE_LOOP ( 'NONE', ( #14388, #9396, #14525, #12211 ) ) ;
#17173=ORIENTED_EDGE ( 'NONE', *, *, #13260, .F. ) ;
#17189=CARTESIAN_POINT ( 'NONE',  ( -16.75000000000000000, -16.21813761408365195, 13.00000000000000178 ) ) ;
#17190=CARTESIAN_POINT ( 'NONE',  ( 33.27602027394517847, -2.146833986953896822, 6.861505862736165362 ) ) ;
#17191=EDGE_CURVE ( 'NONE', #1012, #14557, #11640, .T. ) ;
#17197=CARTESIAN_POINT ( 'NONE',  ( 28.01872616749444944, -6.841866079205687790, 7.033357778048657138 ) ) ;
#17205=EDGE_CURVE ( 'NONE', #12240, #14461, #7353, .T. ) ;
#17213=DIRECTION ( 'NONE',  ( 0.9928203230275512992, 0.1196152422706610180, 4.006172263299093133E-17 ) ) ;
#17214=VECTOR ( 'NONE', #390, 1000.000000000000227 ) ;
#17215=CARTESIAN_POINT ( 'NONE',  ( 28.52162355051263987, -6.481468097106410475, 4.705209693361159573 ) ) ;
#17220=ORIENTED_EDGE ( 'NONE', *, *, #5162, .F. ) ;
#17221=CARTESIAN_POINT ( 'NONE',  ( 33.56515079149260572, -5.873822666371450119, 4.705209693361159573 ) ) ;
#17222=CARTESIAN_POINT ( 'NONE',  ( 14.00000000000000178, -1.714505518806294835E-15, 10.50000000000000000 ) ) ;
#17223=CARTESIAN_POINT ( 'NONE',  ( 26.31556265977298992, -7.384422263489805793, 5.783357778048663356 ) ) ;
#17237=CARTESIAN_POINT ( 'NONE',  ( 27.93543013035303701, -2.153102235610331316, 6.453230759126468818 ) ) ;
#17238=CARTESIAN_POINT ( 'NONE',  ( 31.01321894478757812, -1.392741288986461212, 5.783357778048668685 ) ) ;
#17239=( BOUNDED_CURVE ( )  B_SPLINE_CURVE ( 2, ( #4965, #17149, #537, #15680, #3260, #7698, #8795, #6332, #13224, #10403, #895, #11761, #3435, #717, #9057, #14328, #11854, #628, #6154, #6242, #17334, #4697, #11677, #7522, #17433, #10226, #3524, #8964, #801, #16055, #15772, #10495, #3624, #9148, #14686, #2267, #2091, #1910, #7433, #17247, #16141, #10836, #1337, #991, #16227, #7965, #7879, #3797, #9316, #3885, #14855, #17616, #13498, #13411, #5136, #17874, #2519, #8044, #17703, #6518, #12309, #2443, #2612, #9566, #5224, #12030, #12387, #1072, #16401, #10655, #9399, #10745, #6594, #12124, #14773, #8226, #5397, #16321, #14941, #13757, #15023, #13582, #1164, #6683, #12218, #17793, #6861, #5313, #3969, #9484, #9226, #1260, #8140, #13670, #15116, #6776, #10915, #16483, #4055, #2703, #2360, #5055, #10574, #3701, #7331, #15289, #5757, #13836, #4323, #153, #11096, #1425, #9653, #3145, #7234, #11177, #8308, #8681, #9928, #12571, #2870, #9734, #246, #4155, #8397, #15203, #14115, #5488, #7146, #6948, #12481, #12657, #2785, #15563, #11272, #67, #14206, #5579, #16944, #15477, #16662, #4501, #16849, #14028, #16750, #4414, #1800, #15384, #4235 ),
 .UNSPECIFIED., .F., .T. ) 
 B_SPLINE_CURVE_WITH_KNOTS ( ( 3, 2, 2, 2, 2, 2, 2, 2, 2, 2, 2, 2, 2, 2, 2, 2, 2, 2, 2, 2, 2, 2, 2, 2, 2, 2, 2, 2, 2, 2, 2, 2, 2, 2, 2, 2, 2, 2, 2, 2, 2, 2, 2, 2, 2, 2, 2, 2, 2, 2, 2, 2, 2, 2, 2, 2, 2, 2, 2, 2, 2, 2, 2, 2, 2, 2, 2, 2, 2, 2, 2, 2, 2, 2, 3 ),
 ( 0.000000000000000000, 0.01322951878407230102, 0.02645903756814460203, 0.03968855635221691519, 0.05291807513628920406, 0.06614759392036151375, 0.07937711270443383038, 0.09260663148850611925, 0.1058361502725784081, 0.1190656690566507248, 0.1322951878407230275, 0.1455247066247953303, 0.1587542254088676608, 0.1719837441929399358, 0.1852132629770122385, 0.1984427817610845690, 0.2116723005451568163, 0.2249018193292291468, 0.2381313381133014495, 0.2513608568973737523, 0.2645903756814460550, 0.2778198944655183578, 0.2910494132495906605, 0.3042789320336629633, 0.3175084508177353215, 0.3307379696018076243, 0.3439674883858798715, 0.3571970071699521743, 0.3704265259540244770, 0.3836560447380968353, 0.3968855635221691380, 0.4101150823062413853, 0.4233446010903136325, 0.4365741198743859908, 0.4498036386584582935, 0.4630331574425305963, 0.4762626762266028990, 0.4894921950106752018, 0.5027217137947475045, 0.5159512325788198073, 0.5291807513628921100, 0.5424102701469644128, 0.5556397889310367155, 0.5688693077151090183, 0.5820988264991813210, 0.5953283452832536238, 0.6085578640673259265, 0.6217873828513982293, 0.6350169016354706431, 0.6482464204195428348, 0.6614759392036152486, 0.6747054579876874403, 0.6879349767717597430, 0.7011644955558321568, 0.7143940143399043485, 0.7276235331239767623, 0.7408530519080489540, 0.7540825706921212568, 0.7673120894761936706, 0.7805416082602658623, 0.7937711270443382761, 0.8070006458284105788, 0.8202301646124827705, 0.8334596833965551843, 0.8466892021806272650, 0.8599187209646996788, 0.8731482397487719815, 0.8863777585328441733, 0.8996072773169165870, 0.9128367961009887788, 0.9260663148850611925, 0.9392958336691334953, 0.9525253524532057980, 0.9657548712372781008, 0.9750618896629086318 ),
 .UNSPECIFIED. ) 
 CURVE ( )  GEOMETRIC_REPRESENTATION_ITEM ( )  RATIONAL_B_SPLINE_CURVE ( ( 1.000000000000000000, 0.8660254037844387076, 1.000000000000000000, 0.8660254037844387076, 1.000000000000000000, 0.8660254037844387076, 1.000000000000000000, 0.8660254037844387076, 1.000000000000000000, 0.8660254037844387076, 1.000000000000000000, 0.8660254037844387076, 1.000000000000000000, 0.8660254037844387076, 1.000000000000000000, 0.8660254037844387076, 1.000000000000000000, 0.8660254037844387076, 1.000000000000000000, 0.8660254037844387076, 1.000000000000000000, 0.8660254037844387076, 1.000000000000000000, 0.8660254037844387076, 1.000000000000000000, 0.8660254037844387076, 1.000000000000000000, 0.8660254037844387076, 1.000000000000000000, 0.8660254037844387076, 1.000000000000000000, 0.8660254037844387076, 1.000000000000000000, 0.8660254037844387076, 1.000000000000000000, 0.8660254037844387076, 1.000000000000000000, 0.8660254037844387076, 1.000000000000000000, 0.8660254037844387076, 1.000000000000000000, 0.8660254037844387076, 1.000000000000000000, 0.8660254037844387076, 1.000000000000000000, 0.8660254037844387076, 1.000000000000000000, 0.8660254037844387076, 1.000000000000000000, 0.8660254037844387076, 1.000000000000000000, 0.8660254037844387076, 1.000000000000000000, 0.8660254037844387076, 1.000000000000000000, 0.8660254037844387076, 1.000000000000000000, 0.8660254037844387076, 1.000000000000000000, 0.8660254037844387076, 1.000000000000000000, 0.8660254037844387076, 1.000000000000000000, 0.8660254037844387076, 1.000000000000000000, 0.8660254037844387076, 1.000000000000000000, 0.8660254037844387076, 1.000000000000000000, 0.8660254037844387076, 1.000000000000000000, 0.8660254037844387076, 1.000000000000000000, 0.8660254037844387076, 1.000000000000000000, 0.8660254037844387076, 1.000000000000000000, 0.8660254037844387076, 1.000000000000000000, 0.8660254037844387076, 1.000000000000000000, 0.8660254037844387076, 1.000000000000000000, 0.8660254037844387076, 1.000000000000000000, 0.8660254037844387076, 1.000000000000000000, 0.8660254037844387076, 1.000000000000000000, 0.8660254037844387076, 1.000000000000000000, 0.8660254037844387076, 1.000000000000000000, 0.8660254037844387076, 1.000000000000000000, 0.8660254037844387076, 1.000000000000000000, 0.8660254037844387076, 1.000000000000000000, 0.8660254037844387076, 1.000000000000000000, 0.8660254037844387076, 1.000000000000000000, 0.8660254037844387076, 1.000000000000000000, 0.8660254037844387076, 1.000000000000000000, 0.8660254037844387076, 1.000000000000000000, 0.8660254037844387076, 1.000000000000000000, 0.8660254037844387076, 1.000000000000000000, 0.8660254037844387076, 1.000000000000000000, 0.8660254037844387076, 1.000000000000000000, 0.8660254037844387076, 1.000000000000000000, 0.8660254037844387076, 1.000000000000000000, 0.8660254037844387076, 1.000000000000000000, 0.8660254037844387076, 1.000000000000000000, 0.8660254037844387076, 1.000000000000000000, 0.8660254037844387076, 1.000000000000000000, 0.8660254037844387076, 1.000000000000000000, 0.8660254037844387076, 1.000000000000000000, 0.8660254037844387076, 1.000000000000000000, 0.8660254037844387076, 1.000000000000000000, 0.8660254037844387076, 1.000000000000000000, 0.8660254037844387076, 1.000000000000000000, 0.8660254037844387076, 1.000000000000000000, 0.8660254037844387076, 1.000000000000000000, 0.8660254037844387076, 1.000000000000000000, 0.9057483453558528019, 0.9441095091726994237 ) ) 
 REPRESENTATION_ITEM ( '' )  );
#17243=VERTEX_POINT ( 'NONE', #4873 ) ;
#17246=CARTESIAN_POINT ( 'NONE',  ( 26.49461065740898391, -7.352653653197164907, 5.783357778048658915 ) ) ;
#17247=CARTESIAN_POINT ( 'NONE',  ( 31.41531425212677675, -1.744041783721344219, 5.783357778048668685 ) ) ;
#17254=CYLINDRICAL_SURFACE ( 'NONE', #11626, 5.000000000000000000 ) ;
#17256=EDGE_CURVE ( 'NONE', #6312, #15379, #14002, .T. ) ;
#17259=EDGE_LOOP ( 'NONE', ( #5661, #9814, #8471, #11651 ) ) ;
#17261=CYLINDRICAL_SURFACE ( 'NONE', #15069, 2.749999999999992895 ) ;
#17262=VERTEX_POINT ( 'NONE', #10130 ) ;
#17263=CARTESIAN_POINT ( 'NONE',  ( 26.31556265977298992, -7.384422263489805793, 5.783357778048663356 ) ) ;
#17264=CARTESIAN_POINT ( 'NONE',  ( 27.42949161418789572, -3.278323244185609830, 8.283357778048664244 ) ) ;
#17265=ORIENTED_EDGE ( 'NONE', *, *, #7690, .T. ) ;
#17273=DIRECTION ( 'NONE',  ( 0.9928203230275512992, 0.1196152422706610180, 4.006172263299093133E-17 ) ) ;
#17275=ADVANCED_FACE ( 'NONE', ( #13138 ), #15956, .T. ) ;
#17281=CARTESIAN_POINT ( 'NONE',  ( -23.00000000000000000, -16.21813761408365195, 13.00000000000000178 ) ) ;
#17283=CARTESIAN_POINT ( 'NONE',  ( 31.41114436565740320, -6.133337902414513820, 6.861505862736158257 ) ) ;
#17286=DIRECTION ( 'NONE',  ( 0.8243186046180107640, -0.5661261679878571984, 0.000000000000000000 ) ) ;
#17287=CARTESIAN_POINT ( 'NONE',  ( 27.42949161418789217, -3.278323244185609830, 8.283357778048666020 ) ) ;
#17290=DIRECTION ( 'NONE',  ( 0.000000000000000000, 3.469446951953614189E-16, 1.000000000000000000 ) ) ;
#17293=CARTESIAN_POINT ( 'NONE',  ( -7.499998387031003411, -20.49508120620799900, 12.00000000000000000 ) ) ;
#17295=EDGE_CURVE ( 'NONE', #17243, #6446, #7615, .T. ) ;
#17297=DIRECTION ( 'NONE',  ( 0.000000000000000000, 0.000000000000000000, -1.000000000000000000 ) ) ;
#17301=DIRECTION ( 'NONE',  ( -0.000000000000000000, -0.000000000000000000, 1.000000000000000000 ) ) ;
#17303=EDGE_CURVE ( 'NONE', #14701, #3274, #17239, .T. ) ;
#17304=CARTESIAN_POINT ( 'NONE',  ( 28.26310972651430120, -2.123820177930694442, 5.783357778048668685 ) ) ;
#17305=ORIENTED_EDGE ( 'NONE', *, *, #4330, .T. ) ;
#17306=EDGE_CURVE ( 'NONE', #14000, #11482, #5377, .T. ) ;
#17310=CARTESIAN_POINT ( 'NONE',  ( 31.87075164095941915, -4.197052703815608687, 7.939653947423662039 ) ) ;
#17311=CARTESIAN_POINT ( 'NONE',  ( -26.79938379600875109, -11.23877132507977805, 14.03531701109484331 ) ) ;
#17315=CARTESIAN_POINT ( 'NONE',  ( 33.95908713831674675, -3.945449517755637903, 5.783357778048663356 ) ) ;
#17318=CARTESIAN_POINT ( 'NONE',  ( 25.11802603177690330, -16.03270077640482683, 10.53798182577225084 ) ) ;
#17326=CARTESIAN_POINT ( 'NONE',  ( 30.03006034954003667, -2.965006068755446478, 8.283357778048664244 ) ) ;
#17327=VERTEX_POINT ( 'NONE', #7419 ) ;
#17333=CARTESIAN_POINT ( 'NONE',  ( 26.59574320524588842, -2.314508053356755024, 6.453230759126468818 ) ) ;
#17334=CARTESIAN_POINT ( 'NONE',  ( 32.93470988637010066, -5.949778345213319497, 4.705209693361159573 ) ) ;
#17336=SURFACE_SIDE_STYLE ('',( #6520 ) ) ;
#17343=DIRECTION ( 'NONE',  ( 0.9928203230275510771, 0.1196152422706610596, 9.614813431917826478E-17 ) ) ;
#17348=ORIENTED_EDGE ( 'NONE', *, *, #7732, .T. ) ;
#17367=ORIENTED_EDGE ( 'NONE', *, *, #17144, .F. ) ;
#17370=AXIS2_PLACEMENT_3D ( 'NONE', #58, #17945, #15552 ) ;
#17374=PLANE ( 'NONE',  #1498 ) ;
#17375=CARTESIAN_POINT ( 'NONE',  ( -5.499998817156067865, -20.49639288455253450, 6.000000000000000000 ) ) ;
#17380=EDGE_LOOP ( 'NONE', ( #8697, #8136, #10551, #5660 ) ) ;
#17388=FACE_OUTER_BOUND ( 'NONE', #1610, .T. ) ;
#17391=CARTESIAN_POINT ( 'NONE',  ( 30.08145424927873535, -6.930706697444451336, 5.783357778048664244 ) ) ;
#17392=EDGE_CURVE ( 'NONE', #6854, #16186, #11978, .T. ) ;
#17402=CARTESIAN_POINT ( 'NONE',  ( 33.64386668575551198, -3.983427357176565486, 3.283357778048664244 ) ) ;
#17408=CARTESIAN_POINT ( 'NONE',  ( 32.08959525433819238, -2.916745304588811649, 3.627061608673666893 ) ) ;
#17410=B_SPLINE_CURVE_WITH_KNOTS ( 'NONE', 3,
 ( #3603, #6221, #11920, #9293, #14586, #6126, #9203, #2337, #8941, #13384, #6495, #17592, #2067, #16206, #17311, #870, #6402, #15837, #3771, #696, #7496, #13019, #605, #4761, #4848, #10377, #15931, #2162, #780, #7679, #11829, #9373, #17678, #10806, #16380, #5371, #17851, #1313, #15180, #10721, #10890, #5199, #16459, #2582 ),
 .UNSPECIFIED., .F., .F.,
 ( 4, 2, 2, 2, 2, 2, 2, 2, 2, 2, 2, 2, 2, 2, 2, 2, 2, 2, 2, 2, 2, 4 ),
 ( 0.000000000000000000, 0.001235571410315390150, 0.001853357115473088478, 0.002471142820630786805, 0.003706714230946187797, 0.004324499936103893064, 0.004942285641261598764, 0.006177857051577013633, 0.007413428461892427636, 0.008031214167050130734, 0.008648999872207834699, 0.009884571282523253039, 0.01112014269283866964, 0.01235571410315408972, 0.01297349980831179542, 0.01359128551346949765, 0.01482685692378490731, 0.01606242833410031698, 0.01668021403925802268, 0.01729799974441572491, 0.01853357115473113284, 0.01976914256504654077 ),
 .UNSPECIFIED. ) ;
#17413=ORIENTED_EDGE ( 'NONE', *, *, #14153, .F. ) ;
#17418=CARTESIAN_POINT ( 'NONE',  ( 31.37049041475757605, -6.775403295959669947, 5.113484796970852564 ) ) ;
#17424=CARTESIAN_POINT ( 'NONE',  ( 32.46178999037268653, -4.125844254797621957, 3.283357778048664244 ) ) ;
#17426=CIRCLE ( 'NONE', #15068, 5.000000000000000000 ) ;
#17428=CIRCLE ( 'NONE', #13624, 2.000000000000001776 ) ;
#17429=VERTEX_POINT ( 'NONE', #3607 ) ;
#17431=ORIENTED_EDGE ( 'NONE', *, *, #7966, .T. ) ;
#17433=CARTESIAN_POINT ( 'NONE',  ( 32.50119254608192421, -4.121097024973739309, 7.939653947423662039 ) ) ;
#17437=CARTESIAN_POINT ( 'NONE',  ( 33.12669930479518854, -6.563814807098823145, 6.453230759126467042 ) ) ;
#17444=CARTESIAN_POINT ( 'NONE',  ( 17.08564552898659272, -14.18688536295006664, 15.98696333172761719 ) ) ;
#17452=CARTESIAN_POINT ( 'NONE',  ( 26.14503574297738098, -5.691300421908874085, 3.283357778048664688 ) ) ;
#17455=CARTESIAN_POINT ( 'NONE',  ( 26.00347982711925710, -2.723222710571018279, 4.533357778048667797 ) ) ;
#17459=VERTEX_POINT ( 'NONE', #3412 ) ;
#17464=CYLINDRICAL_SURFACE ( 'NONE', #17758, 2.500000000000001776 ) ;
#17466=ADVANCED_FACE ( 'NONE', ( #1977 ), #7499, .F. ) ;
#17475=EDGE_CURVE ( 'NONE', #3702, #15383, #5115, .T. ) ;
#17483=DIRECTION ( 'NONE',  ( -0.000000000000000000, -0.000000000000000000, 1.000000000000000000 ) ) ;
#17485=CARTESIAN_POINT ( 'NONE',  ( 21.42601376483257880, 2.765314980223224417, 6.000000000000000000 ) ) ;
#17486=FACE_OUTER_BOUND ( 'NONE', #13378, .T. ) ;
#17489=AXIS2_PLACEMENT_3D ( 'NONE', #9209, #13210, #702 ) ;
#17496=CARTESIAN_POINT ( 'NONE',  ( 27.19802975513453092, -2.241944418315925613, 5.783357778048667797 ) ) ;
#17497=CARTESIAN_POINT ( 'NONE',  ( 26.01652455409633902, -4.902371455920926380, 5.783357778048663356 ) ) ;
#17498=ORIENTED_EDGE ( 'NONE', *, *, #16801, .F. ) ;
#17503=CARTESIAN_POINT ( 'NONE',  ( 27.23882169172318513, -6.009049854935478052, 3.627061608673662896 ) ) ;
#17510=CARTESIAN_POINT ( 'NONE',  ( 30.15443244188179150, -1.895953141405084086, 5.783357778048668685 ) ) ;
#17525=( BOUNDED_CURVE ( )  B_SPLINE_CURVE ( 3, ( #7302, #12909, #3211, #9012 ),
 .UNSPECIFIED., .F., .T. ) 
 B_SPLINE_CURVE_WITH_KNOTS ( ( 4, 4 ),
 ( 1.514099494053832595, 1.567750514535811712 ),
 .UNSPECIFIED. ) 
 CURVE ( )  GEOMETRIC_REPRESENTATION_ITEM ( )  RATIONAL_B_SPLINE_CURVE ( ( 1.000000000000000000, 0.9997601450507493936, 0.9997601450507493936, 1.000000000000000000 ) ) 
 REPRESENTATION_ITEM ( '' )  );
#17527=CARTESIAN_POINT ( 'NONE',  ( -36.27615609941022257, -23.17738945083361557, -0.000000000000000000 ) ) ;
#17528=LINE ( 'NONE', #4863, #16522 ) ;
#17529=CARTESIAN_POINT ( 'NONE',  ( 26.97551107961034944, -7.694459687869362519, 5.783357778048657138 ) ) ;
#17537=DIRECTION ( 'NONE',  ( 0.1196152422706609902, -0.9928203230275510771, 0.000000000000000000 ) ) ;
#17543=CARTESIAN_POINT ( 'NONE',  ( 23.43390247958827288, -9.970148115950962620, 14.83177094038517652 ) ) ;
#17544=EDGE_CURVE ( 'NONE', #2945, #8113, #16307, .T. ) ;
#17550=CARTESIAN_POINT ( 'NONE',  ( 26.75784435724945709, -6.993777436889428323, 7.033357778048657138 ) ) ;
#17554=DIRECTION ( 'NONE',  ( 0.9928203230275512992, 0.1196152422706610180, 4.006172263299093133E-17 ) ) ;
#17558=LINE ( 'NONE', #8166, #9859 ) ;
#17572=DIRECTION ( 'NONE',  ( -0.5661261679878573094, 0.8243186046180107640, 0.000000000000000000 ) ) ;
#17575=DIRECTION ( 'NONE',  ( 0.000000000000000000, 0.000000000000000000, 1.000000000000000000 ) ) ;
#17581=CARTESIAN_POINT ( 'NONE',  ( 20.00000000000000000, 7.999999999999996447, 12.00000000000000000 ) ) ;
#17583=DIRECTION ( 'NONE',  ( -0.000000000000000000, -1.000000000000000000, 3.469446951953614189E-16 ) ) ;
#17588=CARTESIAN_POINT ( 'NONE',  ( 27.04606801335823718, -3.524390735323772006, 3.627061608673666893 ) ) ;
#17589=ORIENTED_EDGE ( 'NONE', *, *, #15442, .F. ) ;
#17590=ADVANCED_FACE ( 'NONE', ( #9809 ), #8374, .T. ) ;
#17591=CARTESIAN_POINT ( 'NONE',  ( 30.39102621733566423, -5.629271460726126719, 3.627061608673662896 ) ) ;
#17592=CARTESIAN_POINT ( 'NONE',  ( -27.68235608956435811, -12.07326681422359194, 13.80428259828453896 ) ) ;
#17594=EDGE_CURVE ( 'NONE', #2265, #14461, #11351, .T. ) ;
#17605=CARTESIAN_POINT ( 'NONE',  ( 26.34117031759772942, -2.982346454214467535, 6.861505862736165362 ) ) ;
#17611=CARTESIAN_POINT ( 'NONE',  ( 27.26436163736424945, -2.571311352887278190, 4.533357778048667797 ) ) ;
#17612=VERTEX_POINT ( 'NONE', #4478 ) ;
#17615=CARTESIAN_POINT ( 'NONE',  ( 31.91459173804834748, -5.445711903524953712, 7.939653947423658487 ) ) ;
#17616=CARTESIAN_POINT ( 'NONE',  ( 30.78487334700428235, -1.819997462563214263, 5.783357778048668685 ) ) ;
#17620=EDGE_CURVE ( 'NONE', #17612, #6838, #15735, .T. ) ;
#17622=DIRECTION ( 'NONE',  ( 0.000000000000000000, 0.000000000000000000, -1.000000000000000000 ) ) ;
#17624=CARTESIAN_POINT ( 'NONE',  ( 29.37220822929407760, -7.016156836349003001, 5.783357778048657138 ) ) ;
#17625=DIRECTION ( 'NONE',  ( -0.000000000000000000, -0.000000000000000000, -1.000000000000000000 ) ) ;
#17626=LINE ( 'NONE', #16065, #16014 ) ;
#17629=CARTESIAN_POINT ( 'NONE',  ( 18.46842688268906230, -11.90892979872008084, 15.77307170257308933 ) ) ;
#17630=EDGE_CURVE ( 'NONE', #11134, #3677, #15616, .T. ) ;
#17636=AXIS2_PLACEMENT_3D ( 'NONE', #7275, #1652, #9966 ) ;
#17638=CARTESIAN_POINT ( 'NONE',  ( 31.51169109130924184, -2.986371343527201905, 7.939653947423662927 ) ) ;
#17659=AXIS2_PLACEMENT_3D ( 'NONE', #5026, #8012, #13551 ) ;
#17668=CARTESIAN_POINT ( 'NONE',  ( 25.89690931182567724, -3.909551132893385184, 5.783357778048662468 ) ) ;
#17673=CARTESIAN_POINT ( 'NONE',  ( 31.87265695910486230, -5.650636735497883478, 3.283357778048663800 ) ) ;
#17677=CARTESIAN_POINT ( 'NONE',  ( 28.30694982360322953, -3.372479377640031473, 3.627061608673666893 ) ) ;
#17678=CARTESIAN_POINT ( 'NONE',  ( -18.90926271784950075, -11.47470670281267857, 15.70082023719634989 ) ) ;
#17679=LINE ( 'NONE', #12365, #13577 ) ;
#17689=CARTESIAN_POINT ( 'NONE',  ( 26.98483462626008134, -4.785709214840094816, 3.627061608673664228 ) ) ;
#17692=CYLINDRICAL_SURFACE ( 'NONE', #11639, 2.500000000000001776 ) ;
#17694=CARTESIAN_POINT ( 'NONE',  ( 32.69811611091622439, -2.216460025892273311, 4.705209693361168455 ) ) ;
#17695=CARTESIAN_POINT ( 'NONE',  ( 27.32822876973539294, -6.198150586942257512, 8.283357778048658915 ) ) ;
#17696=VECTOR ( 'NONE', #12413, 1000.000000000000000 ) ;
#17697=ORIENTED_EDGE ( 'NONE', *, *, #12076, .F. ) ;
#17698=VERTEX_POINT ( 'NONE', #7397 ) ;
#17700=CARTESIAN_POINT ( 'NONE',  ( 33.42946061375642586, -6.517141185936593750, 5.783357778048658027 ) ) ;
#17703=CARTESIAN_POINT ( 'NONE',  ( 30.93831368681553684, -6.190304661545915188, 6.861505862736157368 ) ) ;
#17704=ORIENTED_EDGE ( 'NONE', *, *, #3137, .F. ) ;
#17707=CARTESIAN_POINT ( 'NONE',  ( 32.26971135134834867, -1.630906943779925955, 6.453230759126469707 ) ) ;
#17710=CARTESIAN_POINT ( 'NONE',  ( 33.76207435632690590, -3.969185667289998332, 7.939653947423662039 ) ) ;
#17713=CARTESIAN_POINT ( 'NONE',  ( 31.95146207396702565, -5.641142275435199416, 3.283357778048663356 ) ) ;
#17714=DIRECTION ( 'NONE',  ( 0.1113444980252557837, 0.9937818688019538493, 0.000000000000000000 ) ) ;
#17715=LINE ( 'NONE', #3537, #973 ) ;
#17718=VECTOR ( 'NONE', #6752, 1000.000000000000227 ) ;
#17720=ORIENTED_EDGE ( 'NONE', *, *, #5277, .T. ) ;
#17726=CARTESIAN_POINT ( 'NONE',  ( 30.86385689617753059, -5.572304701594727128, 3.627061608673662896 ) ) ;
#17731=DIRECTION ( 'NONE',  ( -0.1196152422706610735, 0.9928203230275511881, 0.000000000000000000 ) ) ;
#17735=AXIS2_PLACEMENT_3D ( 'NONE', #16690, #11405, #15415 ) ;
#17741=( BOUNDED_CURVE ( )  B_SPLINE_CURVE ( 2, ( #12585, #9494, #10846, #17966, #15035, #12399, #1270, #1176, #8319 ),
 .UNSPECIFIED., .F., .T. ) 
 B_SPLINE_CURVE_WITH_KNOTS ( ( 3, 2, 2, 2, 3 ),
 ( 0.8269230769230769829, 0.8333333333333333703, 0.8461538461538461453, 0.8589743589743589203, 0.8653846153846154188 ),
 .UNSPECIFIED. ) 
 CURVE ( )  GEOMETRIC_REPRESENTATION_ITEM ( )  RATIONAL_B_SPLINE_CURVE ( ( 0.9330127018922192983, 0.9330127018922198534, 1.000000000000000000, 0.8660254037844387076, 1.000000000000000000, 0.8660254037844387076, 1.000000000000000000, 0.9330127018922187432, 0.9330127018922192983 ) ) 
 REPRESENTATION_ITEM ( '' )  );
#17751=CARTESIAN_POINT ( 'NONE',  ( -19.43845002722867221, 2.988003976273734263, 6.000000000000000000 ) ) ;
#17756=DIRECTION ( 'NONE',  ( 0.000000000000000000, 0.000000000000000000, -1.000000000000000000 ) ) ;
#17758=AXIS2_PLACEMENT_3D ( 'NONE', #6182, #17273, #9171 ) ;
#17761=CARTESIAN_POINT ( 'NONE',  ( 31.30979230060565044, -7.172264396038955603, 5.783357778048657138 ) ) ;
#17764=CARTESIAN_POINT ( 'NONE',  ( 30.91186687973582536, -2.431667782610909434, 6.861505862736166250 ) ) ;
#17765=CARTESIAN_POINT ( 'NONE',  ( -23.00000000000000000, -16.21813761408365195, 13.00000000000000355 ) ) ;
#17766=CARTESIAN_POINT ( 'NONE',  ( 28.74176732417158320, -7.092112515190875044, 5.783357778048669573 ) ) ;
#17775=ORIENTED_EDGE ( 'NONE', *, *, #15110, .F. ) ;
#17780=CARTESIAN_POINT ( 'NONE',  ( 25.83772294520678159, -3.669972453104032084, 7.939653947423664704 ) ) ;
#17781=CARTESIAN_POINT ( 'NONE',  ( 28.86293393808771057, -2.678523738846987357, 6.861505862736165362 ) ) ;
#17782=CARTESIAN_POINT ( 'NONE',  ( 32.97895737133300287, -1.545456804875372958, 6.453230759126471483 ) ) ;
#17784=DIRECTION ( 'NONE',  ( -0.000000000000000000, -0.000000000000000000, 1.000000000000000000 ) ) ;
#17786=CARTESIAN_POINT ( 'NONE',  ( 29.39961944441754227, -3.040961747597316300, 8.283357778048664244 ) ) ;
#17790=CARTESIAN_POINT ( 'NONE',  ( 30.88125018618674744, -3.062327022369072171, 7.939653947423664704 ) ) ;
#17792=CARTESIAN_POINT ( 'NONE',  ( 25.74999999999999645, -16.21813761408365195, 0.000000000000000000 ) ) ;
#17793=CARTESIAN_POINT ( 'NONE',  ( 29.14753769709988518, -3.271205139184214072, 7.939653947423662927 ) ) ;
#17799=CARTESIAN_POINT ( 'NONE',  ( 29.71979337562451207, -1.938121702948446323, 5.783357778048662468 ) ) ;
#17809=AXIS2_PLACEMENT_3D ( 'NONE', #4974, #17625, #9156 ) ;
#17810=DIRECTION ( 'NONE',  ( -0.6000000000000000888, -0.7999999999999999334, -0.000000000000000000 ) ) ;
#17812=ORIENTED_EDGE ( 'NONE', *, *, #3192, .T. ) ;
#17813=CARTESIAN_POINT ( 'NONE',  ( 31.91006497951310550, -2.311404624444611589, 4.705209693361167567 ) ) ;
#17815=CARTESIAN_POINT ( 'NONE',  ( 29.45101334415624095, -7.006662376286320715, 5.783357778048669573 ) ) ;
#17816=EDGE_CURVE ( 'NONE', #9808, #15632, #13088, .T. ) ;
#17819=EDGE_CURVE ( 'NONE', #122, #4537, #17525, .T. ) ;
#17827=CARTESIAN_POINT ( 'NONE',  ( 30.35023428074701002, -1.862166024106576057, 5.783357778048662468 ) ) ;
#17832=VERTEX_POINT ( 'NONE', #6286 ) ;
#17847=ORIENTED_EDGE ( 'NONE', *, *, #528, .F. ) ;
#17850=CARTESIAN_POINT ( 'NONE',  ( 28.41655006632555569, -6.494127376913395366, 6.861505862736157368 ) ) ;
#17851=CARTESIAN_POINT ( 'NONE',  ( -17.60362937644963921, -13.05831870693043584, 15.90927928682413928 ) ) ;
#17855=ORIENTED_EDGE ( 'NONE', *, *, #3681, .T. ) ;
#17856=CARTESIAN_POINT ( 'NONE',  ( 0.000000000000000000, 0.000000000000000000, 8.700000000000001066 ) ) ;
#17858=VERTEX_POINT ( 'NONE', #14371 ) ;
#17861=DIRECTION ( 'NONE',  ( 0.000000000000000000, 0.000000000000000000, 1.000000000000000000 ) ) ;
#17864=EDGE_CURVE ( 'NONE', #2720, #4427, #3263, .T. ) ;
#17865=CARTESIAN_POINT ( 'NONE',  ( 30.88577694472199298, -6.196634301449400084, 4.705209693361160461 ) ) ;
#17866=CARTESIAN_POINT ( 'NONE',  ( 32.95080301609915097, -1.548848848676412260, 5.783357778048663356 ) ) ;
#17869=ORIENTED_EDGE ( 'NONE', *, *, #1871, .T. ) ;
#17871=CARTESIAN_POINT ( 'NONE',  ( 32.14213199643172914, -2.910415664685331638, 7.939653947423664704 ) ) ;
#17873=ORIENTED_EDGE ( 'NONE', *, *, #14468, .T. ) ;
#17874=CARTESIAN_POINT ( 'NONE',  ( 31.02146712245815507, -5.553315781884258229, 3.627061608673662896 ) ) ;
#17877=ORIENTED_EDGE ( 'NONE', *, *, #15704, .F. ) ;
#17892=CARTESIAN_POINT ( 'NONE',  ( 31.38469755857769528, -2.374701023479507178, 6.861505862736165362 ) ) ;
#17895=CARTESIAN_POINT ( 'NONE',  ( 28.16881664323204859, -6.096876348486420127, 3.283357778048663356 ) ) ;
#17902=VERTEX_POINT ( 'NONE', #10615 ) ;
#17906=DIRECTION ( 'NONE',  ( 1.000000000000000000, 0.000000000000000000, 0.000000000000000000 ) ) ;
#17918=ORIENTED_EDGE ( 'NONE', *, *, #17306, .F. ) ;
#17919=DIRECTION ( 'NONE',  ( 0.1113444980252557837, 0.9937818688019538493, 0.000000000000000000 ) ) ;
#17930=CARTESIAN_POINT ( 'NONE',  ( 25.74134610602432360, -2.427642893298174620, 5.783357778048668685 ) ) ;
#17932=CARTESIAN_POINT ( 'NONE',  ( 20.27597925817430635, -21.85809165190032743, 15.46244260681514326 ) ) ;
#17933=ORIENTED_EDGE ( 'NONE', *, *, #12430, .F. ) ;
#17936=CARTESIAN_POINT ( 'NONE',  ( 26.31556265977298992, -7.384422263489805793, 5.783357778048663356 ) ) ;
#17938=AXIS2_PLACEMENT_3D ( 'NONE', #5925, #13912, #8479 ) ;
#17939=DIRECTION ( 'NONE',  ( -1.000000000000000000, 0.000000000000000000, 0.000000000000000000 ) ) ;
#17942=CARTESIAN_POINT ( 'NONE',  ( 26.45077056032005913, -6.103994453487816330, 3.627061608673662896 ) ) ;
#17943=CARTESIAN_POINT ( 'NONE',  ( 29.41022140756759029, -3.239556939666760726, 3.627061608673666893 ) ) ;
#17945=DIRECTION ( 'NONE',  ( 0.000000000000000000, 0.000000000000000000, -1.000000000000000000 ) ) ;
#17947=EDGE_CURVE ( 'NONE', #14980, #3522, #4159, .T. ) ;
#17951=CARTESIAN_POINT ( 'NONE',  ( 32.12473870642251939, -5.420393343910986594, 3.627061608673662896 ) ) ;
#17952=DIRECTION ( 'NONE',  ( -0.7681011886108269904, -0.5760758914581204371, 0.2795659695588260107 ) ) ;
#17953=ORIENTED_EDGE ( 'NONE', *, *, #549, .F. ) ;
#17955=EDGE_CURVE ( 'NONE', #9808, #3274, #14377, .T. ) ;
#17956=CARTESIAN_POINT ( 'NONE',  ( 23.02601376483258022, 3.965314980223224151, 0.000000000000000000 ) ) ;
#17958=CARTESIAN_POINT ( 'NONE',  ( 27.24868051476284236, -2.235842002054281075, 5.113484796970861446 ) ) ;
#17961=CARTESIAN_POINT ( 'NONE',  ( 29.40036258452792950, -7.012764792547963033, 5.113484796970851676 ) ) ;
#17964=DIRECTION ( 'NONE',  ( -0.1196152422706610735, 0.9928203230275511881, 0.000000000000000000 ) ) ;
#17966=CARTESIAN_POINT ( 'NONE',  ( 26.69778786461289855, -6.274106265784127778, 8.283357778048660691 ) ) ;
ENDSEC;
END-ISO-10303-21;
